ISO-10303-21;
HEADER;
FILE_DESCRIPTION (('STEP AP214'),
    '1' );
FILE_NAME ('big gear_ISO - Spur gear 2M 80T 20PA 10FW ---S80A75H50L20.0N.step',
    '2026-09-30T12:41:04',
    ( '' ),
    ( '' ),
    'SwSTEP 2.0',
    'SolidWorks 2026',
    '' );
FILE_SCHEMA (( 'AUTOMOTIVE_DESIGN' ));
ENDSEC;

DATA;
#5=EDGE_LOOP ( 'NONE', ( #19827, #27831, #3071, #30075 ) ) ;
#7=CARTESIAN_POINT ( 'NONE',  ( 0.000000000000000000, -15.33399622253423722, -80.55351364060604169 ) ) ;
#13=LINE ( 'NONE', #16590, #37780 ) ;
#14=CARTESIAN_POINT ( 'NONE',  ( 10.00000000000000000, 68.26794271651262136, 31.47745569255165066 ) ) ;
#23=LINE ( 'NONE', #29422, #16608 ) ;
#24=DIRECTION ( 'NONE',  ( -1.000000000000000000, 0.000000000000000000, -0.000000000000000000 ) ) ;
#25=ORIENTED_EDGE ( 'NONE', *, *, #6574, .F. ) ;
#28=DIRECTION ( 'NONE',  ( 0.000000000000000000, 0.000000000000000000, 1.000000000000000000 ) ) ;
#29=CARTESIAN_POINT ( 'NONE',  ( 10.00000000000000000, 31.46837873494978055, 68.27212725128286763 ) ) ;
#34=DIRECTION ( 'NONE',  ( -1.000000000000000000, 0.000000000000000000, 0.000000000000000000 ) ) ;
#35=CARTESIAN_POINT ( 'NONE',  ( 10.00000000000000000, 0.000000000000000000, 0.000000000000000000 ) ) ;
#38=EDGE_CURVE ( 'NONE', #36456, #38853, #23936, .T. ) ;
#41=ADVANCED_FACE ( 'NONE', ( #48333 ), #4038, .T. ) ;
#43=DIRECTION ( 'NONE',  ( -1.000000000000000000, -0.000000000000000000, -0.000000000000000000 ) ) ;
#45=CARTESIAN_POINT ( 'NONE',  ( 0.000000000000000000, 0.000000000000000000, 0.000000000000000000 ) ) ;
#47=AXIS2_PLACEMENT_3D ( 'NONE', #3704, #48253, #7378 ) ;
#52=ORIENTED_EDGE ( 'NONE', *, *, #13978, .F. ) ;
#53=ADVANCED_FACE ( 'NONE', ( #40751 ), #41250, .T. ) ;
#58=DIRECTION ( 'NONE',  ( -1.000000000000000000, -0.000000000000000000, 0.000000000000000000 ) ) ;
#78=CYLINDRICAL_SURFACE ( 'NONE', #28876, 31.99999999999999289 ) ;
#85=DIRECTION ( 'NONE',  ( -1.000000000000000000, 0.000000000000000000, 0.000000000000000000 ) ) ;
#88=DIRECTION ( 'NONE',  ( 0.000000000000000000, 0.000000000000000000, 1.000000000000000000 ) ) ;
#89=ORIENTED_EDGE ( 'NONE', *, *, #44736, .T. ) ;
#90=CARTESIAN_POINT ( 'NONE',  ( 50.00005079999999680, 12.24744871391589207, 2.500000000000000000 ) ) ;
#91=CARTESIAN_POINT ( 'NONE',  ( 10.00000000000000000, -77.49459641780886443, 0.8261519478428377417 ) ) ;
#94=DIRECTION ( 'NONE',  ( 0.000000000000000000, 0.7071067811865436870, 0.7071067811865512365 ) ) ;
#99=CARTESIAN_POINT ( 'NONE',  ( 10.00000000000000000, 66.50666863322000211, 39.78640506895629869 ) ) ;
#101=EDGE_CURVE ( 'NONE', #47663, #34988, #41134, .T. ) ;
#103=AXIS2_PLACEMENT_3D ( 'NONE', #39241, #24552, #10332 ) ;
#105=DIRECTION ( 'NONE',  ( 0.000000000000000000, 0.000000000000000000, -1.000000000000000000 ) ) ;
#114=CARTESIAN_POINT ( 'NONE',  ( 10.00000000000000000, -75.11764819372145041, 29.05362095685286761 ) ) ;
#117=AXIS2_PLACEMENT_3D ( 'NONE', #11604, #8408, #37057 ) ;
#120=ORIENTED_EDGE ( 'NONE', *, *, #24250, .F. ) ;
#129=DIRECTION ( 'NONE',  ( 0.000000000000000000, 0.000000000000000000, 1.000000000000000000 ) ) ;
#146=EDGE_CURVE ( 'NONE', #7626, #23140, #26277, .T. ) ;
#150=LINE ( 'NONE', #15351, #37624 ) ;
#151=DIRECTION ( 'NONE',  ( 0.000000000000000000, 0.000000000000000000, -1.000000000000000000 ) ) ;
#153=CARTESIAN_POINT ( 'NONE',  ( 10.00000000000000000, 69.42325613327439271, 34.44570377933623462 ) ) ;
#167=ORIENTED_EDGE ( 'NONE', *, *, #8723, .T. ) ;
#178=EDGE_LOOP ( 'NONE', ( #25337, #24092, #4200, #25066 ) ) ;
#189=DIRECTION ( 'NONE',  ( -1.000000000000000000, 0.000000000000000000, 0.000000000000000000 ) ) ;
#192=CIRCLE ( 'NONE', #29910, 31.99999999999999645 ) ;
#197=EDGE_CURVE ( 'NONE', #46520, #36004, #14581, .T. ) ;
#202=DIRECTION ( 'NONE',  ( -1.000000000000000000, 0.000000000000000000, 0.000000000000000000 ) ) ;
#204=ORIENTED_EDGE ( 'NONE', *, *, #32028, .T. ) ;
#205=CARTESIAN_POINT ( 'NONE',  ( 10.00000000000000000, 73.44644590900061587, 24.73286445877730699 ) ) ;
#209=DIRECTION ( 'NONE',  ( 1.000000000000000000, 0.000000000000000000, 0.000000000000000000 ) ) ;
#216=CARTESIAN_POINT ( 'NONE',  ( 0.000000000000000000, 66.50666863322000211, 39.78640506895629159 ) ) ;
#217=CARTESIAN_POINT ( 'NONE',  ( 5.000000000000000000, -77.16300072079641836, -27.74655509720751567 ) ) ;
#219=AXIS2_PLACEMENT_3D ( 'NONE', #16274, #42449, #45632 ) ;
#224=EDGE_LOOP ( 'NONE', ( #47074, #36686, #31550, #45019 ) ) ;
#225=UNCERTAINTY_MEASURE_WITH_UNIT (LENGTH_MEASURE( 1.000000000000000082E-05 ), #18543, 'distance_accuracy_value', 'NONE');
#226=CARTESIAN_POINT ( 'NONE',  ( 0.000000000000000000, 39.78640506895604290, 66.50666863322015843 ) ) ;
#227=CYLINDRICAL_SURFACE ( 'NONE', #7289, 31.99999999999999289 ) ;
#230=EDGE_LOOP ( 'NONE', ( #30613, #47609, #22194, #5952 ) ) ;
#232=FACE_OUTER_BOUND ( 'NONE', #26033, .T. ) ;
#233=CIRCLE ( 'NONE', #34611, 32.00000000000000000 ) ;
#234=AXIS2_PLACEMENT_3D ( 'NONE', #44816, #29883, #40658 ) ;
#246=ORIENTED_EDGE ( 'NONE', *, *, #42379, .F. ) ;
#255=EDGE_CURVE ( 'NONE', #32703, #15443, #43843, .T. ) ;
#258=DIRECTION ( 'NONE',  ( -1.000000000000000000, -0.000000000000000000, 0.000000000000000000 ) ) ;
#264=CARTESIAN_POINT ( 'NONE',  ( 10.00000000000000000, 51.03279382321166224, -55.19960302592011914 ) ) ;
#265=ORIENTED_EDGE ( 'NONE', *, *, #11352, .T. ) ;
#270=VERTEX_POINT ( 'NONE', #3695 ) ;
#271=CARTESIAN_POINT ( 'NONE',  ( 0.000000000000000000, 0.000000000000000000, 0.000000000000000000 ) ) ;
#280=CARTESIAN_POINT ( 'NONE',  ( 0.000000000000000000, 55.38113227695782115, 54.21277698773695164 ) ) ;
#282=DIRECTION ( 'NONE',  ( -1.000000000000000000, -0.000000000000000000, 0.000000000000000000 ) ) ;
#291=DIRECTION ( 'NONE',  ( 0.000000000000000000, 0.8910065241883657894, 0.4539904997395510788 ) ) ;
#292=ADVANCED_FACE ( 'NONE', ( #26219 ), #25226, .T. ) ;
#294=AXIS2_PLACEMENT_3D ( 'NONE', #42649, #20350, #47033 ) ;
#298=VECTOR ( 'NONE', #22798, 1000.000000000000000 ) ;
#300=CIRCLE ( 'NONE', #29270, 31.99999999999998934 ) ;
#301=LINE ( 'NONE', #38005, #1852 ) ;
#313=CIRCLE ( 'NONE', #39395, 32.00000000000000000 ) ;
#317=EDGE_CURVE ( 'NONE', #20770, #27040, #8563, .T. ) ;
#319=DIRECTION ( 'NONE',  ( 0.000000000000000000, -1.000000000000000000, -1.047444401652940007E-14 ) ) ;
#328=ORIENTED_EDGE ( 'NONE', *, *, #15612, .F. ) ;
#334=LINE ( 'NONE', #7681, #29329 ) ;
#338=CARTESIAN_POINT ( 'NONE',  ( 5.000000000000002665, -80.28980883073769803, 16.65972982744906261 ) ) ;
#339=VECTOR ( 'NONE', #11184, 1000.000000000000000 ) ;
#347=CARTESIAN_POINT ( 'NONE',  ( 0.000000000000000000, 68.27212725128275395, -31.46837873495001503 ) ) ;
#349=CYLINDRICAL_SURFACE ( 'NONE', #37017, 77.49899999999999523 ) ;
#361=VERTEX_POINT ( 'NONE', #3941 ) ;
#368=VECTOR ( 'NONE', #28016, 1000.000000000000000 ) ;
#371=VERTEX_POINT ( 'NONE', #8335 ) ;
#381=ORIENTED_EDGE ( 'NONE', *, *, #30250, .F. ) ;
#386=FACE_OUTER_BOUND ( 'NONE', #9470, .T. ) ;
#398=CARTESIAN_POINT ( 'NONE',  ( 5.000000000000002665, 80.55351364060589958, 15.33399622253511829 ) ) ;
#404=DIRECTION ( 'NONE',  ( -1.000000000000000000, 0.000000000000000000, 0.000000000000000000 ) ) ;
#415=DIRECTION ( 'NONE',  ( 0.000000000000000000, -0.9723699203976740035, -0.2334453638559161881 ) ) ;
#422=LINE ( 'NONE', #22928, #45953 ) ;
#425=DIRECTION ( 'NONE',  ( 0.000000000000000000, 0.000000000000000000, 1.000000000000000000 ) ) ;
#431=CARTESIAN_POINT ( 'NONE',  ( 5.000000000000002665, -81.50828551894234408, 8.966570791700407383 ) ) ;
#433=ORIENTED_EDGE ( 'NONE', *, *, #40581, .T. ) ;
#434=AXIS2_PLACEMENT_3D ( 'NONE', #9833, #1772, #36012 ) ;
#436=EDGE_CURVE ( 'NONE', #26945, #36459, #32495, .T. ) ;
#440=CIRCLE ( 'NONE', #27049, 77.49900000000000944 ) ;
#442=EDGE_CURVE ( 'NONE', #1544, #24479, #1223, .T. ) ;
#444=DIRECTION ( 'NONE',  ( 0.000000000000000000, 0.000000000000000000, 1.000000000000000000 ) ) ;
#462=FACE_OUTER_BOUND ( 'NONE', #2649, .T. ) ;
#467=LINE ( 'NONE', #3892, #11924 ) ;
#469=CARTESIAN_POINT ( 'NONE',  ( 0.000000000000000000, 0.000000000000000000, 0.000000000000000000 ) ) ;
#471=EDGE_CURVE ( 'NONE', #36574, #26337, #5917, .T. ) ;
#481=LINE ( 'NONE', #3406, #9026 ) ;
#495=AXIS2_PLACEMENT_3D ( 'NONE', #15450, #22781, #48249 ) ;
#502=ORIENTED_EDGE ( 'NONE', *, *, #10661, .T. ) ;
#505=EDGE_CURVE ( 'NONE', #45334, #15443, #24468, .T. ) ;
#514=CIRCLE ( 'NONE', #27902, 82.00000000000000000 ) ;
#521=CARTESIAN_POINT ( 'NONE',  ( 5.000000000000000000, 64.81221759200343513, 50.23322058963371006 ) ) ;
#523=ORIENTED_EDGE ( 'NONE', *, *, #34532, .F. ) ;
#528=CARTESIAN_POINT ( 'NONE',  ( 10.00000000000000000, 0.000000000000000000, 0.000000000000000000 ) ) ;
#531=FACE_OUTER_BOUND ( 'NONE', #25724, .T. ) ;
#534=DIRECTION ( 'NONE',  ( -1.000000000000000000, 0.000000000000000000, 0.000000000000000000 ) ) ;
#535=CARTESIAN_POINT ( 'NONE',  ( 0.000000000000000000, -65.59268652807183742, -36.72794159290312166 ) ) ;
#538=ORIENTED_EDGE ( 'NONE', *, *, #45114, .T. ) ;
#561=EDGE_CURVE ( 'NONE', #22588, #42551, #8244, .T. ) ;
#580=ORIENTED_EDGE ( 'NONE', *, *, #37141, .T. ) ;
#588=CARTESIAN_POINT ( 'NONE',  ( -10.00000000000000000, 0.000000000000000000, 0.000000000000000000 ) ) ;
#595=DIRECTION ( 'NONE',  ( 0.000000000000000000, 0.000000000000000000, 1.000000000000000000 ) ) ;
#600=CARTESIAN_POINT ( 'NONE',  ( 10.00000000000000000, 20.41045688087824317, 72.35160999960824313 ) ) ;
#603=ORIENTED_EDGE ( 'NONE', *, *, #34407, .F. ) ;
#606=EDGE_CURVE ( 'NONE', #20108, #44086, #18071, .T. ) ;
#607=CYLINDRICAL_SURFACE ( 'NONE', #35407, 77.49899999999999523 ) ;
#610=AXIS2_PLACEMENT_3D ( 'NONE', #4448, #45074, #4672 ) ;
#613=EDGE_LOOP ( 'NONE', ( #246, #43774, #36331, #19803 ) ) ;
#628=CIRCLE ( 'NONE', #35006, 77.49899999999999523 ) ;
#638=CARTESIAN_POINT ( 'NONE',  ( 0.000000000000000000, -73.44644590900043113, -24.73286445877782924 ) ) ;
#641=CARTESIAN_POINT ( 'NONE',  ( 0.000000000000000000, -74.18225833017913828, 34.94270380257611919 ) ) ;
#646=CARTESIAN_POINT ( 'NONE',  ( 0.000000000000000000, 74.18225833017937987, -34.94270380257560049 ) ) ;
#653=DIRECTION ( 'NONE',  ( -1.000000000000000000, 0.000000000000000000, 0.000000000000000000 ) ) ;
#654=DIRECTION ( 'NONE',  ( -1.000000000000000000, 0.000000000000000000, 0.000000000000000000 ) ) ;
#655=AXIS2_PLACEMENT_3D ( 'NONE', #32476, #47405, #13879 ) ;
#657=CYLINDRICAL_SURFACE ( 'NONE', #22466, 32.00000000000000000 ) ;
#666=CIRCLE ( 'NONE', #23340, 82.00000000000000000 ) ;
#672=ORIENTED_EDGE ( 'NONE', *, *, #10306, .F. ) ;
#673=ORIENTED_EDGE ( 'NONE', *, *, #36061, .T. ) ;
#674=DIRECTION ( 'NONE',  ( -1.000000000000000000, 0.000000000000000000, 0.000000000000000000 ) ) ;
#685=ORIENTED_EDGE ( 'NONE', *, *, #43394, .F. ) ;
#689=DIRECTION ( 'NONE',  ( 0.000000000000000000, 0.000000000000000000, 1.000000000000000000 ) ) ;
#690=VERTEX_POINT ( 'NONE', #14422 ) ;
#691=ORIENTED_EDGE ( 'NONE', *, *, #27156, .F. ) ;
#694=ORIENTED_EDGE ( 'NONE', *, *, #7584, .T. ) ;
#696=DIRECTION ( 'NONE',  ( -1.000000000000000000, -0.000000000000000000, 0.000000000000000000 ) ) ;
#697=VERTEX_POINT ( 'NONE', #29093 ) ;
#698=DIRECTION ( 'NONE',  ( -1.000000000000000000, 0.000000000000000000, 0.000000000000000000 ) ) ;
#699=CARTESIAN_POINT ( 'NONE',  ( 0.000000000000000000, 77.19088730480524418, 6.903761155838049390 ) ) ;
#700=CARTESIAN_POINT ( 'NONE',  ( 0.000000000000000000, -17.28742895386031719, -75.54627589209962935 ) ) ;
#702=CARTESIAN_POINT ( 'NONE',  ( 0.000000000000000000, -68.55367621811112144, -44.99326035066125939 ) ) ;
#704=CARTESIAN_POINT ( 'NONE',  ( 10.00000000000000000, -72.35432306680498016, 20.40083707022857951 ) ) ;
#706=CIRCLE ( 'NONE', #20238, 77.49900000000000944 ) ;
#707=CARTESIAN_POINT ( 'NONE',  ( 10.00000000000000000, -46.11716303203234446, 67.80270845531873647 ) ) ;
#708=VERTEX_POINT ( 'NONE', #39885 ) ;
#720=EDGE_CURVE ( 'NONE', #1645, #9950, #13569, .T. ) ;
#725=( GEOMETRIC_REPRESENTATION_CONTEXT ( 3 ) GLOBAL_UNCERTAINTY_ASSIGNED_CONTEXT ( ( #225 ) ) GLOBAL_UNIT_ASSIGNED_CONTEXT ( ( #18543, #39862, #44251 ) ) REPRESENTATION_CONTEXT ( 'NONE', 'WORKASPACE' ) );
#727=ORIENTED_EDGE ( 'NONE', *, *, #37638, .F. ) ;
#737=CIRCLE ( 'NONE', #34347, 32.00000000000000000 ) ;
#743=FACE_OUTER_BOUND ( 'NONE', #7183, .T. ) ;
#747=VERTEX_POINT ( 'NONE', #30811 ) ;
#758=CARTESIAN_POINT ( 'NONE',  ( 10.00000000000000000, 30.41916302227113178, 71.27951684758036777 ) ) ;
#762=CYLINDRICAL_SURFACE ( 'NONE', #35772, 82.00000000000000000 ) ;
#763=CARTESIAN_POINT ( 'NONE',  ( -10.00000000000000000, 0.000000000000000000, 0.000000000000000000 ) ) ;
#767=DIRECTION ( 'NONE',  ( 0.000000000000000000, 0.8526401643540935105, -0.5224985647159466895 ) ) ;
#772=EDGE_CURVE ( 'NONE', #17865, #18490, #11973, .T. ) ;
#773=VERTEX_POINT ( 'NONE', #37412 ) ;
#779=AXIS2_PLACEMENT_3D ( 'NONE', #14946, #44074, #36487 ) ;
#783=CYLINDRICAL_SURFACE ( 'NONE', #16695, 82.00000000000000000 ) ;
#784=ORIENTED_EDGE ( 'NONE', *, *, #48196, .T. ) ;
#794=CARTESIAN_POINT ( 'NONE',  ( 10.00000000000000000, 41.76106447765580043, -62.50884508063379741 ) ) ;
#798=CIRCLE ( 'NONE', #14870, 82.00000000000000000 ) ;
#805=CARTESIAN_POINT ( 'NONE',  ( 10.00000000000000178, 0.000000000000000000, 0.000000000000000000 ) ) ;
#807=CIRCLE ( 'NONE', #34414, 77.49899999999999523 ) ;
#809=CYLINDRICAL_SURFACE ( 'NONE', #2722, 82.00000000000000000 ) ;
#810=DIRECTION ( 'NONE',  ( 0.000000000000000000, 0.4539904997395413644, 0.8910065241883706744 ) ) ;
#816=DIRECTION ( 'NONE',  ( 1.000000000000000000, 0.000000000000000000, 0.000000000000000000 ) ) ;
#817=CYLINDRICAL_SURFACE ( 'NONE', #34592, 77.49899999999999523 ) ;
#821=DIRECTION ( 'NONE',  ( -1.000000000000000000, -0.000000000000000000, 0.000000000000000000 ) ) ;
#823=DIRECTION ( 'NONE',  ( -1.000000000000000000, 0.000000000000000000, 0.000000000000000000 ) ) ;
#826=EDGE_CURVE ( 'NONE', #20918, #40419, #19730, .T. ) ;
#828=VERTEX_POINT ( 'NONE', #23209 ) ;
#837=CIRCLE ( 'NONE', #14133, 82.00000000000000000 ) ;
#840=AXIS2_PLACEMENT_3D ( 'NONE', #6349, #2417, #28626 ) ;
#847=CARTESIAN_POINT ( 'NONE',  ( 10.00000000000000000, -59.46389618801999433, 49.70050353004867816 ) ) ;
#851=ORIENTED_EDGE ( 'NONE', *, *, #38332, .T. ) ;
#856=EDGE_LOOP ( 'NONE', ( #31821, #46197, #31070, #23598 ) ) ;
#863=DIRECTION ( 'NONE',  ( -1.000000000000000000, 0.000000000000000000, 0.000000000000000000 ) ) ;
#865=CARTESIAN_POINT ( 'NONE',  ( 10.00000000000000000, -63.18004540532994184, -44.88180994100446952 ) ) ;
#869=FACE_OUTER_BOUND ( 'NONE', #6666, .T. ) ;
#870=CYLINDRICAL_SURFACE ( 'NONE', #41795, 82.00000000000000000 ) ;
#873=ORIENTED_EDGE ( 'NONE', *, *, #27466, .T. ) ;
#875=CIRCLE ( 'NONE', #1653, 32.00000000000000000 ) ;
#880=DIRECTION ( 'NONE',  ( 0.000000000000000000, -0.5877852522924625900, -0.8090169943749551118 ) ) ;
#882=EDGE_CURVE ( 'NONE', #4419, #38922, #39322, .T. ) ;
#883=CARTESIAN_POINT ( 'NONE',  ( 0.000000000000000000, 0.000000000000000000, 0.000000000000000000 ) ) ;
#887=CARTESIAN_POINT ( 'NONE',  ( 10.00000000000000000, 6.903761155838878061, -77.19088730480517313 ) ) ;
#888=EDGE_CURVE ( 'NONE', #38891, #23195, #37753, .T. ) ;
#890=SURFACE_SIDE_STYLE ('',( #34415 ) ) ;
#893=EDGE_CURVE ( 'NONE', #25663, #39708, #9572, .T. ) ;
#895=ORIENTED_EDGE ( 'NONE', *, *, #6333, .T. ) ;
#898=ORIENTED_EDGE ( 'NONE', *, *, #43837, .F. ) ;
#899=CIRCLE ( 'NONE', #28278, 31.99999999999999645 ) ;
#900=FACE_OUTER_BOUND ( 'NONE', #34327, .T. ) ;
#901=VECTOR ( 'NONE', #25481, 1000.000000000000000 ) ;
#902=ORIENTED_EDGE ( 'NONE', *, *, #18463, .T. ) ;
#912=DIRECTION ( 'NONE',  ( 0.000000000000000000, -0.3826834323650969427, 0.9238795325112838519 ) ) ;
#918=AXIS2_PLACEMENT_3D ( 'NONE', #22717, #15619, #8281 ) ;
#919=VERTEX_POINT ( 'NONE', #32019 ) ;
#934=CARTESIAN_POINT ( 'NONE',  ( 10.00000000000000000, -6.903761155837252694, -77.19088730480530103 ) ) ;
#936=DIRECTION ( 'NONE',  ( -1.000000000000000000, -0.000000000000000000, -0.000000000000000000 ) ) ;
#943=ORIENTED_EDGE ( 'NONE', *, *, #31488, .T. ) ;
#948=ORIENTED_EDGE ( 'NONE', *, *, #40567, .F. ) ;
#949=EDGE_CURVE ( 'NONE', #35290, #37233, #9719, .T. ) ;
#950=DIRECTION ( 'NONE',  ( 0.000000000000000000, 0.9876883405951383255, -0.1564344650402277048 ) ) ;
#954=CARTESIAN_POINT ( 'NONE',  ( 10.00000000000000000, -20.41045688087876897, 72.35160999960810102 ) ) ;
#963=ORIENTED_EDGE ( 'NONE', *, *, #16321, .F. ) ;
#964=AXIS2_PLACEMENT_3D ( 'NONE', #24083, #12583, #5247 ) ;
#967=DIRECTION ( 'NONE',  ( 1.000000000000000000, 0.000000000000000000, 0.000000000000000000 ) ) ;
#969=ORIENTED_EDGE ( 'NONE', *, *, #15817, .T. ) ;
#972=ADVANCED_FACE ( 'NONE', ( #39107 ), #5579, .T. ) ;
#979=CARTESIAN_POINT ( 'NONE',  ( 0.000000000000000000, 0.000000000000000000, 0.000000000000000000 ) ) ;
#980=AXIS2_PLACEMENT_3D ( 'NONE', #9861, #42429, #9370 ) ;
#983=ORIENTED_EDGE ( 'NONE', *, *, #4572, .T. ) ;
#984=CYLINDRICAL_SURFACE ( 'NONE', #17972, 31.99999999999999289 ) ;
#985=CARTESIAN_POINT ( 'NONE',  ( 10.00000000000000000, -62.20884554314051940, 46.21855187248608132 ) ) ;
#987=CIRCLE ( 'NONE', #17401, 77.49900000000002365 ) ;
#991=ADVANCED_FACE ( 'NONE', ( #36397 ), #10703, .T. ) ;
#1004=DIRECTION ( 'NONE',  ( -1.000000000000000000, 0.000000000000000000, 0.000000000000000000 ) ) ;
#1005=ORIENTED_EDGE ( 'NONE', *, *, #37761, .T. ) ;
#1006=CYLINDRICAL_SURFACE ( 'NONE', #40884, 31.99999999999999289 ) ;
#1012=AXIS2_PLACEMENT_3D ( 'NONE', #9094, #45554, #24027 ) ;
#1017=VECTOR ( 'NONE', #5041, 1000.000000000000000 ) ;
#1018=AXIS2_PLACEMENT_3D ( 'NONE', #794, #30668, #45589 ) ;
#1020=AXIS2_PLACEMENT_3D ( 'NONE', #37359, #37842, #19459 ) ;
#1023=ORIENTED_EDGE ( 'NONE', *, *, #15434, .F. ) ;
#1033=EDGE_LOOP ( 'NONE', ( #40955, #9788, #11053, #10812 ) ) ;
#1036=EDGE_CURVE ( 'NONE', #43938, #40433, #32954, .T. ) ;
#1037=DIRECTION ( 'NONE',  ( -1.000000000000000000, 0.000000000000000000, -0.000000000000000000 ) ) ;
#1038=DIRECTION ( 'NONE',  ( 0.000000000000000000, 0.000000000000000000, 1.000000000000000000 ) ) ;
#1042=ORIENTED_EDGE ( 'NONE', *, *, #8061, .F. ) ;
#1050=CIRCLE ( 'NONE', #26849, 82.00000000000000000 ) ;
#1054=EDGE_CURVE ( 'NONE', #20071, #37949, #13540, .T. ) ;
#1055=DIRECTION ( 'NONE',  ( 0.000000000000000000, 0.7071067811865489050, -0.7071067811865462405 ) ) ;
#1057=ORIENTED_EDGE ( 'NONE', *, *, #29918, .F. ) ;
#1060=DIRECTION ( 'NONE',  ( -1.000000000000000000, 0.000000000000000000, 0.000000000000000000 ) ) ;
#1064=AXIS2_PLACEMENT_3D ( 'NONE', #19658, #43416, #17441 ) ;
#1065=CARTESIAN_POINT ( 'NONE',  ( 10.00000000000000000, 0.000000000000000000, 0.000000000000000000 ) ) ;
#1066=CARTESIAN_POINT ( 'NONE',  ( 0.000000000000000000, 75.54627589209943039, 17.28742895386112721 ) ) ;
#1067=DIRECTION ( 'NONE',  ( 0.000000000000000000, 0.000000000000000000, 1.000000000000000000 ) ) ;
#1071=CYLINDRICAL_SURFACE ( 'NONE', #19808, 12.50000000000000000 ) ;
#1076=DIRECTION ( 'NONE',  ( 0.000000000000000000, 0.000000000000000000, 1.000000000000000000 ) ) ;
#1078=ORIENTED_EDGE ( 'NONE', *, *, #46239, .F. ) ;
#1082=AXIS2_PLACEMENT_3D ( 'NONE', #14006, #36515, #13779 ) ;
#1083=EDGE_CURVE ( 'NONE', #9308, #24221, #40129, .T. ) ;
#1088=ORIENTED_EDGE ( 'NONE', *, *, #25577, .T. ) ;
#1095=DIRECTION ( 'NONE',  ( 0.000000000000000000, 0.000000000000000000, 1.000000000000000000 ) ) ;
#1098=ORIENTED_EDGE ( 'NONE', *, *, #5630, .T. ) ;
#1101=VERTEX_POINT ( 'NONE', #11435 ) ;
#1102=CIRCLE ( 'NONE', #45658, 31.99999999999999645 ) ;
#1112=LINE ( 'NONE', #26822, #9011 ) ;
#1116=DIRECTION ( 'NONE',  ( 0.000000000000000000, 0.000000000000000000, 1.000000000000000000 ) ) ;
#1120=CARTESIAN_POINT ( 'NONE',  ( 10.00000000000000000, 14.67089635893819377, -73.72996012237423713 ) ) ;
#1122=LINE ( 'NONE', #23633, #13666 ) ;
#1134=CYLINDRICAL_SURFACE ( 'NONE', #8852, 32.00000000000000000 ) ;
#1142=AXIS2_PLACEMENT_3D ( 'NONE', #18898, #7171, #48288 ) ;
#1144=CARTESIAN_POINT ( 'NONE',  ( 10.00000000000000000, -39.78640506895559525, -66.50666863322042843 ) ) ;
#1151=DIRECTION ( 'NONE',  ( -1.000000000000000000, 0.000000000000000000, 0.000000000000000000 ) ) ;
#1155=AXIS2_PLACEMENT_3D ( 'NONE', #6083, #29721, #35918 ) ;
#1163=ADVANCED_FACE ( 'NONE', ( #7510 ), #44699, .T. ) ;
#1165=CYLINDRICAL_SURFACE ( 'NONE', #34218, 31.99999999999999289 ) ;
#1174=EDGE_LOOP ( 'NONE', ( #32465, #41102, #15608, #21253 ) ) ;
#1178=VECTOR ( 'NONE', #30755, 1000.000000000000000 ) ;
#1179=DIRECTION ( 'NONE',  ( -1.000000000000000000, 0.000000000000000000, -0.000000000000000000 ) ) ;
#1182=AXIS2_PLACEMENT_3D ( 'NONE', #36099, #2558, #37112 ) ;
#1183=VERTEX_POINT ( 'NONE', #26825 ) ;
#1186=FACE_OUTER_BOUND ( 'NONE', #12739, .T. ) ;
#1187=EDGE_CURVE ( 'NONE', #16097, #10794, #33915, .T. ) ;
#1189=ORIENTED_EDGE ( 'NONE', *, *, #35205, .F. ) ;
#1195=DIRECTION ( 'NONE',  ( -1.000000000000000000, -0.000000000000000000, 0.000000000000000000 ) ) ;
#1201=CYLINDRICAL_SURFACE ( 'NONE', #10724, 31.99999999999999289 ) ;
#1205=ORIENTED_EDGE ( 'NONE', *, *, #27577, .F. ) ;
#1212=AXIS2_PLACEMENT_3D ( 'NONE', #4040, #47841, #6417 ) ;
#1213=DIRECTION ( 'NONE',  ( 1.000000000000000000, 0.000000000000000000, 0.000000000000000000 ) ) ;
#1217=CYLINDRICAL_SURFACE ( 'NONE', #28054, 82.00000000000000000 ) ;
#1219=EDGE_CURVE ( 'NONE', #15799, #16528, #41699, .T. ) ;
#1220=AXIS2_PLACEMENT_3D ( 'NONE', #45133, #44166, #37055 ) ;
#1223=CIRCLE ( 'NONE', #4347, 31.99999999999999289 ) ;
#1230=CIRCLE ( 'NONE', #23908, 31.99999999999999289 ) ;
#1231=ORIENTED_EDGE ( 'NONE', *, *, #45937, .T. ) ;
#1234=AXIS2_PLACEMENT_3D ( 'NONE', #9549, #35983, #13242 ) ;
#1235=CARTESIAN_POINT ( 'NONE',  ( 10.00000000000000000, 0.000000000000000000, 0.000000000000000000 ) ) ;
#1239=ORIENTED_EDGE ( 'NONE', *, *, #15759, .F. ) ;
#1240=CARTESIAN_POINT ( 'NONE',  ( 0.000000000000000000, -75.16055320797016748, -18.89407956138335365 ) ) ;
#1244=DIRECTION ( 'NONE',  ( -1.000000000000000000, -0.000000000000000000, -0.000000000000000000 ) ) ;
#1245=ORIENTED_EDGE ( 'NONE', *, *, #43663, .T. ) ;
#1247=ADVANCED_FACE ( 'NONE', ( #5038 ), #27809, .T. ) ;
#1253=ORIENTED_EDGE ( 'NONE', *, *, #14819, .F. ) ;
#1256=FACE_OUTER_BOUND ( 'NONE', #41126, .T. ) ;
#1281=EDGE_CURVE ( 'NONE', #3891, #9834, #46158, .T. ) ;
#1290=CYLINDRICAL_SURFACE ( 'NONE', #13658, 82.00000000000000000 ) ;
#1292=ORIENTED_EDGE ( 'NONE', *, *, #44650, .T. ) ;
#1293=CYLINDRICAL_SURFACE ( 'NONE', #38311, 82.00000000000000000 ) ;
#1306=DIRECTION ( 'NONE',  ( -1.000000000000000000, 0.000000000000000000, -0.000000000000000000 ) ) ;
#1307=CARTESIAN_POINT ( 'NONE',  ( 0.000000000000000000, 0.000000000000000000, 0.000000000000000000 ) ) ;
#1309=CARTESIAN_POINT ( 'NONE',  ( 10.00000000000000000, 46.21855187248719687, -62.20884554313968806 ) ) ;
#1310=VERTEX_POINT ( 'NONE', #46646 ) ;
#1314=CARTESIAN_POINT ( 'NONE',  ( 10.00000000000000000, 0.000000000000000000, 0.000000000000000000 ) ) ;
#1317=VERTEX_POINT ( 'NONE', #20431 ) ;
#1319=CARTESIAN_POINT ( 'NONE',  ( 5.000000000000002665, -74.18225833017913828, 34.94270380257611919 ) ) ;
#1321=DIRECTION ( 'NONE',  ( -1.000000000000000000, 0.000000000000000000, -0.000000000000000000 ) ) ;
#1325=FACE_OUTER_BOUND ( 'NONE', #41133, .T. ) ;
#1329=DIRECTION ( 'NONE',  ( -0.000000000000000000, 0.000000000000000000, 1.000000000000000000 ) ) ;
#1332=EDGE_CURVE ( 'NONE', #12095, #23501, #35123, .T. ) ;
#1341=CARTESIAN_POINT ( 'NONE',  ( 0.000000000000000000, -73.73191006444561424, -14.66109333815538918 ) ) ;
#1346=ADVANCED_FACE ( 'NONE', ( #39959 ), #1370, .T. ) ;
#1354=ORIENTED_EDGE ( 'NONE', *, *, #41018, .T. ) ;
#1359=ORIENTED_EDGE ( 'NONE', *, *, #3672, .F. ) ;
#1360=CARTESIAN_POINT ( 'NONE',  ( 0.000000000000000000, 0.000000000000000000, -2.500000000000000000 ) ) ;
#1362=DIRECTION ( 'NONE',  ( -1.000000000000000000, 0.000000000000000000, 0.000000000000000000 ) ) ;
#1366=LINE ( 'NONE', #16294, #2088 ) ;
#1370=CYLINDRICAL_SURFACE ( 'NONE', #43195, 31.99999999999999289 ) ;
#1371=CARTESIAN_POINT ( 'NONE',  ( 10.00000000000000000, 0.000000000000000000, 0.000000000000000000 ) ) ;
#1373=CARTESIAN_POINT ( 'NONE',  ( 10.00000000000000000, 55.20638768913831029, -51.02545421589267960 ) ) ;
#1375=ORIENTED_EDGE ( 'NONE', *, *, #6520, .T. ) ;
#1378=AXIS2_PLACEMENT_3D ( 'NONE', #14927, #11262, #26189 ) ;
#1379=DIRECTION ( 'NONE',  ( 0.000000000000000000, 0.000000000000000000, 1.000000000000000000 ) ) ;
#1380=CARTESIAN_POINT ( 'NONE',  ( 10.00000000000000000, -66.50666863321973210, -39.78640506895676765 ) ) ;
#1386=CARTESIAN_POINT ( 'NONE',  ( 10.00000000000000000, 70.53064760720278059, 26.01480285779964774 ) ) ;
#1396=ORIENTED_EDGE ( 'NONE', *, *, #18111, .T. ) ;
#1399=CARTESIAN_POINT ( 'NONE',  ( 0.000000000000000000, 75.16055320797057959, -18.89407956138176914 ) ) ;
#1400=ORIENTED_EDGE ( 'NONE', *, *, #442, .F. ) ;
#1404=VECTOR ( 'NONE', #12182, 1000.000000000000000 ) ;
#1405=ORIENTED_EDGE ( 'NONE', *, *, #27096, .F. ) ;
#1406=EDGE_LOOP ( 'NONE', ( #44187, #851, #16151, #32013, #39258, #34914, #30211, #46182, #40253, #8744, #32601, #5738, #8437, #35308, #6785, #38820, #24635, #22335, #27916, #10075, #21931, #10575, #10917, #31410, #35401, #42530, #37969, #35902, #18172, #45179, #15217, #38139, #2520, #22701, #38439, #8650, #22176, #10980, #39985, #39632, #21189, #10177, #31778, #13615, #23126, #8998, #8605, #12486, #15270, #5758, #3556, #41046, #35219, #13981, #10814, #45251, #38015, #8989, #38322, #2957, #12835, #40110, #33377, #9015, #45132, #6446, #4060, #15543, #9713, #1923, #4974, #33948, #15557, #27433, #21991, #28211, #52, #19143, #20680, #16400, #16233, #37415, #47232, #22432, #5609, #34863, #43006, #18752, #2227, #12909, #20265, #35784, #12863, #40893, #48244, #32237, #10185, #20021, #45773, #4169, #21994, #42387, #35733, #20224, #41583, #7616, #3436, #3522, #21144, #31096, #29873, #21909, #17178, #17236, #42591, #44308, #27167, #3327, #19540, #17304, #43273, #34334, #29486, #13292, #27427, #17646, #36750, #39250, #41550, #23205, #3793, #29281, #21740, #14756, #25667, #14435, #43677, #17361, #5963, #47909, #32224, #12785, #25008, #3249, #5193, #18962, #15611, #39659, #27866, #30437, #29122, #22529, #45861, #31420, #34746, #13562, #43320, #23452, #41438, #27595, #43642, #42857, #46772, #2329, #25702, #23015, #13375, #11440, #13834, #23374, #27108, #34189, #48182, #13153, #8350, #1292, #25597, #6814, #5051, #4185, #18557, #26961, #34078, #47806, #24936, #26171, #27864, #22320, #48119, #35177, #7749, #35771, #21924, #8386, #18950, #33971, #11547, #42895, #41553, #21025, #48297, #46749, #29219, #45568, #13093, #15648, #12008, #28289, #41325, #32133, #39831, #6166, #31150, #46038, #23029, #5694, #14557, #32226, #38031, #28574, #27546, #38603, #38285, #47085, #14334, #538, #26280, #47847, #43799, #46236, #30265, #14582, #1359, #7623, #31518, #9229, #36770, #29130, #33937, #19383, #24383, #31117, #22046, #44473, #39655, #38538, #44655, #8658, #35914, #6126, #15622, #34153, #32377, #14827, #36259, #28610, #9630, #37227, #43660, #38733, #42207, #38358, #15482, #38016, #28009, #40050, #41624, #28653, #31105, #27545, #30597, #12499, #580, #41162, #20176, #47738, #4392, #44224, #47633, #32763, #22225, #21557, #8287, #21504, #30030, #3982, #19693, #23475, #42162, #31218, #16215, #23747, #18849, #35352, #16331, #28310, #34223, #43490, #37156, #34270, #12944, #7350, #43908, #31896, #18607, #13835, #36970, #25423, #27906, #36056, #29474, #47968, #43467, #26638, #19232, #37050, #35035, #17266, #10825, #28885, #42300, #45745, #5527, #43446, #30053 ) ) ;
#1410=CARTESIAN_POINT ( 'NONE',  ( 10.00000000000000000, -51.03279382321125723, 55.19960302592048862 ) ) ;
#1417=ORIENTED_EDGE ( 'NONE', *, *, #20509, .T. ) ;
#1430=CARTESIAN_POINT ( 'NONE',  ( 10.00000000000000000, -29.01471420065507090, -76.69515212746047439 ) ) ;
#1436=DIRECTION ( 'NONE',  ( -1.000000000000000000, -0.000000000000000000, 0.000000000000000000 ) ) ;
#1437=EDGE_CURVE ( 'NONE', #45989, #31737, #23, .T. ) ;
#1442=CARTESIAN_POINT ( 'NONE',  ( 10.00000000000000000, 0.000000000000000000, 77.49899999999999523 ) ) ;
#1445=CARTESIAN_POINT ( 'NONE',  ( 5.000000000000002665, -39.47590169984793818, -71.87247863392457248 ) ) ;
#1448=AXIS2_PLACEMENT_3D ( 'NONE', #40226, #48276, #37264 ) ;
#1462=CARTESIAN_POINT ( 'NONE',  ( 5.000000000000002665, 68.55367621811205936, -44.99326035065983120 ) ) ;
#1464=EDGE_LOOP ( 'NONE', ( #6655, #44629, #28449, #47036 ) ) ;
#1465=ADVANCED_FACE ( 'NONE', ( #22057 ), #36988, .T. ) ;
#1471=ORIENTED_EDGE ( 'NONE', *, *, #23150, .F. ) ;
#1477=ORIENTED_EDGE ( 'NONE', *, *, #25577, .F. ) ;
#1485=DIRECTION ( 'NONE',  ( -1.000000000000000000, 0.000000000000000000, -0.000000000000000000 ) ) ;
#1497=CARTESIAN_POINT ( 'NONE',  ( 10.00000000000000000, -16.65972982744878195, -80.28980883073774066 ) ) ;
#1498=CARTESIAN_POINT ( 'NONE',  ( 10.00000000000000000, 0.000000000000000000, 0.000000000000000000 ) ) ;
#1503=FACE_OUTER_BOUND ( 'NONE', #6233, .T. ) ;
#1507=LINE ( 'NONE', #16430, #41941 ) ;
#1513=EDGE_CURVE ( 'NONE', #42302, #20404, #44101, .T. ) ;
#1518=DIRECTION ( 'NONE',  ( 0.000000000000000000, -0.9969173337331287410, 0.07845909572783489605 ) ) ;
#1528=CARTESIAN_POINT ( 'NONE',  ( 5.000000000000000000, -46.11716303203234446, 67.80270845531873647 ) ) ;
#1538=ORIENTED_EDGE ( 'NONE', *, *, #4386, .F. ) ;
#1544=VERTEX_POINT ( 'NONE', #38711 ) ;
#1545=CARTESIAN_POINT ( 'NONE',  ( 5.000000000000000000, -56.15606465355001120, 59.75363087400055662 ) ) ;
#1554=CARTESIAN_POINT ( 'NONE',  ( 0.000000000000000000, -72.35160999960831418, 20.41045688087797672 ) ) ;
#1560=FACE_OUTER_BOUND ( 'NONE', #42288, .T. ) ;
#1562=CIRCLE ( 'NONE', #16394, 31.99999999999999289 ) ;
#1563=CIRCLE ( 'NONE', #25780, 82.00000000000000000 ) ;
#1570=CARTESIAN_POINT ( 'NONE',  ( 10.00000000000000000, 0.000000000000000000, 0.000000000000000000 ) ) ;
#1573=DIRECTION ( 'NONE',  ( 0.000000000000000000, 0.000000000000000000, -1.000000000000000000 ) ) ;
#1576=CARTESIAN_POINT ( 'NONE',  ( 0.000000000000000000, -55.20638768913724448, -51.02545421589383068 ) ) ;
#1577=DIRECTION ( 'NONE',  ( -1.000000000000000000, -0.000000000000000000, -0.000000000000000000 ) ) ;
#1583=EDGE_CURVE ( 'NONE', #43969, #15443, #27442, .T. ) ;
#1587=AXIS2_PLACEMENT_3D ( 'NONE', #8614, #27971, #34553 ) ;
#1588=CYLINDRICAL_SURFACE ( 'NONE', #18763, 82.00000000000000000 ) ;
#1590=AXIS2_PLACEMENT_3D ( 'NONE', #37542, #8169, #88 ) ;
#1591=AXIS2_PLACEMENT_3D ( 'NONE', #38926, #967, #19806 ) ;
#1601=VECTOR ( 'NONE', #12028, 1000.000000000000000 ) ;
#1608=CARTESIAN_POINT ( 'NONE',  ( 0.000000000000000000, 76.66974797899835892, 11.30684508768368346 ) ) ;
#1611=LINE ( 'NONE', #38095, #1017 ) ;
#1615=LINE ( 'NONE', #40025, #7212 ) ;
#1627=DIRECTION ( 'NONE',  ( 0.000000000000000000, 0.000000000000000000, 1.000000000000000000 ) ) ;
#1629=ORIENTED_EDGE ( 'NONE', *, *, #48081, .T. ) ;
#1633=EDGE_LOOP ( 'NONE', ( #23619, #28994, #2601, #45353 ) ) ;
#1641=ORIENTED_EDGE ( 'NONE', *, *, #16747, .F. ) ;
#1645=VERTEX_POINT ( 'NONE', #45806 ) ;
#1646=ORIENTED_EDGE ( 'NONE', *, *, #2526, .T. ) ;
#1653=AXIS2_PLACEMENT_3D ( 'NONE', #47358, #43911, #29225 ) ;
#1658=CARTESIAN_POINT ( 'NONE',  ( 10.00000000000000000, 17.28742895386084655, 75.54627589209950145 ) ) ;
#1665=EDGE_CURVE ( 'NONE', #24652, #39658, #43998, .T. ) ;
#1675=ORIENTED_EDGE ( 'NONE', *, *, #13205, .T. ) ;
#1678=EDGE_CURVE ( 'NONE', #33852, #20108, #3351, .T. ) ;
#1680=DIRECTION ( 'NONE',  ( -1.000000000000000000, 0.000000000000000000, 0.000000000000000000 ) ) ;
#1686=CARTESIAN_POINT ( 'NONE',  ( 10.00000000000000000, -72.35160999960801576, -20.41045688087902121 ) ) ;
#1687=DIRECTION ( 'NONE',  ( 0.000000000000000000, 0.000000000000000000, 1.000000000000000000 ) ) ;
#1689=CARTESIAN_POINT ( 'NONE',  ( 5.000000000000002665, -76.69515212745996280, -29.01471420065644580 ) ) ;
#1691=CARTESIAN_POINT ( 'NONE',  ( 10.00000000000000000, 31.47745569255237896, -68.26794271651228030 ) ) ;
#1700=CARTESIAN_POINT ( 'NONE',  ( 10.00000000000000000, -75.54627589209955829, 17.28742895386058009 ) ) ;
#1707=VECTOR ( 'NONE', #12986, 1000.000000000000000 ) ;
#1713=DIRECTION ( 'NONE',  ( 1.000000000000000000, 0.000000000000000000, 0.000000000000000000 ) ) ;
#1717=FACE_OUTER_BOUND ( 'NONE', #44692, .T. ) ;
#1721=EDGE_CURVE ( 'NONE', #18546, #11579, #43233, .T. ) ;
#1723=EDGE_CURVE ( 'NONE', #2146, #23354, #22117, .T. ) ;
#1725=AXIS2_PLACEMENT_3D ( 'NONE', #28770, #29250, #43217 ) ;
#1728=CARTESIAN_POINT ( 'NONE',  ( 10.00000000000000000, 0.000000000000000000, 0.000000000000000000 ) ) ;
#1729=VERTEX_POINT ( 'NONE', #36213 ) ;
#1730=ORIENTED_EDGE ( 'NONE', *, *, #27119, .T. ) ;
#1735=CARTESIAN_POINT ( 'NONE',  ( 10.00000000000000000, 75.54627589209943039, 17.28742895386112721 ) ) ;
#1739=DIRECTION ( 'NONE',  ( 0.000000000000000000, -6.938893903907228378E-15, 1.000000000000000000 ) ) ;
#1741=DIRECTION ( 'NONE',  ( 1.000000000000000000, 0.000000000000000000, 0.000000000000000000 ) ) ;
#1749=DIRECTION ( 'NONE',  ( 0.000000000000000000, -0.4539904997395350916, -0.8910065241883738940 ) ) ;
#1754=DIRECTION ( 'NONE',  ( 0.000000000000000000, 0.000000000000000000, 1.000000000000000000 ) ) ;
#1758=VECTOR ( 'NONE', #2740, 1000.000000000000000 ) ;
#1765=ORIENTED_EDGE ( 'NONE', *, *, #45721, .F. ) ;
#1766=DIRECTION ( 'NONE',  ( 0.000000000000000000, 0.000000000000000000, 1.000000000000000000 ) ) ;
#1772=DIRECTION ( 'NONE',  ( -1.000000000000000000, 0.000000000000000000, -0.000000000000000000 ) ) ;
#1775=DIRECTION ( 'NONE',  ( 0.000000000000000000, 0.000000000000000000, -1.000000000000000000 ) ) ;
#1776=EDGE_CURVE ( 'NONE', #34549, #42227, #192, .T. ) ;
#1780=DIRECTION ( 'NONE',  ( -1.000000000000000000, -0.000000000000000000, 0.000000000000000000 ) ) ;
#1781=DIRECTION ( 'NONE',  ( -1.000000000000000000, -0.000000000000000000, -0.000000000000000000 ) ) ;
#1790=CARTESIAN_POINT ( 'NONE',  ( 0.000000000000000000, 70.52718814184260054, 26.02418014898334420 ) ) ;
#1792=VERTEX_POINT ( 'NONE', #13714 ) ;
#1793=CARTESIAN_POINT ( 'NONE',  ( 5.000000000000000000, 50.23322058963442061, -64.81221759200289512 ) ) ;
#1794=CIRCLE ( 'NONE', #27579, 31.99999999999999289 ) ;
#1796=LINE ( 'NONE', #4740, #39146 ) ;
#1805=AXIS2_PLACEMENT_3D ( 'NONE', #22965, #30552, #11713 ) ;
#1809=AXIS2_PLACEMENT_3D ( 'NONE', #37378, #7267, #415 ) ;
#1822=ORIENTED_EDGE ( 'NONE', *, *, #3672, .T. ) ;
#1824=ORIENTED_EDGE ( 'NONE', *, *, #18288, .F. ) ;
#1828=LINE ( 'NONE', #2299, #19025 ) ;
#1829=EDGE_CURVE ( 'NONE', #15099, #17725, #35389, .T. ) ;
#1835=ORIENTED_EDGE ( 'NONE', *, *, #33379, .F. ) ;
#1845=ORIENTED_EDGE ( 'NONE', *, *, #9064, .F. ) ;
#1849=ADVANCED_FACE ( 'NONE', ( #10516 ), #28864, .T. ) ;
#1852=VECTOR ( 'NONE', #4476, 1000.000000000000000 ) ;
#1854=DIRECTION ( 'NONE',  ( 0.000000000000000000, 0.000000000000000000, 1.000000000000000000 ) ) ;
#1855=DIRECTION ( 'NONE',  ( -1.000000000000000000, -0.000000000000000000, 0.000000000000000000 ) ) ;
#1857=DIRECTION ( 'NONE',  ( -1.000000000000000000, -0.000000000000000000, 0.000000000000000000 ) ) ;
#1859=EDGE_LOOP ( 'NONE', ( #45005, #46756, #29798, #31221 ) ) ;
#1864=CARTESIAN_POINT ( 'NONE',  ( 10.00000000000000000, 75.16055320797030959, 18.89407956138283851 ) ) ;
#1871=CARTESIAN_POINT ( 'NONE',  ( 10.00000000000000000, -26.02418014898260878, -70.52718814184285634 ) ) ;
#1875=CARTESIAN_POINT ( 'NONE',  ( 0.000000000000000000, 2.956366410620650420, 75.11725578898469280 ) ) ;
#1885=ORIENTED_EDGE ( 'NONE', *, *, #34338, .T. ) ;
#1886=ORIENTED_EDGE ( 'NONE', *, *, #24377, .F. ) ;
#1898=AXIS2_PLACEMENT_3D ( 'NONE', #39465, #19867, #39214 ) ;
#1901=DIRECTION ( 'NONE',  ( -1.000000000000000000, 0.000000000000000000, -0.000000000000000000 ) ) ;
#1905=DIRECTION ( 'NONE',  ( -1.000000000000000000, 0.000000000000000000, -0.000000000000000000 ) ) ;
#1906=CARTESIAN_POINT ( 'NONE',  ( 0.000000000000000000, -50.95692526931372157, 58.39081064771733054 ) ) ;
#1909=DIRECTION ( 'NONE',  ( -1.000000000000000000, 0.000000000000000000, -0.000000000000000000 ) ) ;
#1911=ORIENTED_EDGE ( 'NONE', *, *, #13116, .F. ) ;
#1915=CARTESIAN_POINT ( 'NONE',  ( 10.00000000000000000, -51.02545421589363883, 55.20638768913742922 ) ) ;
#1918=CARTESIAN_POINT ( 'NONE',  ( 10.00000000000000000, -73.72996012237429397, -14.67089635893794508 ) ) ;
#1923=ORIENTED_EDGE ( 'NONE', *, *, #37157, .T. ) ;
#1926=AXIS2_PLACEMENT_3D ( 'NONE', #26451, #44800, #31277 ) ;
#1937=CIRCLE ( 'NONE', #17524, 31.99999999999998579 ) ;
#1954=ADVANCED_FACE ( 'NONE', ( #47944 ), #33013, .T. ) ;
#1955=DIRECTION ( 'NONE',  ( 0.000000000000000000, 0.000000000000000000, 1.000000000000000000 ) ) ;
#1958=CIRCLE ( 'NONE', #9853, 77.49899999999999523 ) ;
#1959=EDGE_CURVE ( 'NONE', #26190, #34606, #34224, .T. ) ;
#1964=ADVANCED_FACE ( 'NONE', ( #4617 ), #8037, .T. ) ;
#1966=CIRCLE ( 'NONE', #37133, 31.99999999999999289 ) ;
#1967=VECTOR ( 'NONE', #41625, 1000.000000000000000 ) ;
#1976=ORIENTED_EDGE ( 'NONE', *, *, #17064, .T. ) ;
#1979=DIRECTION ( 'NONE',  ( -1.000000000000000000, 0.000000000000000000, 0.000000000000000000 ) ) ;
#1988=EDGE_LOOP ( 'NONE', ( #33319, #21691, #38064, #12586 ) ) ;
#1993=DIRECTION ( 'NONE',  ( 0.000000000000000000, 0.8910065241883691201, -0.4539904997395446951 ) ) ;
#1995=ADVANCED_FACE ( 'NONE', ( #12454 ), #16136, .T. ) ;
#1996=AXIS2_PLACEMENT_3D ( 'NONE', #20917, #27789, #43669 ) ;
#1997=AXIS2_PLACEMENT_3D ( 'NONE', #26021, #36558, #2785 ) ;
#1999=DIRECTION ( 'NONE',  ( -1.000000000000000000, -0.000000000000000000, 0.000000000000000000 ) ) ;
#2002=DIRECTION ( 'NONE',  ( 0.000000000000000000, -0.3090169943749349613, -0.9510565162951576390 ) ) ;
#2004=DIRECTION ( 'NONE',  ( -1.000000000000000000, -0.000000000000000000, -0.000000000000000000 ) ) ;
#2005=EDGE_CURVE ( 'NONE', #9517, #21969, #467, .T. ) ;
#2011=DIRECTION ( 'NONE',  ( -1.000000000000000000, 0.000000000000000000, 0.000000000000000000 ) ) ;
#2025=ADVANCED_FACE ( 'NONE', ( #4861 ), #41585, .T. ) ;
#2038=CARTESIAN_POINT ( 'NONE',  ( 0.000000000000000000, 0.000000000000000000, 0.000000000000000000 ) ) ;
#2042=ORIENTED_EDGE ( 'NONE', *, *, #31128, .T. ) ;
#2043=DIRECTION ( 'NONE',  ( 0.000000000000000000, 0.000000000000000000, 1.000000000000000000 ) ) ;
#2044=CYLINDRICAL_SURFACE ( 'NONE', #15258, 31.99999999999998579 ) ;
#2049=FACE_OUTER_BOUND ( 'NONE', #13559, .T. ) ;
#2055=EDGE_CURVE ( 'NONE', #15936, #23071, #9562, .T. ) ;
#2062=EDGE_CURVE ( 'NONE', #11314, #27936, #42308, .T. ) ;
#2064=AXIS2_PLACEMENT_3D ( 'NONE', #38629, #12677, #912 ) ;
#2066=ORIENTED_EDGE ( 'NONE', *, *, #3140, .T. ) ;
#2076=AXIS2_PLACEMENT_3D ( 'NONE', #14, #29642, #36736 ) ;
#2083=CARTESIAN_POINT ( 'NONE',  ( 0.000000000000000000, 39.78640506895700213, -66.50666863321957578 ) ) ;
#2088=VECTOR ( 'NONE', #12618, 1000.000000000000000 ) ;
#2090=ORIENTED_EDGE ( 'NONE', *, *, #4080, .T. ) ;
#2095=DIRECTION ( 'NONE',  ( -1.000000000000000000, 0.000000000000000000, -0.000000000000000000 ) ) ;
#2100=CARTESIAN_POINT ( 'NONE',  ( 10.00000000000000000, 0.000000000000000000, 0.000000000000000000 ) ) ;
#2101=CARTESIAN_POINT ( 'NONE',  ( 10.00000000000000000, -65.64334221924882229, -41.19522573413803457 ) ) ;
#2107=EDGE_CURVE ( 'NONE', #16993, #41512, #32227, .T. ) ;
#2116=LINE ( 'NONE', #39072, #20623 ) ;
#2120=VERTEX_POINT ( 'NONE', #35436 ) ;
#2121=DIRECTION ( 'NONE',  ( 0.000000000000000000, 0.000000000000000000, 1.000000000000000000 ) ) ;
#2126=CIRCLE ( 'NONE', #38111, 77.49900000000000944 ) ;
#2128=VERTEX_POINT ( 'NONE', #9255 ) ;
#2129=CIRCLE ( 'NONE', #38078, 31.99999999999999289 ) ;
#2135=FACE_OUTER_BOUND ( 'NONE', #25396, .T. ) ;
#2137=VERTEX_POINT ( 'NONE', #32257 ) ;
#2140=DIRECTION ( 'NONE',  ( 0.000000000000000000, 0.000000000000000000, 1.000000000000000000 ) ) ;
#2141=CYLINDRICAL_SURFACE ( 'NONE', #33688, 31.99999999999999289 ) ;
#2146=VERTEX_POINT ( 'NONE', #42802 ) ;
#2154=CARTESIAN_POINT ( 'NONE',  ( 10.00000000000000000, 0.000000000000000000, 0.000000000000000000 ) ) ;
#2162=CARTESIAN_POINT ( 'NONE',  ( 10.00000000000000000, 44.99326035066052754, 68.55367621811160461 ) ) ;
#2165=CYLINDRICAL_SURFACE ( 'NONE', #14614, 82.00000000000000000 ) ;
#2171=DIRECTION ( 'NONE',  ( 0.000000000000000000, 0.000000000000000000, 1.000000000000000000 ) ) ;
#2182=EDGE_LOOP ( 'NONE', ( #36448, #41682, #39832, #45012 ) ) ;
#2183=VERTEX_POINT ( 'NONE', #6081 ) ;
#2184=AXIS2_PLACEMENT_3D ( 'NONE', #20555, #23751, #27935 ) ;
#2189=VERTEX_POINT ( 'NONE', #38892 ) ;
#2190=ORIENTED_EDGE ( 'NONE', *, *, #13426, .F. ) ;
#2199=DIRECTION ( 'NONE',  ( 0.000000000000000000, 0.000000000000000000, 1.000000000000000000 ) ) ;
#2208=EDGE_CURVE ( 'NONE', #5642, #32047, #20760, .T. ) ;
#2214=DIRECTION ( 'NONE',  ( -1.000000000000000000, -0.000000000000000000, -0.000000000000000000 ) ) ;
#2219=CARTESIAN_POINT ( 'NONE',  ( 0.000000000000000000, -62.20884554314051940, 46.21855187248608132 ) ) ;
#2222=ADVANCED_FACE ( 'NONE', ( #43748 ), #47424, .T. ) ;
#2224=CARTESIAN_POINT ( 'NONE',  ( 0.000000000000000000, -50.23322058963393744, 64.81221759200325039 ) ) ;
#2225=DIRECTION ( 'NONE',  ( 0.000000000000000000, 0.6494480483301793283, 0.7604059656000345946 ) ) ;
#2227=ORIENTED_EDGE ( 'NONE', *, *, #48094, .F. ) ;
#2229=DIRECTION ( 'NONE',  ( -1.000000000000000000, 0.000000000000000000, 0.000000000000000000 ) ) ;
#2237=VERTEX_POINT ( 'NONE', #47646 ) ;
#2239=ADVANCED_FACE ( 'NONE', ( #18028 ), #14134, .T. ) ;
#2245=EDGE_CURVE ( 'NONE', #28305, #45131, #18530, .T. ) ;
#2254=DIRECTION ( 'NONE',  ( 0.000000000000000000, 0.000000000000000000, 1.000000000000000000 ) ) ;
#2257=DIRECTION ( 'NONE',  ( 1.000000000000000000, -0.000000000000000000, 0.000000000000000000 ) ) ;
#2261=CYLINDRICAL_SURFACE ( 'NONE', #40278, 31.99999999999999289 ) ;
#2263=LINE ( 'NONE', #6429, #35223 ) ;
#2265=LINE ( 'NONE', #1793, #10486 ) ;
#2270=EDGE_CURVE ( 'NONE', #28609, #13398, #31979, .T. ) ;
#2271=CARTESIAN_POINT ( 'NONE',  ( 10.00000000000000000, 16.65972982745046238, -80.28980883073739960 ) ) ;
#2275=CARTESIAN_POINT ( 'NONE',  ( 5.000000000000000000, -64.81221759200379040, 50.23322058963324110 ) ) ;
#2276=CARTESIAN_POINT ( 'NONE',  ( 10.00000000000000000, 11.30684508768339569, 76.66974797899841576 ) ) ;
#2277=CARTESIAN_POINT ( 'NONE',  ( 10.00000000000000000, -81.34940948281328588, -10.30890764327469711 ) ) ;
#2284=AXIS2_PLACEMENT_3D ( 'NONE', #15606, #674, #37395 ) ;
#2286=DIRECTION ( 'NONE',  ( 1.000000000000000000, 0.000000000000000000, 0.000000000000000000 ) ) ;
#2289=LINE ( 'NONE', #43425, #13510 ) ;
#2295=VERTEX_POINT ( 'NONE', #29544 ) ;
#2299=CARTESIAN_POINT ( 'NONE',  ( 10.00000000000000000, -63.18004540533059554, 44.88180994100355292 ) ) ;
#2311=CARTESIAN_POINT ( 'NONE',  ( 10.00000000000000000, 0.000000000000000000, 0.000000000000000000 ) ) ;
#2319=CARTESIAN_POINT ( 'NONE',  ( 10.00000000000000000, -71.91182617369207719, 28.89263327155721228 ) ) ;
#2321=CARTESIAN_POINT ( 'NONE',  ( 0.000000000000000000, -20.40083707022829174, -72.35432306680507963 ) ) ;
#2323=ADVANCED_FACE ( 'NONE', ( #40083 ), #2870, .T. ) ;
#2329=ORIENTED_EDGE ( 'NONE', *, *, #13700, .T. ) ;
#2335=EDGE_CURVE ( 'NONE', #27708, #2670, #24164, .T. ) ;
#2339=VERTEX_POINT ( 'NONE', #34177 ) ;
#2340=DIRECTION ( 'NONE',  ( -1.000000000000000000, 0.000000000000000000, 0.000000000000000000 ) ) ;
#2343=ORIENTED_EDGE ( 'NONE', *, *, #9334, .T. ) ;
#2348=EDGE_LOOP ( 'NONE', ( #46876, #24503, #36334, #14177 ) ) ;
#2350=CIRCLE ( 'NONE', #6283, 82.00000000000000000 ) ;
#2363=VERTEX_POINT ( 'NONE', #15579 ) ;
#2365=DIRECTION ( 'NONE',  ( 0.000000000000000000, 0.1564344650402311743, -0.9876883405951377704 ) ) ;
#2367=DIRECTION ( 'NONE',  ( -1.000000000000000000, -0.000000000000000000, -0.000000000000000000 ) ) ;
#2373=EDGE_CURVE ( 'NONE', #47251, #10794, #24929, .T. ) ;
#2379=EDGE_CURVE ( 'NONE', #22588, #38490, #22453, .T. ) ;
#2395=DIRECTION ( 'NONE',  ( 0.000000000000000000, -0.8910065241883722287, 0.4539904997395382558 ) ) ;
#2396=CARTESIAN_POINT ( 'NONE',  ( 10.00000000000000000, 20.41045688087930898, -72.35160999960793049 ) ) ;
#2401=LINE ( 'NONE', #25400, #23012 ) ;
#2402=ORIENTED_EDGE ( 'NONE', *, *, #29275, .F. ) ;
#2409=EDGE_CURVE ( 'NONE', #3237, #37330, #13988, .T. ) ;
#2411=ORIENTED_EDGE ( 'NONE', *, *, #13766, .F. ) ;
#2414=EDGE_CURVE ( 'NONE', #2183, #8188, #12230, .T. ) ;
#2415=CIRCLE ( 'NONE', #25101, 31.99999999999999289 ) ;
#2417=DIRECTION ( 'NONE',  ( -1.000000000000000000, -0.000000000000000000, -0.000000000000000000 ) ) ;
#2418=EDGE_CURVE ( 'NONE', #12188, #11742, #2803, .T. ) ;
#2424=CARTESIAN_POINT ( 'NONE',  ( 10.00000000000000000, -30.41916302227164337, 71.27951684758015460 ) ) ;
#2433=ADVANCED_FACE ( 'NONE', ( #11187 ), #26113, .T. ) ;
#2438=DIRECTION ( 'NONE',  ( -1.000000000000000000, 0.000000000000000000, 0.000000000000000000 ) ) ;
#2446=CIRCLE ( 'NONE', #40750, 82.00000000000000000 ) ;
#2451=CARTESIAN_POINT ( 'NONE',  ( -10.00000000000000000, 0.000000000000000000, 0.000000000000000000 ) ) ;
#2454=DIRECTION ( 'NONE',  ( 0.000000000000000000, 0.000000000000000000, 1.000000000000000000 ) ) ;
#2466=EDGE_CURVE ( 'NONE', #17380, #7163, #17650, .T. ) ;
#2467=DIRECTION ( 'NONE',  ( -1.000000000000000000, 0.000000000000000000, 0.000000000000000000 ) ) ;
#2473=AXIS2_PLACEMENT_3D ( 'NONE', #37858, #22920, #26119 ) ;
#2477=EDGE_CURVE ( 'NONE', #24169, #36004, #27329, .T. ) ;
#2479=ORIENTED_EDGE ( 'NONE', *, *, #34455, .F. ) ;
#2481=CIRCLE ( 'NONE', #35292, 31.99999999999999645 ) ;
#2487=LINE ( 'NONE', #36503, #14585 ) ;
#2489=VERTEX_POINT ( 'NONE', #5298 ) ;
#2493=ORIENTED_EDGE ( 'NONE', *, *, #41737, .T. ) ;
#2496=ORIENTED_EDGE ( 'NONE', *, *, #17939, .T. ) ;
#2497=VECTOR ( 'NONE', #6117, 1000.000000000000000 ) ;
#2498=DIRECTION ( 'NONE',  ( 0.000000000000000000, -0.3090169943749349613, -0.9510565162951576390 ) ) ;
#2499=CARTESIAN_POINT ( 'NONE',  ( 0.000000000000000000, -40.65526001592565564, -71.21200624218839437 ) ) ;
#2500=DIRECTION ( 'NONE',  ( 1.000000000000000000, 0.000000000000000000, 0.000000000000000000 ) ) ;
#2503=CARTESIAN_POINT ( 'NONE',  ( 10.00000000000000000, 76.41127070299292257, -12.93880638057232346 ) ) ;
#2504=CYLINDRICAL_SURFACE ( 'NONE', #39950, 82.00000000000000000 ) ;
#2505=CARTESIAN_POINT ( 'NONE',  ( 10.00000000000000000, -10.30890764327324227, -81.34940948281347062 ) ) ;
#2508=DIRECTION ( 'NONE',  ( -1.000000000000000000, 0.000000000000000000, 0.000000000000000000 ) ) ;
#2514=DIRECTION ( 'NONE',  ( -1.000000000000000000, -0.000000000000000000, -0.000000000000000000 ) ) ;
#2515=ORIENTED_EDGE ( 'NONE', *, *, #24090, .T. ) ;
#2516=DIRECTION ( 'NONE',  ( 0.000000000000000000, 0.000000000000000000, -1.000000000000000000 ) ) ;
#2518=CARTESIAN_POINT ( 'NONE',  ( 10.00000000000000000, -0.8261519478425671803, -77.49459641780887864 ) ) ;
#2520=ORIENTED_EDGE ( 'NONE', *, *, #23929, .T. ) ;
#2521=AXIS2_PLACEMENT_3D ( 'NONE', #9215, #36117, #31761 ) ;
#2523=ORIENTED_EDGE ( 'NONE', *, *, #26572, .F. ) ;
#2526=EDGE_CURVE ( 'NONE', #17865, #43495, #23141, .T. ) ;
#2529=EDGE_CURVE ( 'NONE', #6477, #34129, #8299, .T. ) ;
#2536=VECTOR ( 'NONE', #33591, 1000.000000000000000 ) ;
#2539=FACE_OUTER_BOUND ( 'NONE', #20569, .T. ) ;
#2541=CARTESIAN_POINT ( 'NONE',  ( 10.00000000000000000, 0.000000000000000000, 0.000000000000000000 ) ) ;
#2547=EDGE_LOOP ( 'NONE', ( #1396, #40468, #33772, #12585 ) ) ;
#2548=CIRCLE ( 'NONE', #43200, 32.00000000000000000 ) ;
#2555=VECTOR ( 'NONE', #23229, 1000.000000000000000 ) ;
#2558=DIRECTION ( 'NONE',  ( -1.000000000000000000, -0.000000000000000000, -0.000000000000000000 ) ) ;
#2559=CARTESIAN_POINT ( 'NONE',  ( 10.00000000000000000, 18.89407956138362010, -75.16055320797013906 ) ) ;
#2562=AXIS2_PLACEMENT_3D ( 'NONE', #13062, #28462, #42682 ) ;
#2564=CARTESIAN_POINT ( 'NONE',  ( 10.00000000000000000, 62.50884508063487033, -41.76106447765422303 ) ) ;
#2565=CIRCLE ( 'NONE', #219, 77.49899999999999523 ) ;
#2566=FACE_OUTER_BOUND ( 'NONE', #29309, .T. ) ;
#2573=ORIENTED_EDGE ( 'NONE', *, *, #4080, .F. ) ;
#2574=DIRECTION ( 'NONE',  ( 0.000000000000000000, 0.000000000000000000, 1.000000000000000000 ) ) ;
#2576=ADVANCED_FACE ( 'NONE', ( #13593 ), #47829, .T. ) ;
#2581=AXIS2_PLACEMENT_3D ( 'NONE', #14854, #3833, #29770 ) ;
#2583=AXIS2_PLACEMENT_3D ( 'NONE', #17786, #32717, #40551 ) ;
#2584=LINE ( 'NONE', #13378, #41429 ) ;
#2587=ADVANCED_FACE ( 'NONE', ( #32447 ), #25318, .T. ) ;
#2593=ORIENTED_EDGE ( 'NONE', *, *, #20633, .F. ) ;
#2594=FACE_OUTER_BOUND ( 'NONE', #19789, .T. ) ;
#2596=CARTESIAN_POINT ( 'NONE',  ( 10.00000000000000000, 65.64334221924966073, -41.19522573413664190 ) ) ;
#2601=ORIENTED_EDGE ( 'NONE', *, *, #2409, .T. ) ;
#2613=CIRCLE ( 'NONE', #29989, 82.00000000000000000 ) ;
#2621=AXIS2_PLACEMENT_3D ( 'NONE', #10793, #14709, #7109 ) ;
#2625=CYLINDRICAL_SURFACE ( 'NONE', #48107, 77.49899999999999523 ) ;
#2631=EDGE_CURVE ( 'NONE', #17516, #10088, #21678, .T. ) ;
#2633=EDGE_LOOP ( 'NONE', ( #10303, #21374, #31222, #38580 ) ) ;
#2638=CARTESIAN_POINT ( 'NONE',  ( 10.00000000000000000, 0.000000000000000000, 0.000000000000000000 ) ) ;
#2645=DIRECTION ( 'NONE',  ( -1.000000000000000000, 0.000000000000000000, -0.000000000000000000 ) ) ;
#2647=VECTOR ( 'NONE', #8690, 1000.000000000000000 ) ;
#2649=EDGE_LOOP ( 'NONE', ( #42446, #25067, #30589, #41280 ) ) ;
#2656=ORIENTED_EDGE ( 'NONE', *, *, #42878, .T. ) ;
#2668=CARTESIAN_POINT ( 'NONE',  ( 10.00000000000000000, 40.65526001592612459, 71.21200624218811015 ) ) ;
#2669=DIRECTION ( 'NONE',  ( -1.000000000000000000, -0.000000000000000000, 0.000000000000000000 ) ) ;
#2670=VERTEX_POINT ( 'NONE', #21663 ) ;
#2679=VECTOR ( 'NONE', #20035, 1000.000000000000000 ) ;
#2682=ORIENTED_EDGE ( 'NONE', *, *, #17701, .T. ) ;
#2683=CIRCLE ( 'NONE', #38671, 31.99999999999999289 ) ;
#2685=CYLINDRICAL_SURFACE ( 'NONE', #30910, 82.00000000000000000 ) ;
#2686=CIRCLE ( 'NONE', #17542, 82.00000000000000000 ) ;
#2688=EDGE_CURVE ( 'NONE', #11204, #39764, #31063, .T. ) ;
#2691=DIRECTION ( 'NONE',  ( -1.000000000000000000, 0.000000000000000000, 0.000000000000000000 ) ) ;
#2701=EDGE_CURVE ( 'NONE', #14023, #37807, #3779, .T. ) ;
#2702=VECTOR ( 'NONE', #44475, 1000.000000000000000 ) ;
#2707=DIRECTION ( 'NONE',  ( -1.000000000000000000, 0.000000000000000000, -0.000000000000000000 ) ) ;
#2718=ORIENTED_EDGE ( 'NONE', *, *, #36616, .T. ) ;
#2722=AXIS2_PLACEMENT_3D ( 'NONE', #19407, #38267, #4502 ) ;
#2723=CARTESIAN_POINT ( 'NONE',  ( 10.00000000000000000, 8.840884882376133902, -74.65374052328640175 ) ) ;
#2733=CARTESIAN_POINT ( 'NONE',  ( 10.00000000000000000, -17.28742895386031719, -75.54627589209962935 ) ) ;
#2736=ORIENTED_EDGE ( 'NONE', *, *, #561, .T. ) ;
#2737=DIRECTION ( 'NONE',  ( -1.000000000000000000, 0.000000000000000000, 0.000000000000000000 ) ) ;
#2740=DIRECTION ( 'NONE',  ( -1.000000000000000000, 0.000000000000000000, 0.000000000000000000 ) ) ;
#2742=DIRECTION ( 'NONE',  ( -1.000000000000000000, -0.000000000000000000, 0.000000000000000000 ) ) ;
#2745=DIRECTION ( 'NONE',  ( 0.000000000000000000, -0.7604059656000228262, -0.6494480483301932061 ) ) ;
#2749=DIRECTION ( 'NONE',  ( 0.000000000000000000, 0.000000000000000000, 1.000000000000000000 ) ) ;
#2756=FACE_OUTER_BOUND ( 'NONE', #8111, .T. ) ;
#2759=EDGE_CURVE ( 'NONE', #26945, #5219, #37794, .T. ) ;
#2761=CIRCLE ( 'NONE', #36372, 32.00000000000000711 ) ;
#2762=DIRECTION ( 'NONE',  ( 0.000000000000000000, 0.07845909572783797692, 0.9969173337331285190 ) ) ;
#2765=ORIENTED_EDGE ( 'NONE', *, *, #7174, .F. ) ;
#2769=EDGE_CURVE ( 'NONE', #28305, #27618, #28672, .T. ) ;
#2770=FACE_OUTER_BOUND ( 'NONE', #42471, .T. ) ;
#2785=DIRECTION ( 'NONE',  ( 0.000000000000000000, 0.000000000000000000, 1.000000000000000000 ) ) ;
#2802=DIRECTION ( 'NONE',  ( -1.000000000000000000, -0.000000000000000000, -0.000000000000000000 ) ) ;
#2803=CIRCLE ( 'NONE', #40352, 32.00000000000000000 ) ;
#2805=DIRECTION ( 'NONE',  ( 0.000000000000000000, 0.000000000000000000, -1.000000000000000000 ) ) ;
#2818=CIRCLE ( 'NONE', #6630, 31.99999999999999289 ) ;
#2822=AXIS2_PLACEMENT_3D ( 'NONE', #19203, #30233, #33413 ) ;
#2823=VERTEX_POINT ( 'NONE', #41968 ) ;
#2830=VERTEX_POINT ( 'NONE', #1066 ) ;
#2833=ORIENTED_EDGE ( 'NONE', *, *, #35142, .T. ) ;
#2844=LINE ( 'NONE', #43728, #39877 ) ;
#2846=ORIENTED_EDGE ( 'NONE', *, *, #13321, .F. ) ;
#2847=ORIENTED_EDGE ( 'NONE', *, *, #34455, .T. ) ;
#2850=LINE ( 'NONE', #18010, #40754 ) ;
#2851=ADVANCED_FACE ( 'NONE', ( #1325 ), #13070, .T. ) ;
#2854=EDGE_LOOP ( 'NONE', ( #45653, #17468, #34764, #23893 ) ) ;
#2855=CARTESIAN_POINT ( 'NONE',  ( 10.00000000000000000, 35.91791733033570466, -68.67312586194960033 ) ) ;
#2858=EDGE_CURVE ( 'NONE', #37895, #45965, #23595, .T. ) ;
#2864=AXIS2_PLACEMENT_3D ( 'NONE', #3347, #33226, #48152 ) ;
#2865=ADVANCED_FACE ( 'NONE', ( #16013 ), #19655, .T. ) ;
#2868=FACE_OUTER_BOUND ( 'NONE', #43775, .T. ) ;
#2869=ORIENTED_EDGE ( 'NONE', *, *, #14040, .F. ) ;
#2870=CYLINDRICAL_SURFACE ( 'NONE', #37400, 31.99999999999998579 ) ;
#2871=DIRECTION ( 'NONE',  ( -1.000000000000000000, -0.000000000000000000, 0.000000000000000000 ) ) ;
#2877=EDGE_CURVE ( 'NONE', #9073, #20085, #12580, .T. ) ;
#2883=CARTESIAN_POINT ( 'NONE',  ( 0.000000000000000000, -80.55351364060578589, -15.33399622253568673 ) ) ;
#2888=ORIENTED_EDGE ( 'NONE', *, *, #35460, .T. ) ;
#2889=VERTEX_POINT ( 'NONE', #8897 ) ;
#2890=AXIS2_PLACEMENT_3D ( 'NONE', #21353, #22072, #32391 ) ;
#2892=AXIS2_PLACEMENT_3D ( 'NONE', #43474, #46666, #28058 ) ;
#2895=VECTOR ( 'NONE', #11394, 1000.000000000000000 ) ;
#2898=EDGE_LOOP ( 'NONE', ( #26263, #38088, #25427, #15314 ) ) ;
#2901=VECTOR ( 'NONE', #25301, 1000.000000000000000 ) ;
#2913=EDGE_CURVE ( 'NONE', #19886, #28052, #34586, .T. ) ;
#2916=ORIENTED_EDGE ( 'NONE', *, *, #38071, .T. ) ;
#2925=ORIENTED_EDGE ( 'NONE', *, *, #45711, .T. ) ;
#2936=CARTESIAN_POINT ( 'NONE',  ( 10.00000000000000000, -59.03342792756231461, -46.54456581323868392 ) ) ;
#2939=LINE ( 'NONE', #41132, #37323 ) ;
#2943=AXIS2_PLACEMENT_3D ( 'NONE', #43391, #9847, #5696 ) ;
#2947=EDGE_LOOP ( 'NONE', ( #8786, #22367, #17204, #26752 ) ) ;
#2953=ORIENTED_EDGE ( 'NONE', *, *, #1959, .T. ) ;
#2957=ORIENTED_EDGE ( 'NONE', *, *, #45172, .T. ) ;
#2958=CARTESIAN_POINT ( 'NONE',  ( 0.000000000000000000, -67.80270845531921964, 46.11716303203163392 ) ) ;
#2971=DIRECTION ( 'NONE',  ( 0.000000000000000000, 0.8090169943749487835, -0.5877852522924712497 ) ) ;
#2972=ORIENTED_EDGE ( 'NONE', *, *, #37365, .F. ) ;
#2976=EDGE_CURVE ( 'NONE', #37949, #43544, #10336, .T. ) ;
#2981=CYLINDRICAL_SURFACE ( 'NONE', #14905, 77.49899999999999523 ) ;
#2989=VERTEX_POINT ( 'NONE', #40219 ) ;
#2993=DIRECTION ( 'NONE',  ( 0.000000000000000000, -0.7604059656000368150, 0.6494480483301767748 ) ) ;
#2995=FACE_OUTER_BOUND ( 'NONE', #47205, .T. ) ;
#2998=DIRECTION ( 'NONE',  ( -1.000000000000000000, 0.000000000000000000, 0.000000000000000000 ) ) ;
#2999=CARTESIAN_POINT ( 'NONE',  ( 10.00000000000000000, 2.956366410621684260, -75.11725578898465017 ) ) ;
#3006=DIRECTION ( 'NONE',  ( -1.000000000000000000, 0.000000000000000000, 0.000000000000000000 ) ) ;
#3009=ORIENTED_EDGE ( 'NONE', *, *, #4094, .F. ) ;
#3011=CARTESIAN_POINT ( 'NONE',  ( 10.00000000000000000, -16.65972982744992592, 80.28980883073749908 ) ) ;
#3021=EDGE_CURVE ( 'NONE', #45240, #13460, #28473, .T. ) ;
#3029=CIRCLE ( 'NONE', #26496, 77.49900000000002365 ) ;
#3030=EDGE_CURVE ( 'NONE', #13135, #28683, #19979, .T. ) ;
#3047=AXIS2_PLACEMENT_3D ( 'NONE', #40586, #21509, #28617 ) ;
#3050=DIRECTION ( 'NONE',  ( 0.000000000000000000, 0.3826834323650842862, 0.9238795325112890700 ) ) ;
#3055=CARTESIAN_POINT ( 'NONE',  ( 0.000000000000000000, 0.000000000000000000, 0.000000000000000000 ) ) ;
#3058=LINE ( 'NONE', #17260, #40245 ) ;
#3060=CARTESIAN_POINT ( 'NONE',  ( 10.00000000000000000, 55.20638768913760686, 51.02545421589343988 ) ) ;
#3061=ORIENTED_EDGE ( 'NONE', *, *, #37337, .T. ) ;
#3066=FACE_OUTER_BOUND ( 'NONE', #16381, .T. ) ;
#3069=CARTESIAN_POINT ( 'NONE',  ( 10.00000000000000000, -75.11725578898466438, -2.956366410621452001 ) ) ;
#3071=ORIENTED_EDGE ( 'NONE', *, *, #25984, .T. ) ;
#3073=CARTESIAN_POINT ( 'NONE',  ( 10.00000000000000000, -15.33399622253540251, 80.55351364060582853 ) ) ;
#3077=ORIENTED_EDGE ( 'NONE', *, *, #34407, .T. ) ;
#3087=EDGE_CURVE ( 'NONE', #2339, #35473, #7370, .T. ) ;
#3089=DIRECTION ( 'NONE',  ( 0.000000000000000000, 0.8910065241883690090, -0.4539904997395446395 ) ) ;
#3098=ORIENTED_EDGE ( 'NONE', *, *, #15540, .T. ) ;
#3106=AXIS2_PLACEMENT_3D ( 'NONE', #35258, #39178, #3160 ) ;
#3110=AXIS2_PLACEMENT_3D ( 'NONE', #27172, #46015, #45511 ) ;
#3118=ORIENTED_EDGE ( 'NONE', *, *, #21084, .F. ) ;
#3122=ORIENTED_EDGE ( 'NONE', *, *, #25130, .F. ) ;
#3125=ORIENTED_EDGE ( 'NONE', *, *, #36938, .F. ) ;
#3133=DIRECTION ( 'NONE',  ( -1.000000000000000000, -0.000000000000000000, 0.000000000000000000 ) ) ;
#3136=EDGE_CURVE ( 'NONE', #6704, #9220, #19780, .T. ) ;
#3139=AXIS2_PLACEMENT_3D ( 'NONE', #39939, #47987, #32358 ) ;
#3140=EDGE_CURVE ( 'NONE', #43853, #8436, #47246, .T. ) ;
#3145=ORIENTED_EDGE ( 'NONE', *, *, #25841, .T. ) ;
#3146=AXIS2_PLACEMENT_3D ( 'NONE', #19121, #7862, #37727 ) ;
#3147=DIRECTION ( 'NONE',  ( 1.000000000000000000, 0.000000000000000000, 0.000000000000000000 ) ) ;
#3149=VERTEX_POINT ( 'NONE', #10832 ) ;
#3160=DIRECTION ( 'NONE',  ( 0.000000000000000000, 0.9238795325112877377, -0.3826834323650873948 ) ) ;
#3165=LINE ( 'NONE', #33284, #18315 ) ;
#3174=DIRECTION ( 'NONE',  ( -1.000000000000000000, -0.000000000000000000, -0.000000000000000000 ) ) ;
#3175=AXIS2_PLACEMENT_3D ( 'NONE', #13525, #2500, #24791 ) ;
#3182=AXIS2_PLACEMENT_3D ( 'NONE', #41109, #37911, #15874 ) ;
#3187=ORIENTED_EDGE ( 'NONE', *, *, #22923, .T. ) ;
#3193=VERTEX_POINT ( 'NONE', #5122 ) ;
#3202=CIRCLE ( 'NONE', #103, 77.49900000000002365 ) ;
#3203=LINE ( 'NONE', #36505, #23425 ) ;
#3204=CARTESIAN_POINT ( 'NONE',  ( 10.00000000000000000, 0.000000000000000000, 0.000000000000000000 ) ) ;
#3213=VECTOR ( 'NONE', #32945, 1000.000000000000000 ) ;
#3218=FACE_OUTER_BOUND ( 'NONE', #27755, .T. ) ;
#3220=FACE_OUTER_BOUND ( 'NONE', #31301, .T. ) ;
#3222=DIRECTION ( 'NONE',  ( 1.000000000000000000, 0.000000000000000000, -0.000000000000000000 ) ) ;
#3226=DIRECTION ( 'NONE',  ( 0.000000000000000000, 0.000000000000000000, 1.000000000000000000 ) ) ;
#3227=CARTESIAN_POINT ( 'NONE',  ( 10.00000000000000000, -41.19522573413687638, -65.64334221924953283 ) ) ;
#3231=DIRECTION ( 'NONE',  ( -1.000000000000000000, 0.000000000000000000, 0.000000000000000000 ) ) ;
#3235=EDGE_CURVE ( 'NONE', #23364, #10143, #33344, .T. ) ;
#3237=VERTEX_POINT ( 'NONE', #9980 ) ;
#3246=AXIS2_PLACEMENT_3D ( 'NONE', #2541, #40011, #24832 ) ;
#3249=ORIENTED_EDGE ( 'NONE', *, *, #43702, .T. ) ;
#3250=ORIENTED_EDGE ( 'NONE', *, *, #44216, .F. ) ;
#3256=CARTESIAN_POINT ( 'NONE',  ( 5.000000000000002665, -16.65972982744991882, 80.28980883073752750 ) ) ;
#3257=DIRECTION ( 'NONE',  ( 0.000000000000000000, -0.9510565162951565288, 0.3090169943749382919 ) ) ;
#3258=CIRCLE ( 'NONE', #918, 82.00000000000000000 ) ;
#3259=VERTEX_POINT ( 'NONE', #13669 ) ;
#3262=DIRECTION ( 'NONE',  ( -1.000000000000000000, -0.000000000000000000, 0.000000000000000000 ) ) ;
#3268=DIRECTION ( 'NONE',  ( 0.000000000000000000, 0.000000000000000000, 1.000000000000000000 ) ) ;
#3290=CARTESIAN_POINT ( 'NONE',  ( 10.00000000000000000, -73.72996012237449293, 14.67089635893687571 ) ) ;
#3292=CARTESIAN_POINT ( 'NONE',  ( 10.00000000000000000, -75.11764819372149304, 2.946379043146075905 ) ) ;
#3294=EDGE_CURVE ( 'NONE', #45623, #6665, #3842, .T. ) ;
#3296=CARTESIAN_POINT ( 'NONE',  ( 0.000000000000000000, 0.000000000000000000, 0.000000000000000000 ) ) ;
#3302=DIRECTION ( 'NONE',  ( -1.000000000000000000, -0.000000000000000000, 0.000000000000000000 ) ) ;
#3303=ORIENTED_EDGE ( 'NONE', *, *, #32493, .F. ) ;
#3308=CARTESIAN_POINT ( 'NONE',  ( 10.00000000000000000, -71.21200624218823805, 40.65526001592589722 ) ) ;
#3313=DIRECTION ( 'NONE',  ( -1.000000000000000000, 0.000000000000000000, 0.000000000000000000 ) ) ;
#3315=CARTESIAN_POINT ( 'NONE',  ( 10.00000000000000000, 77.32052557432841411, 5.256550761633138613 ) ) ;
#3316=AXIS2_PLACEMENT_3D ( 'NONE', #28094, #20492, #12442 ) ;
#3319=AXIS2_PLACEMENT_3D ( 'NONE', #42183, #41706, #23576 ) ;
#3322=LINE ( 'NONE', #29287, #14933 ) ;
#3325=AXIS2_PLACEMENT_3D ( 'NONE', #42013, #4559, #38830 ) ;
#3326=ORIENTED_EDGE ( 'NONE', *, *, #25398, .F. ) ;
#3327=ORIENTED_EDGE ( 'NONE', *, *, #30178, .T. ) ;
#3333=CARTESIAN_POINT ( 'NONE',  ( 10.00000000000000000, -36.73666225445940370, 65.58780272294062286 ) ) ;
#3335=CYLINDRICAL_SURFACE ( 'NONE', #46372, 31.99999999999999289 ) ;
#3344=DIRECTION ( 'NONE',  ( -1.000000000000000000, 0.000000000000000000, 0.000000000000000000 ) ) ;
#3346=CARTESIAN_POINT ( 'NONE',  ( 5.000000000000000000, -68.55367621811112144, -44.99326035066125939 ) ) ;
#3347=CARTESIAN_POINT ( 'NONE',  ( 10.00000000000000000, 0.000000000000000000, 0.000000000000000000 ) ) ;
#3349=CIRCLE ( 'NONE', #36952, 82.00000000000000000 ) ;
#3350=EDGE_CURVE ( 'NONE', #22595, #7784, #19003, .T. ) ;
#3351=CIRCLE ( 'NONE', #5713, 77.49900000000002365 ) ;
#3357=AXIS2_PLACEMENT_3D ( 'NONE', #15810, #863, #37114 ) ;
#3368=EDGE_LOOP ( 'NONE', ( #24723, #11491, #31582, #33311 ) ) ;
#3375=DIRECTION ( 'NONE',  ( -1.000000000000000000, 0.000000000000000000, 0.000000000000000000 ) ) ;
#3377=CARTESIAN_POINT ( 'NONE',  ( 0.000000000000000000, 24.73286445877703699, 73.44644590900068692 ) ) ;
#3379=VECTOR ( 'NONE', #5315, 1000.000000000000000 ) ;
#3383=VECTOR ( 'NONE', #654, 1000.000000000000000 ) ;
#3386=DIRECTION ( 'NONE',  ( -1.000000000000000000, -0.000000000000000000, -0.000000000000000000 ) ) ;
#3390=ORIENTED_EDGE ( 'NONE', *, *, #38914, .F. ) ;
#3406=CARTESIAN_POINT ( 'NONE',  ( 5.000000000000002665, 81.34940948281351325, -10.30890764327296161 ) ) ;
#3410=DIRECTION ( 'NONE',  ( 1.000000000000000000, 0.000000000000000000, -0.000000000000000000 ) ) ;
#3411=ADVANCED_FACE ( 'NONE', ( #36645 ), #43753, .T. ) ;
#3418=AXIS2_PLACEMENT_3D ( 'NONE', #11059, #2742, #28924 ) ;
#3423=CIRCLE ( 'NONE', #13608, 31.99999999999999645 ) ;
#3433=DIRECTION ( 'NONE',  ( 0.000000000000000000, 0.7071067811865439090, 0.7071067811865512365 ) ) ;
#3434=ORIENTED_EDGE ( 'NONE', *, *, #30667, .F. ) ;
#3436=ORIENTED_EDGE ( 'NONE', *, *, #21804, .T. ) ;
#3439=CARTESIAN_POINT ( 'NONE',  ( 0.000000000000000000, -15.33399622253540961, 80.55351364060584274 ) ) ;
#3441=DIRECTION ( 'NONE',  ( 1.000000000000000000, 0.000000000000000000, 0.000000000000000000 ) ) ;
#3444=ORIENTED_EDGE ( 'NONE', *, *, #17635, .T. ) ;
#3452=ORIENTED_EDGE ( 'NONE', *, *, #11934, .T. ) ;
#3455=EDGE_CURVE ( 'NONE', #18078, #12619, #35713, .T. ) ;
#3467=DIRECTION ( 'NONE',  ( -1.000000000000000000, -0.000000000000000000, 0.000000000000000000 ) ) ;
#3473=CYLINDRICAL_SURFACE ( 'NONE', #10909, 77.49899999999999523 ) ;
#3477=VECTOR ( 'NONE', #46918, 1000.000000000000000 ) ;
#3492=ORIENTED_EDGE ( 'NONE', *, *, #15630, .F. ) ;
#3494=ORIENTED_EDGE ( 'NONE', *, *, #25032, .F. ) ;
#3495=CYLINDRICAL_SURFACE ( 'NONE', #12083, 82.00000000000000000 ) ;
#3497=CARTESIAN_POINT ( 'NONE',  ( 10.00000000000000000, 72.35160999960817207, 20.41045688087850607 ) ) ;
#3511=CIRCLE ( 'NONE', #5102, 77.49899999999999523 ) ;
#3512=EDGE_LOOP ( 'NONE', ( #29808, #38762, #16961, #15142 ) ) ;
#3513=CIRCLE ( 'NONE', #5876, 31.99999999999999289 ) ;
#3515=DIRECTION ( 'NONE',  ( 1.000000000000000000, 0.000000000000000000, 0.000000000000000000 ) ) ;
#3519=ORIENTED_EDGE ( 'NONE', *, *, #37903, .T. ) ;
#3522=ORIENTED_EDGE ( 'NONE', *, *, #46589, .T. ) ;
#3526=VECTOR ( 'NONE', #43810, 1000.000000000000000 ) ;
#3535=AXIS2_PLACEMENT_3D ( 'NONE', #5714, #46603, #28000 ) ;
#3539=CARTESIAN_POINT ( 'NONE',  ( 10.00000000000000000, 17.28742895386084655, 75.54627589209950145 ) ) ;
#3541=DIRECTION ( 'NONE',  ( -1.000000000000000000, -0.000000000000000000, 0.000000000000000000 ) ) ;
#3543=EDGE_CURVE ( 'NONE', #13144, #12926, #31045, .T. ) ;
#3545=CARTESIAN_POINT ( 'NONE',  ( 10.00000000000000000, -15.33399622253424965, -80.55351364060605590 ) ) ;
#3556=ORIENTED_EDGE ( 'NONE', *, *, #22753, .F. ) ;
#3558=VECTOR ( 'NONE', #39500, 1000.000000000000000 ) ;
#3561=CARTESIAN_POINT ( 'NONE',  ( 10.00000000000000000, 51.02545421589324803, 55.20638768913779870 ) ) ;
#3568=DIRECTION ( 'NONE',  ( 1.000000000000000000, -0.000000000000000000, -0.000000000000000000 ) ) ;
#3573=DIRECTION ( 'NONE',  ( 0.000000000000000000, 0.000000000000000000, 1.000000000000000000 ) ) ;
#3583=CIRCLE ( 'NONE', #30968, 82.00000000000000000 ) ;
#3597=CARTESIAN_POINT ( 'NONE',  ( -10.00000000000000000, 0.000000000000000000, 0.000000000000000000 ) ) ;
#3603=EDGE_CURVE ( 'NONE', #45052, #28496, #38059, .T. ) ;
#3604=DIRECTION ( 'NONE',  ( -1.000000000000000000, -0.000000000000000000, 0.000000000000000000 ) ) ;
#3605=DIRECTION ( 'NONE',  ( -1.000000000000000000, 0.000000000000000000, -0.000000000000000000 ) ) ;
#3606=AXIS2_PLACEMENT_3D ( 'NONE', #47706, #25676, #40155 ) ;
#3608=DIRECTION ( 'NONE',  ( -1.000000000000000000, -0.000000000000000000, -0.000000000000000000 ) ) ;
#3612=AXIS2_PLACEMENT_3D ( 'NONE', #15358, #38105, #41532 ) ;
#3613=CARTESIAN_POINT ( 'NONE',  ( -10.00000000000000000, 0.000000000000000000, 0.000000000000000000 ) ) ;
#3617=AXIS2_PLACEMENT_3D ( 'NONE', #11481, #18317, #26403 ) ;
#3619=CIRCLE ( 'NONE', #8307, 82.00000000000000000 ) ;
#3621=CARTESIAN_POINT ( 'NONE',  ( 0.000000000000000000, 62.50329211542494789, -41.76937507738723099 ) ) ;
#3623=ORIENTED_EDGE ( 'NONE', *, *, #2418, .T. ) ;
#3635=ORIENTED_EDGE ( 'NONE', *, *, #37997, .T. ) ;
#3637=EDGE_CURVE ( 'NONE', #6704, #16500, #20864, .T. ) ;
#3641=DIRECTION ( 'NONE',  ( -1.000000000000000000, -0.000000000000000000, 0.000000000000000000 ) ) ;
#3654=DIRECTION ( 'NONE',  ( -1.000000000000000000, -0.000000000000000000, -0.000000000000000000 ) ) ;
#3667=DIRECTION ( 'NONE',  ( 1.000000000000000000, 0.000000000000000000, 0.000000000000000000 ) ) ;
#3669=VERTEX_POINT ( 'NONE', #24138 ) ;
#3671=AXIS2_PLACEMENT_3D ( 'NONE', #36112, #18222, #13363 ) ;
#3672=EDGE_CURVE ( 'NONE', #2120, #16057, #22442, .T. ) ;
#3680=LINE ( 'NONE', #39932, #8492 ) ;
#3681=ORIENTED_EDGE ( 'NONE', *, *, #7115, .F. ) ;
#3687=DIRECTION ( 'NONE',  ( 0.000000000000000000, 0.000000000000000000, 1.000000000000000000 ) ) ;
#3688=DIRECTION ( 'NONE',  ( -1.000000000000000000, -0.000000000000000000, -0.000000000000000000 ) ) ;
#3692=EDGE_CURVE ( 'NONE', #27936, #13603, #26353, .T. ) ;
#3695=CARTESIAN_POINT ( 'NONE',  ( 0.000000000000000000, 74.74816331893430288, 33.71516098798768013 ) ) ;
#3698=ORIENTED_EDGE ( 'NONE', *, *, #41058, .F. ) ;
#3704=CARTESIAN_POINT ( 'NONE',  ( 0.000000000000000000, 62.50884508063427347, 41.76106447765511831 ) ) ;
#3715=CARTESIAN_POINT ( 'NONE',  ( 10.00000000000000000, -34.44570377933649041, 69.42325613327427902 ) ) ;
#3723=DIRECTION ( 'NONE',  ( -1.000000000000000000, -0.000000000000000000, 0.000000000000000000 ) ) ;
#3724=CARTESIAN_POINT ( 'NONE',  ( 0.000000000000000000, 76.66974797899852945, -11.30684508768257679 ) ) ;
#3729=CARTESIAN_POINT ( 'NONE',  ( 10.00000000000000000, 5.256550761633969060, -77.32052557432835727 ) ) ;
#3730=LINE ( 'NONE', #18423, #40530 ) ;
#3732=ORIENTED_EDGE ( 'NONE', *, *, #39586, .F. ) ;
#3734=CIRCLE ( 'NONE', #39705, 31.99999999999999289 ) ;
#3736=LINE ( 'NONE', #18659, #2536 ) ;
#3739=VERTEX_POINT ( 'NONE', #36110 ) ;
#3740=AXIS2_PLACEMENT_3D ( 'NONE', #11899, #8688, #22905 ) ;
#3742=DIRECTION ( 'NONE',  ( -1.000000000000000000, 0.000000000000000000, 0.000000000000000000 ) ) ;
#3743=VERTEX_POINT ( 'NONE', #3545 ) ;
#3755=EDGE_CURVE ( 'NONE', #33968, #47670, #22142, .T. ) ;
#3757=FACE_OUTER_BOUND ( 'NONE', #3958, .T. ) ;
#3758=CARTESIAN_POINT ( 'NONE',  ( 0.000000000000000000, 0.000000000000000000, 0.000000000000000000 ) ) ;
#3759=FACE_OUTER_BOUND ( 'NONE', #29095, .T. ) ;
#3764=VERTEX_POINT ( 'NONE', #21894 ) ;
#3766=DIRECTION ( 'NONE',  ( 0.000000000000000000, 0.000000000000000000, -1.000000000000000000 ) ) ;
#3769=CYLINDRICAL_SURFACE ( 'NONE', #47683, 12.50000000000000000 ) ;
#3776=CARTESIAN_POINT ( 'NONE',  ( 0.000000000000000000, -66.50666863321971789, -39.78640506895676054 ) ) ;
#3778=ORIENTED_EDGE ( 'NONE', *, *, #29950, .T. ) ;
#3779=LINE ( 'NONE', #4029, #42763 ) ;
#3789=AXIS2_PLACEMENT_3D ( 'NONE', #23684, #38636, #39105 ) ;
#3791=AXIS2_PLACEMENT_3D ( 'NONE', #22427, #37103, #27069 ) ;
#3792=CARTESIAN_POINT ( 'NONE',  ( 10.00000000000000000, 73.95703589264006439, -23.16143007188350822 ) ) ;
#3793=ORIENTED_EDGE ( 'NONE', *, *, #40289, .T. ) ;
#3800=CARTESIAN_POINT ( 'NONE',  ( 10.00000000000000000, 62.50884508063487033, -41.76106447765422303 ) ) ;
#3806=CARTESIAN_POINT ( 'NONE',  ( 10.00000000000000000, 55.19960302592066625, 51.03279382321107249 ) ) ;
#3808=LINE ( 'NONE', #29752, #44918 ) ;
#3810=ORIENTED_EDGE ( 'NONE', *, *, #24211, .F. ) ;
#3813=VERTEX_POINT ( 'NONE', #10163 ) ;
#3817=CARTESIAN_POINT ( 'NONE',  ( 10.00000000000000000, 0.000000000000000000, 0.000000000000000000 ) ) ;
#3820=ORIENTED_EDGE ( 'NONE', *, *, #28732, .T. ) ;
#3833=DIRECTION ( 'NONE',  ( -1.000000000000000000, 0.000000000000000000, 0.000000000000000000 ) ) ;
#3835=DIRECTION ( 'NONE',  ( 0.000000000000000000, 0.3826834323650907810, -0.9238795325112864054 ) ) ;
#3836=DIRECTION ( 'NONE',  ( 1.000000000000000000, -0.000000000000000000, 0.000000000000000000 ) ) ;
#3842=CIRCLE ( 'NONE', #37449, 31.99999999999998934 ) ;
#3845=LINE ( 'NONE', #41780, #39991 ) ;
#3850=ORIENTED_EDGE ( 'NONE', *, *, #9160, .F. ) ;
#3853=VERTEX_POINT ( 'NONE', #6497 ) ;
#3855=SHAPE_REPRESENTATION_RELATIONSHIP ( 'NONE' , 'NONE' ,  #31260, #31571 ) ;
#3856=CARTESIAN_POINT ( 'NONE',  ( 0.000000000000000000, 0.000000000000000000, 0.000000000000000000 ) ) ;
#3866=EDGE_CURVE ( 'NONE', #8218, #34570, #41918, .T. ) ;
#3875=ORIENTED_EDGE ( 'NONE', *, *, #44754, .F. ) ;
#3879=ORIENTED_EDGE ( 'NONE', *, *, #40840, .F. ) ;
#3883=ORIENTED_EDGE ( 'NONE', *, *, #1054, .F. ) ;
#3887=AXIS2_PLACEMENT_3D ( 'NONE', #15414, #41120, #37432 ) ;
#3891=VERTEX_POINT ( 'NONE', #38052 ) ;
#3892=CARTESIAN_POINT ( 'NONE',  ( 5.000000000000000000, 68.55367621811141987, 44.99326035066078333 ) ) ;
#3894=CARTESIAN_POINT ( 'NONE',  ( 10.00000000000000000, -50.95692526931372157, 58.39081064771733054 ) ) ;
#3897=FACE_OUTER_BOUND ( 'NONE', #25999, .T. ) ;
#3900=CARTESIAN_POINT ( 'NONE',  ( 0.000000000000000000, 0.000000000000000000, 0.000000000000000000 ) ) ;
#3902=CARTESIAN_POINT ( 'NONE',  ( 10.00000000000000000, 8.840884882375075193, 74.65374052328651544 ) ) ;
#3904=AXIS2_PLACEMENT_3D ( 'NONE', #28202, #43387, #2254 ) ;
#3906=ORIENTED_EDGE ( 'NONE', *, *, #5531, .T. ) ;
#3918=ORIENTED_EDGE ( 'NONE', *, *, #13261, .F. ) ;
#3924=EDGE_CURVE ( 'NONE', #10878, #23379, #41479, .T. ) ;
#3926=ORIENTED_EDGE ( 'NONE', *, *, #1332, .F. ) ;
#3934=CARTESIAN_POINT ( 'NONE',  ( 10.00000000000000000, 75.11764819372149304, -2.946379043146603482 ) ) ;
#3935=AXIS2_PLACEMENT_3D ( 'NONE', #25424, #3386, #44514 ) ;
#3941=CARTESIAN_POINT ( 'NONE',  ( 10.00000000000000000, -81.90746397400386059, -3.894527615418773347 ) ) ;
#3945=CARTESIAN_POINT ( 'NONE',  ( 10.00000000000000000, 27.74655509720669144, 77.16300072079670258 ) ) ;
#3946=DIRECTION ( 'NONE',  ( 0.000000000000000000, -0.07845909572783053842, -0.9969173337331290741 ) ) ;
#3952=ORIENTED_EDGE ( 'NONE', *, *, #9433, .T. ) ;
#3956=DIRECTION ( 'NONE',  ( -1.000000000000000000, 0.000000000000000000, 0.000000000000000000 ) ) ;
#3957=DIRECTION ( 'NONE',  ( 0.000000000000000000, -0.9238795325112822976, -0.3826834323651006065 ) ) ;
#3958=EDGE_LOOP ( 'NONE', ( #15499, #27224, #24592, #14182 ) ) ;
#3960=CARTESIAN_POINT ( 'NONE',  ( 10.00000000000000000, 73.73191006444551476, 14.66109333815590254 ) ) ;
#3971=CARTESIAN_POINT ( 'NONE',  ( -10.00000000000000000, 0.000000000000000000, 0.000000000000000000 ) ) ;
#3973=VECTOR ( 'NONE', #35315, 1000.000000000000000 ) ;
#3974=CIRCLE ( 'NONE', #38350, 31.99999999999999289 ) ;
#3976=DIRECTION ( 'NONE',  ( -1.000000000000000000, -0.000000000000000000, 0.000000000000000000 ) ) ;
#3978=DIRECTION ( 'NONE',  ( 0.000000000000000000, 0.000000000000000000, 1.000000000000000000 ) ) ;
#3980=CIRCLE ( 'NONE', #22725, 77.49900000000000944 ) ;
#3982=ORIENTED_EDGE ( 'NONE', *, *, #16423, .T. ) ;
#3997=CARTESIAN_POINT ( 'NONE',  ( 0.000000000000000000, 0.000000000000000000, 0.000000000000000000 ) ) ;
#4003=VECTOR ( 'NONE', #16395, 1000.000000000000000 ) ;
#4004=ORIENTED_EDGE ( 'NONE', *, *, #8970, .F. ) ;
#4009=DIRECTION ( 'NONE',  ( -1.000000000000000000, 0.000000000000000000, 0.000000000000000000 ) ) ;
#4013=VECTOR ( 'NONE', #17791, 1000.000000000000000 ) ;
#4014=CARTESIAN_POINT ( 'NONE',  ( 10.00000000000000000, 58.39081064771823293, -50.95692526931266286 ) ) ;
#4017=DIRECTION ( 'NONE',  ( -1.000000000000000000, 0.000000000000000000, 0.000000000000000000 ) ) ;
#4025=CARTESIAN_POINT ( 'NONE',  ( -10.00000000000000000, 0.000000000000000000, 0.000000000000000000 ) ) ;
#4026=DIRECTION ( 'NONE',  ( -1.000000000000000000, 0.000000000000000000, -0.000000000000000000 ) ) ;
#4027=DIRECTION ( 'NONE',  ( -1.000000000000000000, 0.000000000000000000, -0.000000000000000000 ) ) ;
#4029=CARTESIAN_POINT ( 'NONE',  ( 5.000000000000000000, 81.96053171279902472, -2.543863470248670211 ) ) ;
#4032=CARTESIAN_POINT ( 'NONE',  ( 10.00000000000000000, 0.000000000000000000, 0.000000000000000000 ) ) ;
#4036=CARTESIAN_POINT ( 'NONE',  ( 10.00000000000000000, 36.72794159290334903, -65.59268652807170952 ) ) ;
#4038=CYLINDRICAL_SURFACE ( 'NONE', #2822, 31.99999999999999289 ) ;
#4040=CARTESIAN_POINT ( 'NONE',  ( 0.000000000000000000, 75.11764819372149304, -2.946379043146603482 ) ) ;
#4046=EDGE_CURVE ( 'NONE', #13148, #11292, #6713, .T. ) ;
#4053=DIRECTION ( 'NONE',  ( -1.000000000000000000, 0.000000000000000000, 0.000000000000000000 ) ) ;
#4060=ORIENTED_EDGE ( 'NONE', *, *, #37418, .T. ) ;
#4065=ORIENTED_EDGE ( 'NONE', *, *, #29169, .F. ) ;
#4068=CARTESIAN_POINT ( 'NONE',  ( -10.00000000000000000, 0.000000000000000000, 0.000000000000000000 ) ) ;
#4070=AXIS2_PLACEMENT_3D ( 'NONE', #35299, #42901, #1775 ) ;
#4074=DIRECTION ( 'NONE',  ( 1.000000000000000000, 0.000000000000000000, 0.000000000000000000 ) ) ;
#4080=EDGE_CURVE ( 'NONE', #39866, #25379, #44244, .T. ) ;
#4083=ORIENTED_EDGE ( 'NONE', *, *, #17683, .T. ) ;
#4090=EDGE_CURVE ( 'NONE', #17460, #6193, #35648, .T. ) ;
#4091=CYLINDRICAL_SURFACE ( 'NONE', #33179, 31.99999999999999289 ) ;
#4093=CARTESIAN_POINT ( 'NONE',  ( 10.00000000000000000, -68.55367621811110723, -44.99326035066125939 ) ) ;
#4094=EDGE_CURVE ( 'NONE', #28981, #42650, #27057, .T. ) ;
#4097=CARTESIAN_POINT ( 'NONE',  ( 0.000000000000000000, 21.60688246758585507, 79.10210256391376049 ) ) ;
#4099=DIRECTION ( 'NONE',  ( -1.000000000000000000, -0.000000000000000000, -0.000000000000000000 ) ) ;
#4106=VECTOR ( 'NONE', #33814, 1000.000000000000000 ) ;
#4117=ORIENTED_EDGE ( 'NONE', *, *, #15260, .F. ) ;
#4118=ORIENTED_EDGE ( 'NONE', *, *, #8151, .T. ) ;
#4125=ORIENTED_EDGE ( 'NONE', *, *, #7115, .T. ) ;
#4126=ORIENTED_EDGE ( 'NONE', *, *, #45711, .F. ) ;
#4132=ORIENTED_EDGE ( 'NONE', *, *, #18095, .F. ) ;
#4136=AXIS2_PLACEMENT_3D ( 'NONE', #16901, #21042, #20312 ) ;
#4138=VERTEX_POINT ( 'NONE', #10081 ) ;
#4142=CIRCLE ( 'NONE', #18960, 77.49900000000000944 ) ;
#4155=CARTESIAN_POINT ( 'NONE',  ( 10.00000000000000000, 2.946379043147425492, -75.11764819372145041 ) ) ;
#4167=AXIS2_PLACEMENT_3D ( 'NONE', #15184, #44545, #33042 ) ;
#4169=ORIENTED_EDGE ( 'NONE', *, *, #38145, .T. ) ;
#4171=EDGE_CURVE ( 'NONE', #35650, #8522, #2487, .T. ) ;
#4173=CIRCLE ( 'NONE', #29951, 82.00000000000000000 ) ;
#4185=ORIENTED_EDGE ( 'NONE', *, *, #13381, .T. ) ;
#4186=VERTEX_POINT ( 'NONE', #43386 ) ;
#4187=AXIS2_PLACEMENT_3D ( 'NONE', #11061, #18640, #26718 ) ;
#4199=CYLINDRICAL_SURFACE ( 'NONE', #610, 32.00000000000000000 ) ;
#4200=ORIENTED_EDGE ( 'NONE', *, *, #13047, .F. ) ;
#4203=CARTESIAN_POINT ( 'NONE',  ( 10.00000000000000000, 74.65491531819118620, -8.830959090342659579 ) ) ;
#4205=CARTESIAN_POINT ( 'NONE',  ( 0.000000000000000000, 0.000000000000000000, 0.000000000000000000 ) ) ;
#4210=EDGE_CURVE ( 'NONE', #3259, #11083, #25231, .T. ) ;
#4211=CARTESIAN_POINT ( 'NONE',  ( 10.00000000000000000, 16.65972982744934683, 80.28980883073762698 ) ) ;
#4223=CARTESIAN_POINT ( 'NONE',  ( 0.000000000000000000, 81.50828551894227303, 8.966570791700979370 ) ) ;
#4234=DIRECTION ( 'NONE',  ( -1.000000000000000000, -0.000000000000000000, 0.000000000000000000 ) ) ;
#4241=CARTESIAN_POINT ( 'NONE',  ( 0.000000000000000000, 33.71516098798849015, -74.74816331893394761 ) ) ;
#4251=VERTEX_POINT ( 'NONE', #43141 ) ;
#4252=CIRCLE ( 'NONE', #6581, 77.49900000000000944 ) ;
#4254=DIRECTION ( 'NONE',  ( 0.000000000000000000, 0.000000000000000000, 1.000000000000000000 ) ) ;
#4257=CARTESIAN_POINT ( 'NONE',  ( 0.000000000000000000, 31.46837873495072913, -68.27212725128242710 ) ) ;
#4258=ORIENTED_EDGE ( 'NONE', *, *, #4266, .F. ) ;
#4260=VECTOR ( 'NONE', #14450, 1000.000000000000000 ) ;
#4266=EDGE_CURVE ( 'NONE', #39544, #20444, #21811, .T. ) ;
#4268=AXIS2_PLACEMENT_3D ( 'NONE', #2638, #18301, #21245 ) ;
#4269=EDGE_CURVE ( 'NONE', #32513, #46010, #28660, .T. ) ;
#4271=LINE ( 'NONE', #18921, #44561 ) ;
#4275=CIRCLE ( 'NONE', #28511, 82.00000000000000000 ) ;
#4282=DIRECTION ( 'NONE',  ( -1.000000000000000000, 0.000000000000000000, -0.000000000000000000 ) ) ;
#4285=DIRECTION ( 'NONE',  ( 0.000000000000000000, 0.9238795325112851842, 0.3826834323650937786 ) ) ;
#4286=CARTESIAN_POINT ( 'NONE',  ( 0.000000000000000000, 77.32052557432849937, -5.256550761632002633 ) ) ;
#4289=CIRCLE ( 'NONE', #7377, 77.49899999999999523 ) ;
#4292=DIRECTION ( 'NONE',  ( 0.000000000000000000, 0.000000000000000000, 1.000000000000000000 ) ) ;
#4298=CIRCLE ( 'NONE', #5063, 82.00000000000000000 ) ;
#4305=ORIENTED_EDGE ( 'NONE', *, *, #17282, .T. ) ;
#4307=ORIENTED_EDGE ( 'NONE', *, *, #27409, .T. ) ;
#4308=CARTESIAN_POINT ( 'NONE',  ( 10.00000000000000000, 46.53671651293948486, 59.03961581697416250 ) ) ;
#4310=ORIENTED_EDGE ( 'NONE', *, *, #21274, .T. ) ;
#4317=ORIENTED_EDGE ( 'NONE', *, *, #8241, .F. ) ;
#4319=ORIENTED_EDGE ( 'NONE', *, *, #8783, .F. ) ;
#4321=EDGE_LOOP ( 'NONE', ( #26402, #38211, #36173, #32922 ) ) ;
#4323=AXIS2_PLACEMENT_3D ( 'NONE', #6190, #9852, #35072 ) ;
#4334=CYLINDRICAL_SURFACE ( 'NONE', #35533, 32.00000000000000000 ) ;
#4338=AXIS2_PLACEMENT_3D ( 'NONE', #24536, #21589, #17174 ) ;
#4339=ORIENTED_EDGE ( 'NONE', *, *, #24489, .F. ) ;
#4341=CARTESIAN_POINT ( 'NONE',  ( 10.00000000000000000, -41.76106447765533147, 62.50884508063410294 ) ) ;
#4347=AXIS2_PLACEMENT_3D ( 'NONE', #18850, #41391, #7613 ) ;
#4349=FACE_OUTER_BOUND ( 'NONE', #38065, .T. ) ;
#4353=EDGE_CURVE ( 'NONE', #2189, #18404, #42706, .T. ) ;
#4354=AXIS2_PLACEMENT_3D ( 'NONE', #47958, #47254, #13729 ) ;
#4355=SURFACE_STYLE_USAGE ( .BOTH. , #890 ) ;
#4366=CIRCLE ( 'NONE', #31742, 32.00000000000000000 ) ;
#4367=CYLINDRICAL_SURFACE ( 'NONE', #2284, 77.49899999999999523 ) ;
#4368=EDGE_CURVE ( 'NONE', #10399, #16188, #4417, .T. ) ;
#4370=CIRCLE ( 'NONE', #40328, 31.99999999999999289 ) ;
#4374=CYLINDRICAL_SURFACE ( 'NONE', #21014, 77.49899999999999523 ) ;
#4376=ORIENTED_EDGE ( 'NONE', *, *, #34726, .F. ) ;
#4377=CARTESIAN_POINT ( 'NONE',  ( 10.00000000000000000, 0.000000000000000000, 0.000000000000000000 ) ) ;
#4379=ORIENTED_EDGE ( 'NONE', *, *, #45938, .F. ) ;
#4383=FACE_OUTER_BOUND ( 'NONE', #42783, .T. ) ;
#4384=AXIS2_PLACEMENT_3D ( 'NONE', #39858, #9502, #43048 ) ;
#4386=EDGE_CURVE ( 'NONE', #15128, #16057, #10669, .T. ) ;
#4387=CYLINDRICAL_SURFACE ( 'NONE', #29135, 32.00000000000000000 ) ;
#4392=ORIENTED_EDGE ( 'NONE', *, *, #32506, .T. ) ;
#4399=CARTESIAN_POINT ( 'NONE',  ( 0.000000000000000000, -81.50828551894220197, -8.966570791701583332 ) ) ;
#4407=LINE ( 'NONE', #29845, #17685 ) ;
#4415=VECTOR ( 'NONE', #5416, 1000.000000000000000 ) ;
#4417=CIRCLE ( 'NONE', #495, 77.49900000000002365 ) ;
#4419=VERTEX_POINT ( 'NONE', #14726 ) ;
#4420=ADVANCED_FACE ( 'NONE', ( #8093 ), #18626, .T. ) ;
#4421=AXIS2_PLACEMENT_3D ( 'NONE', #5126, #31318, #27898 ) ;
#4424=LINE ( 'NONE', #34490, #25786 ) ;
#4444=FACE_OUTER_BOUND ( 'NONE', #6653, .T. ) ;
#4448=CARTESIAN_POINT ( 'NONE',  ( 10.00000000000000000, -20.41045688087876897, 72.35160999960810102 ) ) ;
#4451=DIRECTION ( 'NONE',  ( 1.000000000000000000, -0.000000000000000000, -0.000000000000000000 ) ) ;
#4459=VECTOR ( 'NONE', #11922, 1000.000000000000000 ) ;
#4469=VECTOR ( 'NONE', #821, 1000.000000000000000 ) ;
#4470=CIRCLE ( 'NONE', #9907, 82.00000000000000000 ) ;
#4476=DIRECTION ( 'NONE',  ( -1.000000000000000000, 0.000000000000000000, -0.000000000000000000 ) ) ;
#4478=AXIS2_PLACEMENT_3D ( 'NONE', #15766, #18932, #18701 ) ;
#4479=CARTESIAN_POINT ( 'NONE',  ( 5.000000000000000000, -79.10210256391353312, -21.60688246758668640 ) ) ;
#4480=ADVANCED_FACE ( 'NONE', ( #27931 ), #42846, .T. ) ;
#4483=AXIS2_PLACEMENT_3D ( 'NONE', #4814, #39307, #19719 ) ;
#4489=DIRECTION ( 'NONE',  ( 0.000000000000000000, 0.000000000000000000, -1.000000000000000000 ) ) ;
#4491=EDGE_CURVE ( 'NONE', #15455, #27599, #7140, .T. ) ;
#4496=DIRECTION ( 'NONE',  ( -1.000000000000000000, 0.000000000000000000, -0.000000000000000000 ) ) ;
#4502=DIRECTION ( 'NONE',  ( 0.000000000000000000, 0.000000000000000000, 1.000000000000000000 ) ) ;
#4504=DIRECTION ( 'NONE',  ( 0.000000000000000000, 0.4539904997395476927, -0.8910065241883674547 ) ) ;
#4518=DIRECTION ( 'NONE',  ( -1.000000000000000000, 0.000000000000000000, 0.000000000000000000 ) ) ;
#4523=DIRECTION ( 'NONE',  ( -1.000000000000000000, -0.000000000000000000, -0.000000000000000000 ) ) ;
#4525=CARTESIAN_POINT ( 'NONE',  ( 10.00000000000000000, 71.87247863392470038, -39.47590169984768238 ) ) ;
#4529=ORIENTED_EDGE ( 'NONE', *, *, #44797, .T. ) ;
#4549=ORIENTED_EDGE ( 'NONE', *, *, #18417, .F. ) ;
#4551=DIRECTION ( 'NONE',  ( -1.000000000000000000, 0.000000000000000000, 0.000000000000000000 ) ) ;
#4552=ORIENTED_EDGE ( 'NONE', *, *, #30873, .T. ) ;
#4553=DIRECTION ( 'NONE',  ( -1.000000000000000000, -0.000000000000000000, 0.000000000000000000 ) ) ;
#4559=DIRECTION ( 'NONE',  ( -1.000000000000000000, 0.000000000000000000, 0.000000000000000000 ) ) ;
#4561=DIRECTION ( 'NONE',  ( -1.000000000000000000, 0.000000000000000000, 0.000000000000000000 ) ) ;
#4569=DIRECTION ( 'NONE',  ( -1.000000000000000000, -0.000000000000000000, 0.000000000000000000 ) ) ;
#4570=CARTESIAN_POINT ( 'NONE',  ( 0.000000000000000000, 36.73666225445988687, -65.58780272294035285 ) ) ;
#4572=EDGE_CURVE ( 'NONE', #10514, #15128, #17600, .T. ) ;
#4582=VERTEX_POINT ( 'NONE', #47466 ) ;
#4584=ORIENTED_EDGE ( 'NONE', *, *, #32230, .F. ) ;
#4588=EDGE_CURVE ( 'NONE', #31998, #21026, #35732, .T. ) ;
#4593=CIRCLE ( 'NONE', #14771, 31.99999999999998579 ) ;
#4595=EDGE_CURVE ( 'NONE', #15919, #13689, #39189, .T. ) ;
#4602=ORIENTED_EDGE ( 'NONE', *, *, #33734, .F. ) ;
#4608=ORIENTED_EDGE ( 'NONE', *, *, #37578, .T. ) ;
#4614=CYLINDRICAL_SURFACE ( 'NONE', #43073, 31.99999999999999289 ) ;
#4616=ORIENTED_EDGE ( 'NONE', *, *, #17064, .F. ) ;
#4617=FACE_OUTER_BOUND ( 'NONE', #9249, .T. ) ;
#4618=ORIENTED_EDGE ( 'NONE', *, *, #5634, .F. ) ;
#4619=CARTESIAN_POINT ( 'NONE',  ( 0.000000000000000000, 0.000000000000000000, 0.000000000000000000 ) ) ;
#4623=CARTESIAN_POINT ( 'NONE',  ( 0.000000000000000000, 54.21277698773752718, -55.38113227695725271 ) ) ;
#4625=CYLINDRICAL_SURFACE ( 'NONE', #35728, 32.00000000000000000 ) ;
#4627=AXIS2_PLACEMENT_3D ( 'NONE', #22949, #26871, #11696 ) ;
#4629=EDGE_LOOP ( 'NONE', ( #31717, #17587, #22411, #12628 ) ) ;
#4634=CIRCLE ( 'NONE', #32007, 77.49899999999999523 ) ;
#4638=CARTESIAN_POINT ( 'NONE',  ( 10.00000000000000000, 41.19522573413826194, -65.64334221924865176 ) ) ;
#4647=DIRECTION ( 'NONE',  ( -1.000000000000000000, 0.000000000000000000, 0.000000000000000000 ) ) ;
#4659=CARTESIAN_POINT ( 'NONE',  ( 0.000000000000000000, -55.38113227695820484, 54.21277698773656084 ) ) ;
#4662=ADVANCED_FACE ( 'NONE', ( #6596 ), #10022, .T. ) ;
#4665=ORIENTED_EDGE ( 'NONE', *, *, #41445, .F. ) ;
#4668=DIRECTION ( 'NONE',  ( 1.000000000000000000, 0.000000000000000000, 0.000000000000000000 ) ) ;
#4669=ORIENTED_EDGE ( 'NONE', *, *, #20115, .F. ) ;
#4671=ORIENTED_EDGE ( 'NONE', *, *, #42094, .F. ) ;
#4672=DIRECTION ( 'NONE',  ( 0.000000000000000000, 0.000000000000000000, 1.000000000000000000 ) ) ;
#4678=EDGE_LOOP ( 'NONE', ( #10562, #18332, #9865, #38379 ) ) ;
#4681=FACE_OUTER_BOUND ( 'NONE', #41157, .T. ) ;
#4693=DIRECTION ( 'NONE',  ( -1.000000000000000000, 0.000000000000000000, -0.000000000000000000 ) ) ;
#4694=FACE_OUTER_BOUND ( 'NONE', #26874, .T. ) ;
#4712=ADVANCED_FACE ( 'NONE', ( #11180 ), #12161, .T. ) ;
#4727=ORIENTED_EDGE ( 'NONE', *, *, #42945, .F. ) ;
#4729=DIRECTION ( 'NONE',  ( -1.000000000000000000, -0.000000000000000000, 0.000000000000000000 ) ) ;
#4732=CIRCLE ( 'NONE', #39924, 82.00000000000000000 ) ;
#4733=CARTESIAN_POINT ( 'NONE',  ( 10.00000000000000000, 75.54627589209943039, 17.28742895386112721 ) ) ;
#4737=CARTESIAN_POINT ( 'NONE',  ( 10.00000000000000000, 63.97538442413425486, 51.29473840253247374 ) ) ;
#4740=CARTESIAN_POINT ( 'NONE',  ( 5.000000000000000000, 44.99326035066149387, -68.55367621811095091 ) ) ;
#4742=CARTESIAN_POINT ( 'NONE',  ( 10.00000000000000000, 0.000000000000000000, 0.000000000000000000 ) ) ;
#4745=AXIS2_PLACEMENT_3D ( 'NONE', #5639, #1979, #16895 ) ;
#4748=CYLINDRICAL_SURFACE ( 'NONE', #26343, 77.49899999999999523 ) ;
#4752=EDGE_CURVE ( 'NONE', #38891, #4419, #45670, .T. ) ;
#4755=DIRECTION ( 'NONE',  ( -1.000000000000000000, 0.000000000000000000, -0.000000000000000000 ) ) ;
#4758=VERTEX_POINT ( 'NONE', #8463 ) ;
#4759=LINE ( 'NONE', #46125, #29928 ) ;
#4761=ORIENTED_EDGE ( 'NONE', *, *, #26148, .T. ) ;
#4764=AXIS2_PLACEMENT_3D ( 'NONE', #30315, #15610, #33722 ) ;
#4771=ORIENTED_EDGE ( 'NONE', *, *, #28519, .F. ) ;
#4776=DIRECTION ( 'NONE',  ( 0.000000000000000000, 0.000000000000000000, 1.000000000000000000 ) ) ;
#4777=AXIS2_PLACEMENT_3D ( 'NONE', #25179, #21528, #14906 ) ;
#4779=CARTESIAN_POINT ( 'NONE',  ( 0.000000000000000000, 0.000000000000000000, 0.000000000000000000 ) ) ;
#4782=ORIENTED_EDGE ( 'NONE', *, *, #30065, .F. ) ;
#4785=DIRECTION ( 'NONE',  ( 0.000000000000000000, 0.000000000000000000, 1.000000000000000000 ) ) ;
#4788=ORIENTED_EDGE ( 'NONE', *, *, #44015, .T. ) ;
#4797=CARTESIAN_POINT ( 'NONE',  ( 10.00000000000000000, -58.39081064771787766, 50.95692526931307498 ) ) ;
#4803=EDGE_LOOP ( 'NONE', ( #16943, #41206, #15984, #1822 ) ) ;
#4804=DIRECTION ( 'NONE',  ( 0.000000000000000000, -0.9876883405951359940, -0.1564344650402420822 ) ) ;
#4805=EDGE_CURVE ( 'NONE', #1310, #33968, #6381, .T. ) ;
#4806=DIRECTION ( 'NONE',  ( 0.000000000000000000, 0.8090169943749486725, -0.5877852522924713607 ) ) ;
#4807=CARTESIAN_POINT ( 'NONE',  ( 10.00000000000000000, 0.000000000000000000, 0.000000000000000000 ) ) ;
#4808=DIRECTION ( 'NONE',  ( 0.000000000000000000, 0.7604059656000276002, 0.6494480483301876550 ) ) ;
#4810=EDGE_CURVE ( 'NONE', #31737, #747, #25122, .T. ) ;
#4814=CARTESIAN_POINT ( 'NONE',  ( 0.000000000000000000, 0.000000000000000000, 0.000000000000000000 ) ) ;
#4830=AXIS2_PLACEMENT_3D ( 'NONE', #34401, #44966, #41068 ) ;
#4831=EDGE_CURVE ( 'NONE', #28609, #18434, #20202, .T. ) ;
#4832=CARTESIAN_POINT ( 'NONE',  ( 10.00000000000000000, 39.47590169984845687, 71.87247863392427405 ) ) ;
#4847=ORIENTED_EDGE ( 'NONE', *, *, #29512, .F. ) ;
#4852=DIRECTION ( 'NONE',  ( 0.000000000000000000, 0.000000000000000000, -1.000000000000000000 ) ) ;
#4853=DIRECTION ( 'NONE',  ( -1.000000000000000000, 0.000000000000000000, 0.000000000000000000 ) ) ;
#4858=CARTESIAN_POINT ( 'NONE',  ( 10.00000000000000000, -14.66109333815410487, -73.73191006444587003 ) ) ;
#4861=FACE_OUTER_BOUND ( 'NONE', #35950, .T. ) ;
#4866=CARTESIAN_POINT ( 'NONE',  ( 10.00000000000000000, 0.000000000000000000, 0.000000000000000000 ) ) ;
#4872=DIRECTION ( 'NONE',  ( -1.000000000000000000, 0.000000000000000000, 0.000000000000000000 ) ) ;
#4874=ADVANCED_FACE ( 'NONE', ( #5040 ), #16536, .T. ) ;
#4877=AXIS2_PLACEMENT_3D ( 'NONE', #30950, #1321, #12576 ) ;
#4881=DIRECTION ( 'NONE',  ( 0.000000000000000000, 0.000000000000000000, -1.000000000000000000 ) ) ;
#4885=DIRECTION ( 'NONE',  ( 0.000000000000000000, 0.2334453638559058908, -0.9723699203976764460 ) ) ;
#4888=ORIENTED_EDGE ( 'NONE', *, *, #19613, .T. ) ;
#4892=DIRECTION ( 'NONE',  ( -1.000000000000000000, -0.000000000000000000, 0.000000000000000000 ) ) ;
#4893=ORIENTED_EDGE ( 'NONE', *, *, #9828, .T. ) ;
#4895=ORIENTED_EDGE ( 'NONE', *, *, #41729, .F. ) ;
#4901=ORIENTED_EDGE ( 'NONE', *, *, #12488, .T. ) ;
#4904=DIRECTION ( 'NONE',  ( 0.000000000000000000, 0.000000000000000000, 1.000000000000000000 ) ) ;
#4911=VERTEX_POINT ( 'NONE', #6018 ) ;
#4914=CYLINDRICAL_SURFACE ( 'NONE', #33220, 31.99999999999999289 ) ;
#4916=CYLINDRICAL_SURFACE ( 'NONE', #44094, 77.49899999999999523 ) ;
#4918=DIRECTION ( 'NONE',  ( 0.000000000000000000, 0.000000000000000000, 1.000000000000000000 ) ) ;
#4921=CARTESIAN_POINT ( 'NONE',  ( 10.00000000000000000, -77.19088730480518734, -6.903761155838607166 ) ) ;
#4927=EDGE_CURVE ( 'NONE', #45521, #32527, #31966, .T. ) ;
#4930=DIRECTION ( 'NONE',  ( -1.000000000000000000, 0.000000000000000000, -0.000000000000000000 ) ) ;
#4932=CIRCLE ( 'NONE', #18954, 31.99999999999999645 ) ;
#4937=CARTESIAN_POINT ( 'NONE',  ( 0.000000000000000000, 0.000000000000000000, 0.000000000000000000 ) ) ;
#4939=LINE ( 'NONE', #19858, #31541 ) ;
#4949=LINE ( 'NONE', #34802, #21478 ) ;
#4970=VERTEX_POINT ( 'NONE', #42237 ) ;
#4974=ORIENTED_EDGE ( 'NONE', *, *, #8970, .T. ) ;
#4981=DIRECTION ( 'NONE',  ( 0.000000000000000000, 0.8526401643540935105, -0.5224985647159468005 ) ) ;
#4984=DIRECTION ( 'NONE',  ( 0.000000000000000000, 0.9723699203976773342, -0.2334453638559025601 ) ) ;
#4986=DIRECTION ( 'NONE',  ( 0.000000000000000000, 0.9238795325112877377, -0.3826834323650873948 ) ) ;
#4987=VECTOR ( 'NONE', #40639, 1000.000000000000000 ) ;
#4992=CIRCLE ( 'NONE', #7316, 31.99999999999999645 ) ;
#4993=AXIS2_PLACEMENT_3D ( 'NONE', #35714, #5373, #9510 ) ;
#4999=CARTESIAN_POINT ( 'NONE',  ( 10.00000000000000000, 28.89263327155850902, -71.91182617369157981 ) ) ;
#5008=AXIS2_PLACEMENT_3D ( 'NONE', #1371, #43203, #34890 ) ;
#5011=ORIENTED_EDGE ( 'NONE', *, *, #2529, .F. ) ;
#5012=ADVANCED_FACE ( 'NONE', ( #29238 ), #40733, .T. ) ;
#5013=AXIS2_PLACEMENT_3D ( 'NONE', #5326, #8988, #3687 ) ;
#5016=AXIS2_PLACEMENT_3D ( 'NONE', #23456, #27387, #42565 ) ;
#5017=CARTESIAN_POINT ( 'NONE',  ( 0.000000000000000000, 0.000000000000000000, 0.000000000000000000 ) ) ;
#5023=DIRECTION ( 'NONE',  ( -1.000000000000000000, 0.000000000000000000, 0.000000000000000000 ) ) ;
#5025=ORIENTED_EDGE ( 'NONE', *, *, #11406, .T. ) ;
#5026=CIRCLE ( 'NONE', #7411, 31.99999999999999289 ) ;
#5032=EDGE_LOOP ( 'NONE', ( #37984, #28347, #22364, #39508 ) ) ;
#5038=FACE_OUTER_BOUND ( 'NONE', #46261, .T. ) ;
#5040=FACE_OUTER_BOUND ( 'NONE', #10690, .T. ) ;
#5041=DIRECTION ( 'NONE',  ( 1.000000000000000000, -0.000000000000000000, -0.000000000000000000 ) ) ;
#5045=ADVANCED_FACE ( 'NONE', ( #29479 ), #44408, .T. ) ;
#5050=DIRECTION ( 'NONE',  ( -1.000000000000000000, 0.000000000000000000, 0.000000000000000000 ) ) ;
#5051=ORIENTED_EDGE ( 'NONE', *, *, #42354, .T. ) ;
#5054=AXIS2_PLACEMENT_3D ( 'NONE', #23589, #8186, #34355 ) ;
#5061=ADVANCED_FACE ( 'NONE', ( #32896 ), #6961, .T. ) ;
#5063=AXIS2_PLACEMENT_3D ( 'NONE', #15071, #10913, #30000 ) ;
#5071=CARTESIAN_POINT ( 'NONE',  ( 0.000000000000000000, 0.000000000000000000, 0.000000000000000000 ) ) ;
#5073=ORIENTED_EDGE ( 'NONE', *, *, #33269, .F. ) ;
#5074=VERTEX_POINT ( 'NONE', #36338 ) ;
#5075=ORIENTED_EDGE ( 'NONE', *, *, #20999, .F. ) ;
#5076=CARTESIAN_POINT ( 'NONE',  ( 0.000000000000000000, 44.99326035066051332, 68.55367621811160461 ) ) ;
#5077=ORIENTED_EDGE ( 'NONE', *, *, #23805, .F. ) ;
#5078=EDGE_LOOP ( 'NONE', ( #33661, #5446, #16805, #18478 ) ) ;
#5080=CARTESIAN_POINT ( 'NONE',  ( 5.000000000000002665, -74.18225833017864090, -34.94270380257719211 ) ) ;
#5083=EDGE_CURVE ( 'NONE', #24941, #45907, #47584, .T. ) ;
#5092=CIRCLE ( 'NONE', #33215, 77.49899999999999523 ) ;
#5098=ORIENTED_EDGE ( 'NONE', *, *, #19485, .T. ) ;
#5102=AXIS2_PLACEMENT_3D ( 'NONE', #44522, #25915, #6846 ) ;
#5109=ORIENTED_EDGE ( 'NONE', *, *, #7633, .T. ) ;
#5111=CARTESIAN_POINT ( 'NONE',  ( -10.00000000000000000, 0.000000000000000000, 0.000000000000000000 ) ) ;
#5117=CARTESIAN_POINT ( 'NONE',  ( 10.00000000000000000, -8.840884882375609877, 74.65374052328647281 ) ) ;
#5122=CARTESIAN_POINT ( 'NONE',  ( 0.000000000000000000, -77.19088730480528682, 6.903761155837488062 ) ) ;
#5125=CIRCLE ( 'NONE', #3535, 31.99999999999999289 ) ;
#5126=CARTESIAN_POINT ( 'NONE',  ( 0.000000000000000000, 0.000000000000000000, 0.000000000000000000 ) ) ;
#5130=ORIENTED_EDGE ( 'NONE', *, *, #14237, .F. ) ;
#5131=EDGE_CURVE ( 'NONE', #12683, #2237, #10178, .T. ) ;
#5132=CIRCLE ( 'NONE', #48095, 82.00000000000000000 ) ;
#5133=AXIS2_PLACEMENT_3D ( 'NONE', #3204, #39722, #40439 ) ;
#5145=EDGE_CURVE ( 'NONE', #29746, #24346, #22687, .T. ) ;
#5146=ORIENTED_EDGE ( 'NONE', *, *, #4752, .F. ) ;
#5148=ORIENTED_EDGE ( 'NONE', *, *, #24466, .T. ) ;
#5153=AXIS2_PLACEMENT_3D ( 'NONE', #7400, #34, #14989 ) ;
#5154=ADVANCED_FACE ( 'NONE', ( #15753 ), #3769, .F. ) ;
#5155=LINE ( 'NONE', #23732, #13330 ) ;
#5158=EDGE_CURVE ( 'NONE', #2670, #23364, #20340, .T. ) ;
#5159=EDGE_LOOP ( 'NONE', ( #22640, #32058, #29030, #23564 ) ) ;
#5168=AXIS2_PLACEMENT_3D ( 'NONE', #20297, #34262, #41878 ) ;
#5169=ORIENTED_EDGE ( 'NONE', *, *, #18937, .T. ) ;
#5185=DIRECTION ( 'NONE',  ( 0.000000000000000000, -0.5877852522924625900, -0.8090169943749551118 ) ) ;
#5187=DIRECTION ( 'NONE',  ( -1.000000000000000000, 0.000000000000000000, 0.000000000000000000 ) ) ;
#5191=VECTOR ( 'NONE', #28200, 1000.000000000000000 ) ;
#5192=CARTESIAN_POINT ( 'NONE',  ( 5.000000000000002665, 76.69515212746016175, 29.01471420065591289 ) ) ;
#5193=ORIENTED_EDGE ( 'NONE', *, *, #41737, .F. ) ;
#5195=AXIS2_PLACEMENT_3D ( 'NONE', #16145, #34968, #2171 ) ;
#5196=EDGE_CURVE ( 'NONE', #34190, #6985, #21907, .T. ) ;
#5197=CARTESIAN_POINT ( 'NONE',  ( 10.00000000000000000, -73.44644590900043113, -24.73286445877782924 ) ) ;
#5202=CIRCLE ( 'NONE', #15374, 31.99999999999999645 ) ;
#5204=ORIENTED_EDGE ( 'NONE', *, *, #10719, .T. ) ;
#5208=CARTESIAN_POINT ( 'NONE',  ( 5.000000000000002665, -81.34940948281344220, 10.30890764327356557 ) ) ;
#5212=ORIENTED_EDGE ( 'NONE', *, *, #2759, .F. ) ;
#5219=VERTEX_POINT ( 'NONE', #19182 ) ;
#5226=DIRECTION ( 'NONE',  ( 0.000000000000000000, 0.6494480483301848794, -0.7604059656000299317 ) ) ;
#5227=ORIENTED_EDGE ( 'NONE', *, *, #31435, .F. ) ;
#5230=ORIENTED_EDGE ( 'NONE', *, *, #18944, .F. ) ;
#5247=DIRECTION ( 'NONE',  ( 0.000000000000000000, -6.938893903907228378E-15, 1.000000000000000000 ) ) ;
#5253=ORIENTED_EDGE ( 'NONE', *, *, #45217, .F. ) ;
#5258=DIRECTION ( 'NONE',  ( -1.000000000000000000, -0.000000000000000000, 0.000000000000000000 ) ) ;
#5261=ORIENTED_EDGE ( 'NONE', *, *, #20374, .F. ) ;
#5270=CARTESIAN_POINT ( 'NONE',  ( 10.00000000000000000, -74.74816331893453025, 33.71516098798714722 ) ) ;
#5278=CARTESIAN_POINT ( 'NONE',  ( 10.00000000000000000, -51.03279382321048985, -55.19960302592120627 ) ) ;
#5279=ORIENTED_EDGE ( 'NONE', *, *, #48082, .F. ) ;
#5283=EDGE_LOOP ( 'NONE', ( #10288, #44873, #35700, #38505 ) ) ;
#5284=CARTESIAN_POINT ( 'NONE',  ( 0.000000000000000000, -63.97538442413390669, -51.29473840253292849 ) ) ;
#5288=DIRECTION ( 'NONE',  ( -1.000000000000000000, 0.000000000000000000, -0.000000000000000000 ) ) ;
#5290=CYLINDRICAL_SURFACE ( 'NONE', #39297, 77.49899999999999523 ) ;
#5292=DIRECTION ( 'NONE',  ( -1.000000000000000000, -0.000000000000000000, 0.000000000000000000 ) ) ;
#5293=CARTESIAN_POINT ( 'NONE',  ( 0.000000000000000000, 0.000000000000000000, 2.500000000000000000 ) ) ;
#5294=AXIS2_PLACEMENT_3D ( 'NONE', #15305, #4755, #24256 ) ;
#5296=CARTESIAN_POINT ( 'NONE',  ( 5.000000000000002665, -34.94270380257586339, -74.18225833017926618 ) ) ;
#5297=ORIENTED_EDGE ( 'NONE', *, *, #36242, .T. ) ;
#5298=CARTESIAN_POINT ( 'NONE',  ( 0.000000000000000000, -56.15606465354917276, -59.75363087400133111 ) ) ;
#5300=DIRECTION ( 'NONE',  ( -1.000000000000000000, 0.000000000000000000, 0.000000000000000000 ) ) ;
#5303=DIRECTION ( 'NONE',  ( -1.000000000000000000, 0.000000000000000000, 0.000000000000000000 ) ) ;
#5304=VECTOR ( 'NONE', #2257, 1000.000000000000000 ) ;
#5305=ORIENTED_EDGE ( 'NONE', *, *, #16689, .T. ) ;
#5315=DIRECTION ( 'NONE',  ( -1.000000000000000000, 0.000000000000000000, -0.000000000000000000 ) ) ;
#5319=LINE ( 'NONE', #5805, #28868 ) ;
#5326=CARTESIAN_POINT ( 'NONE',  ( 50.00005079999999680, 0.000000000000000000, 0.000000000000000000 ) ) ;
#5337=ORIENTED_EDGE ( 'NONE', *, *, #47705, .F. ) ;
#5338=ORIENTED_EDGE ( 'NONE', *, *, #24427, .F. ) ;
#5342=VECTOR ( 'NONE', #32094, 1000.000000000000000 ) ;
#5349=CARTESIAN_POINT ( 'NONE',  ( 0.000000000000000000, 17.28742895386190526, -75.54627589209924565 ) ) ;
#5352=CARTESIAN_POINT ( 'NONE',  ( 10.00000000000000000, -75.54627589209931671, -17.28742895386164591 ) ) ;
#5354=DIRECTION ( 'NONE',  ( 1.000000000000000000, -0.000000000000000000, -0.000000000000000000 ) ) ;
#5356=CARTESIAN_POINT ( 'NONE',  ( 10.00000000000000000, 54.21277698773752718, -55.38113227695725271 ) ) ;
#5364=DIRECTION ( 'NONE',  ( 1.000000000000000000, -0.000000000000000000, -0.000000000000000000 ) ) ;
#5365=EDGE_CURVE ( 'NONE', #33821, #43969, #9137, .T. ) ;
#5370=CIRCLE ( 'NONE', #25679, 31.99999999999999289 ) ;
#5373=DIRECTION ( 'NONE',  ( -1.000000000000000000, -0.000000000000000000, -0.000000000000000000 ) ) ;
#5376=EDGE_CURVE ( 'NONE', #30369, #46765, #24297, .T. ) ;
#5380=EDGE_LOOP ( 'NONE', ( #10296, #873, #43312, #42598 ) ) ;
#5385=DIRECTION ( 'NONE',  ( -1.000000000000000000, 0.000000000000000000, 0.000000000000000000 ) ) ;
#5387=FACE_OUTER_BOUND ( 'NONE', #33200, .T. ) ;
#5394=ORIENTED_EDGE ( 'NONE', *, *, #4491, .F. ) ;
#5397=DIRECTION ( 'NONE',  ( 0.000000000000000000, -0.07845909572783058006, -0.9969173337331290741 ) ) ;
#5399=VECTOR ( 'NONE', #20731, 1000.000000000000000 ) ;
#5408=AXIS2_PLACEMENT_3D ( 'NONE', #15824, #19250, #33689 ) ;
#5410=AXIS2_PLACEMENT_3D ( 'NONE', #3758, #15024, #26757 ) ;
#5412=DIRECTION ( 'NONE',  ( 1.000000000000000000, 0.000000000000000000, 0.000000000000000000 ) ) ;
#5415=CARTESIAN_POINT ( 'NONE',  ( 0.000000000000000000, 69.42325613327439271, 34.44570377933623462 ) ) ;
#5416=DIRECTION ( 'NONE',  ( 1.000000000000000000, -0.000000000000000000, -0.000000000000000000 ) ) ;
#5423=EDGE_CURVE ( 'NONE', #46450, #44447, #37571, .T. ) ;
#5441=CYLINDRICAL_SURFACE ( 'NONE', #26090, 31.99999999999999289 ) ;
#5443=CARTESIAN_POINT ( 'NONE',  ( 0.000000000000000000, -49.70050353004846500, -59.46389618802017907 ) ) ;
#5446=ORIENTED_EDGE ( 'NONE', *, *, #45510, .T. ) ;
#5448=DIRECTION ( 'NONE',  ( 1.000000000000000000, 0.000000000000000000, 0.000000000000000000 ) ) ;
#5449=CARTESIAN_POINT ( 'NONE',  ( 10.00000000000000000, 65.58780272294129077, -36.73666225445822420 ) ) ;
#5453=ORIENTED_EDGE ( 'NONE', *, *, #13441, .T. ) ;
#5456=ORIENTED_EDGE ( 'NONE', *, *, #2688, .F. ) ;
#5457=CARTESIAN_POINT ( 'NONE',  ( 0.000000000000000000, 33.71516098798740302, 74.74816331893443078 ) ) ;
#5464=CYLINDRICAL_SURFACE ( 'NONE', #7867, 77.49899999999999523 ) ;
#5466=EDGE_CURVE ( 'NONE', #9826, #17470, #2263, .T. ) ;
#5471=CARTESIAN_POINT ( 'NONE',  ( 5.000000000000002665, -71.87247863392443037, 39.47590169984818687 ) ) ;
#5476=DIRECTION ( 'NONE',  ( 0.000000000000000000, 0.000000000000000000, 1.000000000000000000 ) ) ;
#5478=EDGE_CURVE ( 'NONE', #17528, #36602, #6672, .T. ) ;
#5482=CARTESIAN_POINT ( 'NONE',  ( 0.000000000000000000, 65.58780272294129077, -36.73666225445822420 ) ) ;
#5490=DIRECTION ( 'NONE',  ( -1.000000000000000000, -0.000000000000000000, -0.000000000000000000 ) ) ;
#5499=AXIS2_PLACEMENT_3D ( 'NONE', #33620, #41231, #4504 ) ;
#5505=STYLED_ITEM ( 'NONE', ( #20352 ), #19734 ) ;
#5509=DIRECTION ( 'NONE',  ( -1.000000000000000000, 0.000000000000000000, 0.000000000000000000 ) ) ;
#5511=ORIENTED_EDGE ( 'NONE', *, *, #14044, .F. ) ;
#5512=CIRCLE ( 'NONE', #10995, 77.49899999999999523 ) ;
#5518=DIRECTION ( 'NONE',  ( -1.000000000000000000, 0.000000000000000000, -0.000000000000000000 ) ) ;
#5524=DIRECTION ( 'NONE',  ( -1.000000000000000000, 0.000000000000000000, -0.000000000000000000 ) ) ;
#5527=ORIENTED_EDGE ( 'NONE', *, *, #26749, .F. ) ;
#5531=EDGE_CURVE ( 'NONE', #6602, #828, #39149, .T. ) ;
#5532=CARTESIAN_POINT ( 'NONE',  ( 0.000000000000000000, -62.50884508063395373, -41.76106447765554464 ) ) ;
#5535=CIRCLE ( 'NONE', #18024, 31.99999999999999645 ) ;
#5543=EDGE_CURVE ( 'NONE', #16459, #10449, #17482, .T. ) ;
#5550=AXIS2_PLACEMENT_3D ( 'NONE', #24670, #27881, #35188 ) ;
#5555=LINE ( 'NONE', #5080, #18698 ) ;
#5557=ORIENTED_EDGE ( 'NONE', *, *, #46248, .T. ) ;
#5561=DIRECTION ( 'NONE',  ( -1.000000000000000000, 0.000000000000000000, 0.000000000000000000 ) ) ;
#5566=EDGE_CURVE ( 'NONE', #32691, #38387, #18244, .T. ) ;
#5575=CIRCLE ( 'NONE', #19627, 82.00000000000000000 ) ;
#5579=CYLINDRICAL_SURFACE ( 'NONE', #29138, 31.99999999999999289 ) ;
#5587=DIRECTION ( 'NONE',  ( 0.000000000000000000, 0.000000000000000000, 1.000000000000000000 ) ) ;
#5595=ORIENTED_EDGE ( 'NONE', *, *, #20225, .F. ) ;
#5596=CARTESIAN_POINT ( 'NONE',  ( 0.000000000000000000, 26.01480285779933510, -70.53064760720289428 ) ) ;
#5599=EDGE_CURVE ( 'NONE', #17528, #36949, #30779, .T. ) ;
#5602=VECTOR ( 'NONE', #24681, 1000.000000000000000 ) ;
#5603=VERTEX_POINT ( 'NONE', #7390 ) ;
#5607=CARTESIAN_POINT ( 'NONE',  ( -10.00000000000000000, 0.000000000000000000, 0.000000000000000000 ) ) ;
#5608=ADVANCED_FACE ( 'NONE', ( #37978 ), #37246, .T. ) ;
#5609=ORIENTED_EDGE ( 'NONE', *, *, #34361, .F. ) ;
#5610=CIRCLE ( 'NONE', #41555, 31.99999999999999289 ) ;
#5612=EDGE_LOOP ( 'NONE', ( #23396, #38233, #36485, #44859 ) ) ;
#5619=LINE ( 'NONE', #32287, #36654 ) ;
#5621=VERTEX_POINT ( 'NONE', #48263 ) ;
#5629=CARTESIAN_POINT ( 'NONE',  ( 10.00000000000000000, -69.42325613327415113, -34.44570377933673910 ) ) ;
#5630=EDGE_CURVE ( 'NONE', #40043, #43833, #14740, .T. ) ;
#5632=DIRECTION ( 'NONE',  ( 0.000000000000000000, 0.8090169943749486725, -0.5877852522924713607 ) ) ;
#5634=EDGE_CURVE ( 'NONE', #13603, #43495, #8899, .T. ) ;
#5638=AXIS2_PLACEMENT_3D ( 'NONE', #26547, #8181, #4285 ) ;
#5639=CARTESIAN_POINT ( 'NONE',  ( 10.00000000000000000, 0.000000000000000000, 0.000000000000000000 ) ) ;
#5640=DIRECTION ( 'NONE',  ( -1.000000000000000000, -0.000000000000000000, -0.000000000000000000 ) ) ;
#5642=VERTEX_POINT ( 'NONE', #44830 ) ;
#5655=DIRECTION ( 'NONE',  ( 0.000000000000000000, 0.000000000000000000, 1.000000000000000000 ) ) ;
#5656=CARTESIAN_POINT ( 'NONE',  ( 10.00000000000000000, 77.16300072079698680, -27.74655509720590274 ) ) ;
#5663=CYLINDRICAL_SURFACE ( 'NONE', #37419, 82.00000000000000000 ) ;
#5665=ORIENTED_EDGE ( 'NONE', *, *, #36527, .T. ) ;
#5667=ORIENTED_EDGE ( 'NONE', *, *, #11888, .F. ) ;
#5671=ORIENTED_EDGE ( 'NONE', *, *, #3924, .T. ) ;
#5681=FACE_OUTER_BOUND ( 'NONE', #28482, .T. ) ;
#5693=DIRECTION ( 'NONE',  ( -1.000000000000000000, 0.000000000000000000, 0.000000000000000000 ) ) ;
#5694=ORIENTED_EDGE ( 'NONE', *, *, #6574, .T. ) ;
#5696=DIRECTION ( 'NONE',  ( 0.000000000000000000, 0.000000000000000000, 1.000000000000000000 ) ) ;
#5701=CARTESIAN_POINT ( 'NONE',  ( 10.00000000000000000, -31.47745569255189224, 68.26794271651249346 ) ) ;
#5711=CARTESIAN_POINT ( 'NONE',  ( 0.000000000000000000, 10.30890764327501863, -81.34940948281325745 ) ) ;
#5713=AXIS2_PLACEMENT_3D ( 'NONE', #528, #26713, #20814 ) ;
#5714=CARTESIAN_POINT ( 'NONE',  ( 10.00000000000000000, 14.67089635893713684, 73.72996012237443608 ) ) ;
#5720=DIRECTION ( 'NONE',  ( -1.000000000000000000, -0.000000000000000000, 0.000000000000000000 ) ) ;
#5729=VECTOR ( 'NONE', #17453, 1000.000000000000000 ) ;
#5738=ORIENTED_EDGE ( 'NONE', *, *, #32337, .T. ) ;
#5754=DIRECTION ( 'NONE',  ( 1.000000000000000000, -0.000000000000000000, -0.000000000000000000 ) ) ;
#5755=FACE_OUTER_BOUND ( 'NONE', #35617, .T. ) ;
#5756=CIRCLE ( 'NONE', #2621, 82.00000000000000000 ) ;
#5758=ORIENTED_EDGE ( 'NONE', *, *, #29347, .T. ) ;
#5759=ORIENTED_EDGE ( 'NONE', *, *, #23600, .F. ) ;
#5762=ADVANCED_FACE ( 'NONE', ( #27446 ), #16194, .T. ) ;
#5766=CARTESIAN_POINT ( 'NONE',  ( 5.000000000000002665, 34.94270380257741948, -74.18225833017852722 ) ) ;
#5769=FACE_OUTER_BOUND ( 'NONE', #1633, .T. ) ;
#5779=FACE_OUTER_BOUND ( 'NONE', #5159, .T. ) ;
#5780=DIRECTION ( 'NONE',  ( 0.000000000000000000, 0.07845909572784529051, -0.9969173337331279638 ) ) ;
#5785=CIRCLE ( 'NONE', #17504, 31.99999999999999289 ) ;
#5786=CARTESIAN_POINT ( 'NONE',  ( 10.00000000000000000, 0.000000000000000000, 0.000000000000000000 ) ) ;
#5787=DIRECTION ( 'NONE',  ( 0.000000000000000000, 0.8090169943749446757, 0.5877852522924769119 ) ) ;
#5801=AXIS2_PLACEMENT_3D ( 'NONE', #44843, #3976, #34063 ) ;
#5805=CARTESIAN_POINT ( 'NONE',  ( 10.00000000000000000, 59.46389618801964616, 49.70050353004912580 ) ) ;
#5809=ADVANCED_FACE ( 'NONE', ( #4681 ), #35505, .T. ) ;
#5821=ORIENTED_EDGE ( 'NONE', *, *, #40835, .T. ) ;
#5830=CIRCLE ( 'NONE', #36312, 31.99999999999998579 ) ;
#5831=ADVANCED_FACE ( 'NONE', ( #8823 ), #38218, .T. ) ;
#5834=CIRCLE ( 'NONE', #1018, 31.99999999999999645 ) ;
#5838=FACE_OUTER_BOUND ( 'NONE', #27016, .T. ) ;
#5844=AXIS2_PLACEMENT_3D ( 'NONE', #31574, #46498, #1955 ) ;
#5855=DIRECTION ( 'NONE',  ( -1.000000000000000000, 0.000000000000000000, -0.000000000000000000 ) ) ;
#5858=ORIENTED_EDGE ( 'NONE', *, *, #39558, .F. ) ;
#5861=ADVANCED_FACE ( 'NONE', ( #39429 ), #47480, .T. ) ;
#5862=AXIS2_PLACEMENT_3D ( 'NONE', #3806, #46746, #47856 ) ;
#5876=AXIS2_PLACEMENT_3D ( 'NONE', #6731, #10396, #47589 ) ;
#5877=ADVANCED_FACE ( 'NONE', ( #6374 ), #21539, .T. ) ;
#5882=ORIENTED_EDGE ( 'NONE', *, *, #31157, .T. ) ;
#5884=CIRCLE ( 'NONE', #44200, 31.99999999999999289 ) ;
#5885=EDGE_CURVE ( 'NONE', #7382, #8218, #4992, .T. ) ;
#5887=CARTESIAN_POINT ( 'NONE',  ( 10.00000000000000000, -62.50329211542407393, -41.76937507738853839 ) ) ;
#5888=ORIENTED_EDGE ( 'NONE', *, *, #40747, .T. ) ;
#5905=VERTEX_POINT ( 'NONE', #44050 ) ;
#5907=VECTOR ( 'NONE', #22630, 1000.000000000000000 ) ;
#5911=CYLINDRICAL_SURFACE ( 'NONE', #9605, 82.00000000000000000 ) ;
#5917=CIRCLE ( 'NONE', #23899, 77.49899999999999523 ) ;
#5932=ORIENTED_EDGE ( 'NONE', *, *, #2688, .T. ) ;
#5952=ORIENTED_EDGE ( 'NONE', *, *, #22880, .T. ) ;
#5953=CYLINDRICAL_SURFACE ( 'NONE', #27002, 82.00000000000000000 ) ;
#5955=CARTESIAN_POINT ( 'NONE',  ( 0.000000000000000000, -81.90746397400393164, 3.894527615417586741 ) ) ;
#5959=CYLINDRICAL_SURFACE ( 'NONE', #4323, 31.99999999999999289 ) ;
#5960=AXIS2_PLACEMENT_3D ( 'NONE', #20572, #1999, #5185 ) ;
#5961=DIRECTION ( 'NONE',  ( -1.000000000000000000, 0.000000000000000000, 0.000000000000000000 ) ) ;
#5963=ORIENTED_EDGE ( 'NONE', *, *, #28703, .T. ) ;
#5964=DIRECTION ( 'NONE',  ( -1.000000000000000000, 0.000000000000000000, -0.000000000000000000 ) ) ;
#5967=DIRECTION ( 'NONE',  ( -1.000000000000000000, -0.000000000000000000, -0.000000000000000000 ) ) ;
#5984=CARTESIAN_POINT ( 'NONE',  ( 0.000000000000000000, -71.21200624218825226, 40.65526001592589722 ) ) ;
#5987=CARTESIAN_POINT ( 'NONE',  ( 10.00000000000000000, 0.000000000000000000, 0.000000000000000000 ) ) ;
#5989=ORIENTED_EDGE ( 'NONE', *, *, #18980, .F. ) ;
#6002=CARTESIAN_POINT ( 'NONE',  ( 0.000000000000000000, 21.60688246758696707, -79.10210256391346206 ) ) ;
#6011=VECTOR ( 'NONE', #7249, 1000.000000000000000 ) ;
#6018=CARTESIAN_POINT ( 'NONE',  ( 10.00000000000000000, 76.66974797899852945, -11.30684508768257679 ) ) ;
#6026=AXIS2_PLACEMENT_3D ( 'NONE', #29178, #29437, #43876 ) ;
#6040=CYLINDRICAL_SURFACE ( 'NONE', #36900, 31.99999999999999289 ) ;
#6045=VECTOR ( 'NONE', #4496, 1000.000000000000000 ) ;
#6047=EDGE_LOOP ( 'NONE', ( #23411, #40956, #17910, #45231 ) ) ;
#6060=CARTESIAN_POINT ( 'NONE',  ( 0.000000000000000000, -33.71516098798685590, -74.74816331893465815 ) ) ;
#6062=CIRCLE ( 'NONE', #20096, 31.99999999999999289 ) ;
#6064=CARTESIAN_POINT ( 'NONE',  ( 0.000000000000000000, 77.49459641780886443, 0.8261519478433866359 ) ) ;
#6065=ORIENTED_EDGE ( 'NONE', *, *, #1721, .F. ) ;
#6071=LINE ( 'NONE', #47169, #21775 ) ;
#6073=DIRECTION ( 'NONE',  ( 1.000000000000000000, 0.000000000000000000, -0.000000000000000000 ) ) ;
#6076=DIRECTION ( 'NONE',  ( -1.000000000000000000, -0.000000000000000000, 0.000000000000000000 ) ) ;
#6080=EDGE_LOOP ( 'NONE', ( #10535, #30872, #4258, #29737 ) ) ;
#6081=CARTESIAN_POINT ( 'NONE',  ( 10.00000000000000000, -39.47590169984896136, 71.87247863392398983 ) ) ;
#6083=CARTESIAN_POINT ( 'NONE',  ( 10.00000000000000000, 65.58780272294129077, -36.73666225445822420 ) ) ;
#6084=DIRECTION ( 'NONE',  ( 0.000000000000000000, 0.000000000000000000, 1.000000000000000000 ) ) ;
#6095=FACE_OUTER_BOUND ( 'NONE', #36393, .T. ) ;
#6098=EDGE_CURVE ( 'NONE', #38630, #13774, #30044, .T. ) ;
#6099=EDGE_LOOP ( 'NONE', ( #14607, #1835, #34984, #42576 ) ) ;
#6100=ORIENTED_EDGE ( 'NONE', *, *, #35931, .T. ) ;
#6105=DIRECTION ( 'NONE',  ( 0.000000000000000000, 0.000000000000000000, 1.000000000000000000 ) ) ;
#6107=ORIENTED_EDGE ( 'NONE', *, *, #41198, .F. ) ;
#6109=DIRECTION ( 'NONE',  ( 0.000000000000000000, -0.9238795325112906243, 0.3826834323650804004 ) ) ;
#6110=ORIENTED_EDGE ( 'NONE', *, *, #41387, .T. ) ;
#6113=CARTESIAN_POINT ( 'NONE',  ( 0.000000000000000000, 8.830959090342393125, 74.65491531819122883 ) ) ;
#6116=EDGE_LOOP ( 'NONE', ( #10696, #27103, #45299, #8951 ) ) ;
#6117=DIRECTION ( 'NONE',  ( -1.000000000000000000, 0.000000000000000000, 0.000000000000000000 ) ) ;
#6126=ORIENTED_EDGE ( 'NONE', *, *, #37923, .T. ) ;
#6130=ORIENTED_EDGE ( 'NONE', *, *, #41494, .T. ) ;
#6139=VECTOR ( 'NONE', #23208, 1000.000000000000000 ) ;
#6141=CARTESIAN_POINT ( 'NONE',  ( -10.00000000000000000, 0.000000000000000000, 0.000000000000000000 ) ) ;
#6143=EDGE_CURVE ( 'NONE', #34627, #31027, #43321, .T. ) ;
#6145=CIRCLE ( 'NONE', #18641, 77.49899999999999523 ) ;
#6151=ORIENTED_EDGE ( 'NONE', *, *, #1083, .F. ) ;
#6152=EDGE_CURVE ( 'NONE', #708, #42399, #38897, .T. ) ;
#6154=ADVANCED_FACE ( 'NONE', ( #19524 ), #9025, .T. ) ;
#6164=ORIENTED_EDGE ( 'NONE', *, *, #23312, .T. ) ;
#6166=ORIENTED_EDGE ( 'NONE', *, *, #19290, .T. ) ;
#6172=DIRECTION ( 'NONE',  ( -1.000000000000000000, 0.000000000000000000, 0.000000000000000000 ) ) ;
#6182=VERTEX_POINT ( 'NONE', #5356 ) ;
#6183=CARTESIAN_POINT ( 'NONE',  ( 0.000000000000000000, -39.78640506895652607, 66.50666863321986000 ) ) ;
#6190=CARTESIAN_POINT ( 'NONE',  ( 10.00000000000000000, -14.67089635893658794, -73.72996012237454977 ) ) ;
#6193=VERTEX_POINT ( 'NONE', #45489 ) ;
#6197=DIRECTION ( 'NONE',  ( 0.000000000000000000, 0.1564344650402312020, -0.9876883405951376593 ) ) ;
#6198=CARTESIAN_POINT ( 'NONE',  ( 10.00000000000000000, 77.19088730480524418, 6.903761155838049390 ) ) ;
#6201=DIRECTION ( 'NONE',  ( 0.000000000000000000, 0.000000000000000000, 1.000000000000000000 ) ) ;
#6206=CARTESIAN_POINT ( 'NONE',  ( 10.00000000000000000, -63.97538442413389248, -51.29473840253292138 ) ) ;
#6209=EDGE_CURVE ( 'NONE', #13885, #5905, #19857, .T. ) ;
#6214=DIRECTION ( 'NONE',  ( -1.000000000000000000, 0.000000000000000000, 0.000000000000000000 ) ) ;
#6219=DIRECTION ( 'NONE',  ( 0.000000000000000000, 0.000000000000000000, -1.000000000000000000 ) ) ;
#6221=EDGE_CURVE ( 'NONE', #23379, #7626, #44886, .T. ) ;
#6223=DIRECTION ( 'NONE',  ( 0.000000000000000000, 0.000000000000000000, 1.000000000000000000 ) ) ;
#6226=ORIENTED_EDGE ( 'NONE', *, *, #14825, .T. ) ;
#6227=DIRECTION ( 'NONE',  ( -1.000000000000000000, -0.000000000000000000, 0.000000000000000000 ) ) ;
#6230=DIRECTION ( 'NONE',  ( -1.000000000000000000, 0.000000000000000000, 0.000000000000000000 ) ) ;
#6233=EDGE_LOOP ( 'NONE', ( #31527, #32537, #36133, #16754 ) ) ;
#6241=VECTOR ( 'NONE', #22418, 1000.000000000000000 ) ;
#6247=LINE ( 'NONE', #5766, #8190 ) ;
#6250=LINE ( 'NONE', #39289, #29214 ) ;
#6257=DIRECTION ( 'NONE',  ( 1.000000000000000000, 0.000000000000000000, 0.000000000000000000 ) ) ;
#6258=VERTEX_POINT ( 'NONE', #21480 ) ;
#6262=DIRECTION ( 'NONE',  ( 0.000000000000000000, 0.000000000000000000, 1.000000000000000000 ) ) ;
#6265=DIRECTION ( 'NONE',  ( -1.000000000000000000, -0.000000000000000000, -0.000000000000000000 ) ) ;
#6268=EDGE_CURVE ( 'NONE', #21081, #39544, #12096, .T. ) ;
#6271=FACE_OUTER_BOUND ( 'NONE', #6080, .T. ) ;
#6272=ORIENTED_EDGE ( 'NONE', *, *, #24466, .F. ) ;
#6282=( GEOMETRIC_REPRESENTATION_CONTEXT ( 3 ) GLOBAL_UNCERTAINTY_ASSIGNED_CONTEXT ( ( #37936 ) ) GLOBAL_UNIT_ASSIGNED_CONTEXT ( ( #9344, #42651, #9110 ) ) REPRESENTATION_CONTEXT ( 'NONE', 'WORKASPACE' ) );
#6283=AXIS2_PLACEMENT_3D ( 'NONE', #12624, #27554, #32895 ) ;
#6294=DIRECTION ( 'NONE',  ( -1.000000000000000000, 0.000000000000000000, 0.000000000000000000 ) ) ;
#6300=DIRECTION ( 'NONE',  ( -1.000000000000000000, 0.000000000000000000, 0.000000000000000000 ) ) ;
#6303=EDGE_CURVE ( 'NONE', #2489, #2128, #13178, .T. ) ;
#6313=VERTEX_POINT ( 'NONE', #10216 ) ;
#6320=AXIS2_PLACEMENT_3D ( 'NONE', #23506, #8342, #42119 ) ;
#6323=DIRECTION ( 'NONE',  ( 1.000000000000000000, -0.000000000000000000, 0.000000000000000000 ) ) ;
#6328=EDGE_CURVE ( 'NONE', #28147, #13467, #26935, .T. ) ;
#6333=EDGE_CURVE ( 'NONE', #40761, #32236, #42588, .T. ) ;
#6341=LINE ( 'NONE', #29082, #35887 ) ;
#6345=ORIENTED_EDGE ( 'NONE', *, *, #32887, .F. ) ;
#6349=CARTESIAN_POINT ( 'NONE',  ( -10.00000000000000000, 0.000000000000000000, 0.000000000000000000 ) ) ;
#6357=CARTESIAN_POINT ( 'NONE',  ( 5.000000000000000000, -51.29473840253177741, -63.97538442413482329 ) ) ;
#6374=FACE_OUTER_BOUND ( 'NONE', #40652, .T. ) ;
#6378=VECTOR ( 'NONE', #26092, 1000.000000000000000 ) ;
#6379=LINE ( 'NONE', #14688, #36440 ) ;
#6381=CIRCLE ( 'NONE', #33717, 12.50000000000000000 ) ;
#6387=DIRECTION ( 'NONE',  ( -1.000000000000000000, -0.000000000000000000, -0.000000000000000000 ) ) ;
#6391=DIRECTION ( 'NONE',  ( 1.000000000000000000, 0.000000000000000000, 0.000000000000000000 ) ) ;
#6394=EDGE_CURVE ( 'NONE', #47670, #25818, #27746, .T. ) ;
#6399=DIRECTION ( 'NONE',  ( 0.000000000000000000, 0.000000000000000000, 1.000000000000000000 ) ) ;
#6402=ORIENTED_EDGE ( 'NONE', *, *, #13836, .F. ) ;
#6406=CARTESIAN_POINT ( 'NONE',  ( 0.000000000000000000, 8.966570791700698706, 81.50828551894228724 ) ) ;
#6408=VERTEX_POINT ( 'NONE', #40804 ) ;
#6412=AXIS2_PLACEMENT_3D ( 'NONE', #4025, #18928, #41470 ) ;
#6417=DIRECTION ( 'NONE',  ( 0.000000000000000000, 0.3826834323650907810, -0.9238795325112864054 ) ) ;
#6426=DIRECTION ( 'NONE',  ( -1.000000000000000000, -0.000000000000000000, 0.000000000000000000 ) ) ;
#6429=CARTESIAN_POINT ( 'NONE',  ( 10.00000000000000000, -55.38113227695820484, 54.21277698773656084 ) ) ;
#6438=DIRECTION ( 'NONE',  ( 1.000000000000000000, 0.000000000000000000, 0.000000000000000000 ) ) ;
#6440=ADVANCED_FACE ( 'NONE', ( #37615 ), #4091, .T. ) ;
#6446=ORIENTED_EDGE ( 'NONE', *, *, #13047, .T. ) ;
#6460=CARTESIAN_POINT ( 'NONE',  ( 0.000000000000000000, -55.19960302592104284, 51.03279382321070301 ) ) ;
#6468=EDGE_CURVE ( 'NONE', #12529, #20404, #17555, .T. ) ;
#6476=ORIENTED_EDGE ( 'NONE', *, *, #13604, .T. ) ;
#6477=VERTEX_POINT ( 'NONE', #48147 ) ;
#6478=CIRCLE ( 'NONE', #1805, 77.49900000000000944 ) ;
#6481=AXIS2_PLACEMENT_3D ( 'NONE', #23442, #41823, #4852 ) ;
#6497=CARTESIAN_POINT ( 'NONE',  ( 0.000000000000000000, -74.18225833017864090, -34.94270380257719211 ) ) ;
#6499=DIRECTION ( 'NONE',  ( 0.000000000000000000, 0.5877852522924685852, 0.8090169943749507819 ) ) ;
#6501=LINE ( 'NONE', #47389, #32455 ) ;
#6507=EDGE_CURVE ( 'NONE', #46808, #34289, #29547, .T. ) ;
#6509=CIRCLE ( 'NONE', #21355, 77.49900000000000944 ) ;
#6519=CYLINDRICAL_SURFACE ( 'NONE', #29678, 82.00000000000000000 ) ;
#6520=EDGE_CURVE ( 'NONE', #44447, #37633, #6625, .T. ) ;
#6523=VERTEX_POINT ( 'NONE', #2277 ) ;
#6532=DIRECTION ( 'NONE',  ( 0.000000000000000000, 0.000000000000000000, 1.000000000000000000 ) ) ;
#6537=DIRECTION ( 'NONE',  ( -1.000000000000000000, 0.000000000000000000, 0.000000000000000000 ) ) ;
#6539=EDGE_LOOP ( 'NONE', ( #35893, #31986, #26321, #29072 ) ) ;
#6554=DIRECTION ( 'NONE',  ( 0.000000000000000000, 0.000000000000000000, 1.000000000000000000 ) ) ;
#6555=CARTESIAN_POINT ( 'NONE',  ( 0.000000000000000000, -77.49459641780886443, 0.8261519478428377417 ) ) ;
#6563=CARTESIAN_POINT ( 'NONE',  ( 10.00000000000000000, 74.65491531819118620, -8.830959090342659579 ) ) ;
#6567=ORIENTED_EDGE ( 'NONE', *, *, #43111, .T. ) ;
#6572=EDGE_CURVE ( 'NONE', #5905, #22595, #31634, .T. ) ;
#6574=EDGE_CURVE ( 'NONE', #1101, #9926, #37870, .T. ) ;
#6581=AXIS2_PLACEMENT_3D ( 'NONE', #32820, #35787, #17171 ) ;
#6584=CIRCLE ( 'NONE', #9729, 82.00000000000000000 ) ;
#6590=CARTESIAN_POINT ( 'NONE',  ( 10.00000000000000000, -46.53671651293991118, 59.03961581697383565 ) ) ;
#6596=FACE_OUTER_BOUND ( 'NONE', #19497, .T. ) ;
#6602=VERTEX_POINT ( 'NONE', #45437 ) ;
#6609=DIRECTION ( 'NONE',  ( 0.000000000000000000, 0.000000000000000000, 1.000000000000000000 ) ) ;
#6610=DIRECTION ( 'NONE',  ( 0.000000000000000000, -0.8090169943749532244, 0.5877852522924652545 ) ) ;
#6615=CIRCLE ( 'NONE', #29295, 82.00000000000000000 ) ;
#6617=DIRECTION ( 'NONE',  ( -1.000000000000000000, -0.000000000000000000, 0.000000000000000000 ) ) ;
#6619=DIRECTION ( 'NONE',  ( 0.000000000000000000, 0.000000000000000000, 1.000000000000000000 ) ) ;
#6625=CIRCLE ( 'NONE', #25380, 32.00000000000000000 ) ;
#6628=AXIS2_PLACEMENT_3D ( 'NONE', #47794, #28960, #37277 ) ;
#6630=AXIS2_PLACEMENT_3D ( 'NONE', #40445, #10584, #44347 ) ;
#6632=CARTESIAN_POINT ( 'NONE',  ( 0.000000000000000000, 68.67312586195046720, -35.91791733033402068 ) ) ;
#6635=EDGE_CURVE ( 'NONE', #24182, #45282, #1958, .T. ) ;
#6636=ORIENTED_EDGE ( 'NONE', *, *, #606, .F. ) ;
#6638=APPLICATION_CONTEXT ( 'automotive_design' ) ;
#6641=DIRECTION ( 'NONE',  ( 0.000000000000000000, -0.9876883405951394357, 0.1564344650402205716 ) ) ;
#6645=ORIENTED_EDGE ( 'NONE', *, *, #5131, .F. ) ;
#6649=VECTOR ( 'NONE', #19644, 1000.000000000000000 ) ;
#6650=CARTESIAN_POINT ( 'NONE',  ( 0.000000000000000000, -63.18004540533059554, 44.88180994100355292 ) ) ;
#6652=CARTESIAN_POINT ( 'NONE',  ( 0.000000000000000000, 0.000000000000000000, 0.000000000000000000 ) ) ;
#6653=EDGE_LOOP ( 'NONE', ( #1824, #10538, #17823, #16848 ) ) ;
#6654=CARTESIAN_POINT ( 'NONE',  ( 0.000000000000000000, -75.54627589209955829, 17.28742895386058009 ) ) ;
#6655=ORIENTED_EDGE ( 'NONE', *, *, #11804, .F. ) ;
#6658=CARTESIAN_POINT ( 'NONE',  ( 0.000000000000000000, 34.44570377933695227, -69.42325613327405165 ) ) ;
#6659=ADVANCED_FACE ( 'NONE', ( #22073 ), #18150, .T. ) ;
#6665=VERTEX_POINT ( 'NONE', #6206 ) ;
#6666=EDGE_LOOP ( 'NONE', ( #44708, #36141, #4847, #6100 ) ) ;
#6667=DIRECTION ( 'NONE',  ( -1.000000000000000000, -0.000000000000000000, 0.000000000000000000 ) ) ;
#6668=LINE ( 'NONE', #18398, #48061 ) ;
#6669=FACE_OUTER_BOUND ( 'NONE', #32545, .T. ) ;
#6672=LINE ( 'NONE', #44109, #43824 ) ;
#6682=CYLINDRICAL_SURFACE ( 'NONE', #25462, 31.99999999999999289 ) ;
#6684=FACE_OUTER_BOUND ( 'NONE', #16270, .T. ) ;
#6703=CIRCLE ( 'NONE', #32489, 31.99999999999999289 ) ;
#6704=VERTEX_POINT ( 'NONE', #3227 ) ;
#6706=AXIS2_PLACEMENT_3D ( 'NONE', #28922, #24068, #32605 ) ;
#6713=CIRCLE ( 'NONE', #13743, 31.99999999999999645 ) ;
#6719=VERTEX_POINT ( 'NONE', #9869 ) ;
#6723=CARTESIAN_POINT ( 'NONE',  ( 0.000000000000000000, 0.000000000000000000, 0.000000000000000000 ) ) ;
#6724=DIRECTION ( 'NONE',  ( -1.000000000000000000, 0.000000000000000000, 0.000000000000000000 ) ) ;
#6725=CARTESIAN_POINT ( 'NONE',  ( 0.000000000000000000, 0.000000000000000000, 0.000000000000000000 ) ) ;
#6731=CARTESIAN_POINT ( 'NONE',  ( 10.00000000000000000, -55.20638768913724448, -51.02545421589383068 ) ) ;
#6733=DIRECTION ( 'NONE',  ( -1.000000000000000000, 0.000000000000000000, 0.000000000000000000 ) ) ;
#6747=CARTESIAN_POINT ( 'NONE',  ( 0.000000000000000000, 75.11764819372142199, 2.946379043147685728 ) ) ;
#6757=EDGE_CURVE ( 'NONE', #31795, #27602, #34862, .T. ) ;
#6760=CARTESIAN_POINT ( 'NONE',  ( 10.00000000000000000, -14.67089635893658794, -73.72996012237454977 ) ) ;
#6762=ORIENTED_EDGE ( 'NONE', *, *, #44154, .T. ) ;
#6765=CARTESIAN_POINT ( 'NONE',  ( 0.000000000000000000, 81.96053171279902472, -2.543863470248670211 ) ) ;
#6766=CARTESIAN_POINT ( 'NONE',  ( 10.00000000000000000, -44.99326035066006568, -68.55367621811190304 ) ) ;
#6774=FACE_OUTER_BOUND ( 'NONE', #37147, .T. ) ;
#6775=DIRECTION ( 'NONE',  ( 0.000000000000000000, 0.9876883405951371042, 0.1564344650402346437 ) ) ;
#6783=CARTESIAN_POINT ( 'NONE',  ( 5.000000000000002665, 29.01471420065564644, 76.69515212746026123 ) ) ;
#6785=ORIENTED_EDGE ( 'NONE', *, *, #33364, .F. ) ;
#6791=CARTESIAN_POINT ( 'NONE',  ( 0.000000000000000000, 0.000000000000000000, 0.000000000000000000 ) ) ;
#6795=ORIENTED_EDGE ( 'NONE', *, *, #22149, .F. ) ;
#6796=DIRECTION ( 'NONE',  ( 0.000000000000000000, -0.07845909572785234043, 0.9969173337331274087 ) ) ;
#6797=ORIENTED_EDGE ( 'NONE', *, *, #37997, .F. ) ;
#6804=DIRECTION ( 'NONE',  ( 0.000000000000000000, 0.000000000000000000, 1.000000000000000000 ) ) ;
#6805=VERTEX_POINT ( 'NONE', #3724 ) ;
#6809=DIRECTION ( 'NONE',  ( 0.000000000000000000, 0.3826834323650907810, -0.9238795325112864054 ) ) ;
#6814=ORIENTED_EDGE ( 'NONE', *, *, #16951, .T. ) ;
#6817=ORIENTED_EDGE ( 'NONE', *, *, #9013, .T. ) ;
#6823=CARTESIAN_POINT ( 'NONE',  ( 10.00000000000000000, 0.000000000000000000, 0.000000000000000000 ) ) ;
#6827=AXIS2_PLACEMENT_3D ( 'NONE', #20426, #46640, #35618 ) ;
#6833=LINE ( 'NONE', #2424, #2497 ) ;
#6836=DIRECTION ( 'NONE',  ( 0.000000000000000000, 0.000000000000000000, 1.000000000000000000 ) ) ;
#6846=DIRECTION ( 'NONE',  ( 0.000000000000000000, -0.9238795325112906243, 0.3826834323650805114 ) ) ;
#6855=CIRCLE ( 'NONE', #43578, 31.99999999999999289 ) ;
#6859=DIRECTION ( 'NONE',  ( 0.000000000000000000, -0.8910065241883722287, 0.4539904997395383668 ) ) ;
#6860=CARTESIAN_POINT ( 'NONE',  ( 10.00000000000000000, 51.29473840253317718, -63.97538442413367932 ) ) ;
#6871=AXIS2_PLACEMENT_3D ( 'NONE', #9205, #5303, #24139 ) ;
#6874=ORIENTED_EDGE ( 'NONE', *, *, #17431, .F. ) ;
#6876=ORIENTED_EDGE ( 'NONE', *, *, #19794, .T. ) ;
#6897=EDGE_LOOP ( 'NONE', ( #31361, #2847, #13043, #22659 ) ) ;
#6901=ORIENTED_EDGE ( 'NONE', *, *, #14370, .F. ) ;
#6902=ADVANCED_FACE ( 'NONE', ( #15472 ), #29665, .T. ) ;
#6903=DIRECTION ( 'NONE',  ( 0.000000000000000000, 0.000000000000000000, 1.000000000000000000 ) ) ;
#6912=ORIENTED_EDGE ( 'NONE', *, *, #37923, .F. ) ;
#6919=ORIENTED_EDGE ( 'NONE', *, *, #19584, .T. ) ;
#6921=DIRECTION ( 'NONE',  ( -1.000000000000000000, -0.000000000000000000, 0.000000000000000000 ) ) ;
#6923=LINE ( 'NONE', #29441, #17033 ) ;
#6924=CARTESIAN_POINT ( 'NONE',  ( 0.000000000000000000, 59.46389618802034960, -49.70050353004825894 ) ) ;
#6926=ORIENTED_EDGE ( 'NONE', *, *, #13097, .T. ) ;
#6930=DIRECTION ( 'NONE',  ( 0.000000000000000000, -0.7604059656000228262, -0.6494480483301932061 ) ) ;
#6940=EDGE_CURVE ( 'NONE', #26295, #45334, #9550, .T. ) ;
#6941=CARTESIAN_POINT ( 'NONE',  ( 0.000000000000000000, 68.26794271651307611, -31.47745569255064169 ) ) ;
#6946=DIRECTION ( 'NONE',  ( -1.000000000000000000, 0.000000000000000000, 0.000000000000000000 ) ) ;
#6951=EDGE_CURVE ( 'NONE', #11599, #32258, #29426, .T. ) ;
#6952=CARTESIAN_POINT ( 'NONE',  ( 10.00000000000000000, -33.71516098798684880, -74.74816331893465815 ) ) ;
#6955=ORIENTED_EDGE ( 'NONE', *, *, #32561, .T. ) ;
#6960=DIRECTION ( 'NONE',  ( 0.000000000000000000, 0.000000000000000000, 1.000000000000000000 ) ) ;
#6961=CYLINDRICAL_SURFACE ( 'NONE', #24367, 32.00000000000000000 ) ;
#6963=EDGE_CURVE ( 'NONE', #35099, #23124, #1507, .T. ) ;
#6965=CARTESIAN_POINT ( 'NONE',  ( 0.000000000000000000, 50.23322058963442061, -64.81221759200289512 ) ) ;
#6967=DIRECTION ( 'NONE',  ( 0.000000000000000000, 0.000000000000000000, -1.000000000000000000 ) ) ;
#6969=CARTESIAN_POINT ( 'NONE',  ( 10.00000000000000000, -26.02418014898359289, 70.52718814184250107 ) ) ;
#6974=AXIS2_PLACEMENT_3D ( 'NONE', #47206, #24930, #39868 ) ;
#6982=DIRECTION ( 'NONE',  ( -1.000000000000000000, 0.000000000000000000, -0.000000000000000000 ) ) ;
#6985=VERTEX_POINT ( 'NONE', #16670 ) ;
#6987=ORIENTED_EDGE ( 'NONE', *, *, #19095, .T. ) ;
#6991=VERTEX_POINT ( 'NONE', #34783 ) ;
#6996=CYLINDRICAL_SURFACE ( 'NONE', #25813, 82.00000000000000000 ) ;
#6999=ORIENTED_EDGE ( 'NONE', *, *, #2208, .F. ) ;
#7004=ORIENTED_EDGE ( 'NONE', *, *, #13327, .F. ) ;
#7008=EDGE_CURVE ( 'NONE', #15030, #39579, #41914, .T. ) ;
#7010=DIRECTION ( 'NONE',  ( 0.000000000000000000, 0.000000000000000000, -1.000000000000000000 ) ) ;
#7014=CYLINDRICAL_SURFACE ( 'NONE', #41694, 77.49899999999999523 ) ;
#7017=EDGE_CURVE ( 'NONE', #16188, #10009, #45823, .T. ) ;
#7019=ORIENTED_EDGE ( 'NONE', *, *, #28946, .F. ) ;
#7020=CARTESIAN_POINT ( 'NONE',  ( 10.00000000000000000, 74.65374052328648702, 8.840884882375350529 ) ) ;
#7022=DIRECTION ( 'NONE',  ( -1.000000000000000000, 0.000000000000000000, -0.000000000000000000 ) ) ;
#7024=VERTEX_POINT ( 'NONE', #13015 ) ;
#7026=CARTESIAN_POINT ( 'NONE',  ( 10.00000000000000000, 77.19088730480534366, -6.903761155836915187 ) ) ;
#7040=ORIENTED_EDGE ( 'NONE', *, *, #36407, .F. ) ;
#7047=ADVANCED_FACE ( 'NONE', ( #24025 ), #19592, .T. ) ;
#7055=LINE ( 'NONE', #33969, #23117 ) ;
#7059=CIRCLE ( 'NONE', #1591, 31.99999999999999289 ) ;
#7060=DIRECTION ( 'NONE',  ( 0.000000000000000000, 0.9969173337331276308, 0.07845909572784864894 ) ) ;
#7064=AXIS2_PLACEMENT_3D ( 'NONE', #38942, #5640, #46523 ) ;
#7065=ADVANCED_FACE ( 'NONE', ( #32785 ), #2685, .T. ) ;
#7066=EDGE_CURVE ( 'NONE', #23020, #10873, #39610, .T. ) ;
#7070=DIRECTION ( 'NONE',  ( 0.000000000000000000, 0.000000000000000000, 1.000000000000000000 ) ) ;
#7073=VERTEX_POINT ( 'NONE', #13475 ) ;
#7078=CARTESIAN_POINT ( 'NONE',  ( 10.00000000000000000, 50.95692526931414790, -58.39081064771693974 ) ) ;
#7082=CYLINDRICAL_SURFACE ( 'NONE', #13299, 31.99999999999999289 ) ;
#7087=ORIENTED_EDGE ( 'NONE', *, *, #41445, .T. ) ;
#7089=CARTESIAN_POINT ( 'NONE',  ( 0.000000000000000000, 55.16347631943042984, 60.67117009219157353 ) ) ;
#7091=DIRECTION ( 'NONE',  ( -1.000000000000000000, -0.000000000000000000, 0.000000000000000000 ) ) ;
#7099=AXIS2_PLACEMENT_3D ( 'NONE', #10248, #32533, #17113 ) ;
#7102=CIRCLE ( 'NONE', #34451, 31.99999999999999645 ) ;
#7103=AXIS2_PLACEMENT_3D ( 'NONE', #44767, #7576, #18810 ) ;
#7109=DIRECTION ( 'NONE',  ( 0.000000000000000000, 0.000000000000000000, 1.000000000000000000 ) ) ;
#7112=ORIENTED_EDGE ( 'NONE', *, *, #41308, .T. ) ;
#7114=CARTESIAN_POINT ( 'NONE',  ( -10.00000000000000000, 0.000000000000000000, 0.000000000000000000 ) ) ;
#7115=EDGE_CURVE ( 'NONE', #43867, #32554, #5884, .T. ) ;
#7116=CARTESIAN_POINT ( 'NONE',  ( 10.00000000000000000, -81.50828551894232987, 8.966570791700396725 ) ) ;
#7129=AXIS2_PLACEMENT_3D ( 'NONE', #18143, #19125, #33087 ) ;
#7130=DIRECTION ( 'NONE',  ( -1.000000000000000000, 0.000000000000000000, 0.000000000000000000 ) ) ;
#7131=ORIENTED_EDGE ( 'NONE', *, *, #44262, .T. ) ;
#7140=CIRCLE ( 'NONE', #15733, 82.00000000000000000 ) ;
#7141=ORIENTED_EDGE ( 'NONE', *, *, #30710, .F. ) ;
#7144=CARTESIAN_POINT ( 'NONE',  ( 10.00000000000000000, 0.000000000000000000, 0.000000000000000000 ) ) ;
#7147=DIRECTION ( 'NONE',  ( 0.000000000000000000, 0.000000000000000000, 1.000000000000000000 ) ) ;
#7151=DIRECTION ( 'NONE',  ( 0.000000000000000000, 0.000000000000000000, 1.000000000000000000 ) ) ;
#7161=EDGE_LOOP ( 'NONE', ( #9463, #21699, #20437, #45412 ) ) ;
#7163=VERTEX_POINT ( 'NONE', #2219 ) ;
#7168=AXIS2_PLACEMENT_3D ( 'NONE', #25624, #13900, #1739 ) ;
#7171=DIRECTION ( 'NONE',  ( -1.000000000000000000, -0.000000000000000000, 0.000000000000000000 ) ) ;
#7174=EDGE_CURVE ( 'NONE', #17338, #15509, #26995, .T. ) ;
#7176=DIRECTION ( 'NONE',  ( -1.000000000000000000, -0.000000000000000000, 0.000000000000000000 ) ) ;
#7177=EDGE_CURVE ( 'NONE', #24526, #43853, #23099, .T. ) ;
#7178=CARTESIAN_POINT ( 'NONE',  ( 0.000000000000000000, 0.000000000000000000, 0.000000000000000000 ) ) ;
#7180=CIRCLE ( 'NONE', #15020, 31.99999999999999289 ) ;
#7183=EDGE_LOOP ( 'NONE', ( #24703, #4319, #33246, #34425 ) ) ;
#7186=EDGE_CURVE ( 'NONE', #45284, #36506, #44299, .T. ) ;
#7192=ORIENTED_EDGE ( 'NONE', *, *, #27115, .T. ) ;
#7194=DIRECTION ( 'NONE',  ( -1.000000000000000000, -0.000000000000000000, 0.000000000000000000 ) ) ;
#7202=AXIS2_PLACEMENT_3D ( 'NONE', #47382, #40279, #3050 ) ;
#7212=VECTOR ( 'NONE', #20692, 1000.000000000000000 ) ;
#7216=DIRECTION ( 'NONE',  ( 0.000000000000000000, 0.000000000000000000, 1.000000000000000000 ) ) ;
#7221=DIRECTION ( 'NONE',  ( -1.000000000000000000, 0.000000000000000000, 0.000000000000000000 ) ) ;
#7227=DIRECTION ( 'NONE',  ( 0.000000000000000000, 0.9510565162951546414, -0.3090169943749446202 ) ) ;
#7233=EDGE_CURVE ( 'NONE', #22033, #31962, #2761, .T. ) ;
#7240=VERTEX_POINT ( 'NONE', #30102 ) ;
#7243=DIRECTION ( 'NONE',  ( -1.000000000000000000, 0.000000000000000000, 0.000000000000000000 ) ) ;
#7248=ORIENTED_EDGE ( 'NONE', *, *, #23677, .F. ) ;
#7249=DIRECTION ( 'NONE',  ( -1.000000000000000000, 0.000000000000000000, 0.000000000000000000 ) ) ;
#7250=ORIENTED_EDGE ( 'NONE', *, *, #12186, .F. ) ;
#7252=CIRCLE ( 'NONE', #44778, 82.00000000000000000 ) ;
#7256=DIRECTION ( 'NONE',  ( -1.000000000000000000, 0.000000000000000000, 0.000000000000000000 ) ) ;
#7258=CYLINDRICAL_SURFACE ( 'NONE', #8566, 31.99999999999999289 ) ;
#7267=DIRECTION ( 'NONE',  ( -1.000000000000000000, -0.000000000000000000, 0.000000000000000000 ) ) ;
#7277=DIRECTION ( 'NONE',  ( 0.000000000000000000, 0.9723699203976773342, -0.2334453638559024213 ) ) ;
#7289=AXIS2_PLACEMENT_3D ( 'NONE', #37688, #29859, #19081 ) ;
#7290=EDGE_CURVE ( 'NONE', #42611, #26945, #13701, .T. ) ;
#7294=ORIENTED_EDGE ( 'NONE', *, *, #44526, .F. ) ;
#7298=CARTESIAN_POINT ( 'NONE',  ( 10.00000000000000000, -63.97538442413463855, 51.29473840253199768 ) ) ;
#7299=ORIENTED_EDGE ( 'NONE', *, *, #17739, .T. ) ;
#7300=ORIENTED_EDGE ( 'NONE', *, *, #7893, .T. ) ;
#7304=VECTOR ( 'NONE', #7651, 1000.000000000000000 ) ;
#7305=EDGE_CURVE ( 'NONE', #29267, #44497, #481, .T. ) ;
#7307=CARTESIAN_POINT ( 'NONE',  ( 0.000000000000000000, -23.16143007188376757, -73.95703589263997912 ) ) ;
#7314=ORIENTED_EDGE ( 'NONE', *, *, #32284, .F. ) ;
#7316=AXIS2_PLACEMENT_3D ( 'NONE', #24960, #46779, #36464 ) ;
#7326=DIRECTION ( 'NONE',  ( -1.000000000000000000, 0.000000000000000000, 0.000000000000000000 ) ) ;
#7327=DIRECTION ( 'NONE',  ( 0.000000000000000000, 0.000000000000000000, 1.000000000000000000 ) ) ;
#7330=DIRECTION ( 'NONE',  ( -1.000000000000000000, 0.000000000000000000, 0.000000000000000000 ) ) ;
#7337=CARTESIAN_POINT ( 'NONE',  ( 10.00000000000000000, -46.53671651293991118, 59.03961581697383565 ) ) ;
#7338=CIRCLE ( 'NONE', #32366, 32.00000000000000000 ) ;
#7339=ORIENTED_EDGE ( 'NONE', *, *, #46366, .F. ) ;
#7344=VERTEX_POINT ( 'NONE', #707 ) ;
#7349=ADVANCED_FACE ( 'NONE', ( #30830 ), #38903, .T. ) ;
#7350=ORIENTED_EDGE ( 'NONE', *, *, #11842, .T. ) ;
#7352=CIRCLE ( 'NONE', #46430, 32.00000000000000000 ) ;
#7359=ORIENTED_EDGE ( 'NONE', *, *, #888, .T. ) ;
#7366=ORIENTED_EDGE ( 'NONE', *, *, #20532, .F. ) ;
#7367=VERTEX_POINT ( 'NONE', #12467 ) ;
#7369=ORIENTED_EDGE ( 'NONE', *, *, #37162, .F. ) ;
#7370=CIRCLE ( 'NONE', #44903, 77.49900000000000944 ) ;
#7375=CARTESIAN_POINT ( 'NONE',  ( 10.00000000000000000, 70.53064760720278059, 26.01480285779964774 ) ) ;
#7376=CARTESIAN_POINT ( 'NONE',  ( 0.000000000000000000, -8.966570791700153364, -81.50828551894237251 ) ) ;
#7377=AXIS2_PLACEMENT_3D ( 'NONE', #271, #22796, #44828 ) ;
#7378=DIRECTION ( 'NONE',  ( 0.000000000000000000, 0.000000000000000000, -1.000000000000000000 ) ) ;
#7382=VERTEX_POINT ( 'NONE', #34721 ) ;
#7390=CARTESIAN_POINT ( 'NONE',  ( 0.000000000000000000, -29.01471420065507090, -76.69515212746047439 ) ) ;
#7391=VECTOR ( 'NONE', #20609, 1000.000000000000000 ) ;
#7395=CARTESIAN_POINT ( 'NONE',  ( 10.00000000000000000, 21.60688246758585862, 79.10210256391376049 ) ) ;
#7397=EDGE_CURVE ( 'NONE', #47663, #21394, #43414, .T. ) ;
#7399=AXIS2_PLACEMENT_3D ( 'NONE', #6141, #21058, #16915 ) ;
#7400=CARTESIAN_POINT ( 'NONE',  ( 10.00000000000000000, -8.840884882374576037, -74.65374052328658649 ) ) ;
#7406=DIRECTION ( 'NONE',  ( -1.000000000000000000, 0.000000000000000000, 0.000000000000000000 ) ) ;
#7408=LINE ( 'NONE', #18883, #27989 ) ;
#7409=DIRECTION ( 'NONE',  ( -1.000000000000000000, -0.000000000000000000, -0.000000000000000000 ) ) ;
#7411=AXIS2_PLACEMENT_3D ( 'NONE', #45674, #9424, #38833 ) ;
#7424=VECTOR ( 'NONE', #16001, 1000.000000000000000 ) ;
#7426=ORIENTED_EDGE ( 'NONE', *, *, #47869, .T. ) ;
#7436=CYLINDRICAL_SURFACE ( 'NONE', #29334, 32.00000000000000000 ) ;
#7440=DIRECTION ( 'NONE',  ( 0.000000000000000000, 0.000000000000000000, -1.000000000000000000 ) ) ;
#7448=CARTESIAN_POINT ( 'NONE',  ( 0.000000000000000000, 8.840884882375075193, 74.65374052328651544 ) ) ;
#7454=CYLINDRICAL_SURFACE ( 'NONE', #19736, 77.49899999999999523 ) ;
#7456=CARTESIAN_POINT ( 'NONE',  ( 10.00000000000000000, 0.000000000000000000, 0.000000000000000000 ) ) ;
#7461=CARTESIAN_POINT ( 'NONE',  ( 0.000000000000000000, -10.30890764327323872, -81.34940948281348483 ) ) ;
#7462=CIRCLE ( 'NONE', #30916, 31.99999999999999645 ) ;
#7463=EDGE_CURVE ( 'NONE', #46126, #29279, #29323, .T. ) ;
#7465=DIRECTION ( 'NONE',  ( -1.000000000000000000, 0.000000000000000000, 0.000000000000000000 ) ) ;
#7468=VECTOR ( 'NONE', #24054, 1000.000000000000000 ) ;
#7470=FACE_OUTER_BOUND ( 'NONE', #44631, .T. ) ;
#7471=LINE ( 'NONE', #18707, #16752 ) ;
#7484=DIRECTION ( 'NONE',  ( -1.000000000000000000, 0.000000000000000000, -0.000000000000000000 ) ) ;
#7489=DIRECTION ( 'NONE',  ( -1.000000000000000000, 0.000000000000000000, -0.000000000000000000 ) ) ;
#7490=DIRECTION ( 'NONE',  ( 0.000000000000000000, 0.9238795325112851842, 0.3826834323650938341 ) ) ;
#7495=VERTEX_POINT ( 'NONE', #14147 ) ;
#7504=ORIENTED_EDGE ( 'NONE', *, *, #35025, .F. ) ;
#7510=FACE_OUTER_BOUND ( 'NONE', #6099, .T. ) ;
#7514=CIRCLE ( 'NONE', #9045, 31.99999999999999289 ) ;
#7520=EDGE_CURVE ( 'NONE', #2120, #26793, #16092, .T. ) ;
#7522=ADVANCED_FACE ( 'NONE', ( #6095 ), #39631, .T. ) ;
#7531=DIRECTION ( 'NONE',  ( 0.000000000000000000, 0.000000000000000000, 1.000000000000000000 ) ) ;
#7537=DIRECTION ( 'NONE',  ( 0.000000000000000000, 0.000000000000000000, 1.000000000000000000 ) ) ;
#7543=CIRCLE ( 'NONE', #34887, 32.00000000000000000 ) ;
#7547=ADVANCED_FACE ( 'NONE', ( #20773 ), #2625, .T. ) ;
#7548=AXIS2_PLACEMENT_3D ( 'NONE', #16856, #21227, #31806 ) ;
#7551=EDGE_CURVE ( 'NONE', #12619, #3891, #33258, .T. ) ;
#7560=CARTESIAN_POINT ( 'NONE',  ( 0.000000000000000000, 3.894527615419058009, -81.90746397400384637 ) ) ;
#7563=AXIS2_PLACEMENT_3D ( 'NONE', #14127, #42851, #24008 ) ;
#7573=ORIENTED_EDGE ( 'NONE', *, *, #47416, .T. ) ;
#7576=DIRECTION ( 'NONE',  ( -1.000000000000000000, 0.000000000000000000, 0.000000000000000000 ) ) ;
#7584=EDGE_CURVE ( 'NONE', #45066, #44958, #13189, .T. ) ;
#7585=ORIENTED_EDGE ( 'NONE', *, *, #6635, .F. ) ;
#7601=VECTOR ( 'NONE', #36880, 1000.000000000000000 ) ;
#7606=CARTESIAN_POINT ( 'NONE',  ( 0.000000000000000000, -70.52718814184240159, -26.02418014898383802 ) ) ;
#7613=DIRECTION ( 'NONE',  ( 0.000000000000000000, 1.000000000000000000, 3.469446951953614978E-15 ) ) ;
#7616=ORIENTED_EDGE ( 'NONE', *, *, #23210, .T. ) ;
#7618=DIRECTION ( 'NONE',  ( -1.000000000000000000, 0.000000000000000000, 0.000000000000000000 ) ) ;
#7623=ORIENTED_EDGE ( 'NONE', *, *, #7520, .T. ) ;
#7626=VERTEX_POINT ( 'NONE', #43291 ) ;
#7633=EDGE_CURVE ( 'NONE', #30791, #43803, #23869, .T. ) ;
#7640=CARTESIAN_POINT ( 'NONE',  ( 5.000000000000002665, 74.18225833017937987, -34.94270380257560049 ) ) ;
#7644=ADVANCED_FACE ( 'NONE', ( #16050 ), #24113, .T. ) ;
#7646=CYLINDRICAL_SURFACE ( 'NONE', #38650, 31.99999999999999289 ) ;
#7651=DIRECTION ( 'NONE',  ( -1.000000000000000000, -0.000000000000000000, 0.000000000000000000 ) ) ;
#7652=ORIENTED_EDGE ( 'NONE', *, *, #22459, .T. ) ;
#7654=CARTESIAN_POINT ( 'NONE',  ( 5.000000000000000000, 46.11716303203188261, 67.80270845531904911 ) ) ;
#7656=EDGE_CURVE ( 'NONE', #45038, #6991, #35608, .T. ) ;
#7657=VECTOR ( 'NONE', #37358, 1000.000000000000000 ) ;
#7660=EDGE_CURVE ( 'NONE', #29685, #33124, #1230, .T. ) ;
#7665=DIRECTION ( 'NONE',  ( 0.000000000000000000, 0.000000000000000000, -1.000000000000000000 ) ) ;
#7670=AXIS2_PLACEMENT_3D ( 'NONE', #23143, #45659, #19448 ) ;
#7672=CARTESIAN_POINT ( 'NONE',  ( 10.00000000000000000, 0.000000000000000000, 0.000000000000000000 ) ) ;
#7675=DIRECTION ( 'NONE',  ( -1.000000000000000000, 0.000000000000000000, 0.000000000000000000 ) ) ;
#7681=CARTESIAN_POINT ( 'NONE',  ( 10.00000000000000000, -55.38113227695743745, -54.21277698773734244 ) ) ;
#7682=DIRECTION ( 'NONE',  ( -1.000000000000000000, 0.000000000000000000, 0.000000000000000000 ) ) ;
#7686=DIRECTION ( 'NONE',  ( 0.000000000000000000, -0.07845909572783053842, -0.9969173337331290741 ) ) ;
#7688=ADVANCED_FACE ( 'NONE', ( #16772 ), #35112, .T. ) ;
#7702=CYLINDRICAL_SURFACE ( 'NONE', #16031, 31.99999999999999289 ) ;
#7718=FACE_OUTER_BOUND ( 'NONE', #33454, .T. ) ;
#7720=ORIENTED_EDGE ( 'NONE', *, *, #10172, .F. ) ;
#7724=ORIENTED_EDGE ( 'NONE', *, *, #35656, .F. ) ;
#7725=ORIENTED_EDGE ( 'NONE', *, *, #7551, .T. ) ;
#7726=ADVANCED_FACE ( 'NONE', ( #19945 ), #31224, .T. ) ;
#7727=ORIENTED_EDGE ( 'NONE', *, *, #48444, .T. ) ;
#7731=VERTEX_POINT ( 'NONE', #8933 ) ;
#7733=CIRCLE ( 'NONE', #3047, 82.00000000000000000 ) ;
#7742=DIRECTION ( 'NONE',  ( 0.000000000000000000, 0.000000000000000000, 1.000000000000000000 ) ) ;
#7746=EDGE_CURVE ( 'NONE', #37588, #16358, #9904, .T. ) ;
#7749=ORIENTED_EDGE ( 'NONE', *, *, #33453, .T. ) ;
#7750=DIRECTION ( 'NONE',  ( -1.000000000000000000, 0.000000000000000000, 0.000000000000000000 ) ) ;
#7754=DIRECTION ( 'NONE',  ( -1.000000000000000000, -0.000000000000000000, -0.000000000000000000 ) ) ;
#7765=EDGE_LOOP ( 'NONE', ( #19746, #6874, #35666, #41608 ) ) ;
#7769=VECTOR ( 'NONE', #37635, 1000.000000000000000 ) ;
#7770=LINE ( 'NONE', #431, #7769 ) ;
#7771=FACE_OUTER_BOUND ( 'NONE', #36073, .T. ) ;
#7784=VERTEX_POINT ( 'NONE', #13572 ) ;
#7785=DIRECTION ( 'NONE',  ( 0.000000000000000000, -0.1564344650402172687, -0.9876883405951399908 ) ) ;
#7788=CARTESIAN_POINT ( 'NONE',  ( 0.000000000000000000, 71.27951684758068041, -30.41916302227035018 ) ) ;
#7801=CARTESIAN_POINT ( 'NONE',  ( 0.000000000000000000, 0.000000000000000000, 0.000000000000000000 ) ) ;
#7809=CARTESIAN_POINT ( 'NONE',  ( 10.00000000000000000, 64.81221759200342092, 50.23322058963369585 ) ) ;
#7814=AXIS2_PLACEMENT_3D ( 'NONE', #35305, #1781, #31662 ) ;
#7821=ORIENTED_EDGE ( 'NONE', *, *, #6951, .F. ) ;
#7823=FACE_OUTER_BOUND ( 'NONE', #44710, .T. ) ;
#7826=ORIENTED_EDGE ( 'NONE', *, *, #35094, .F. ) ;
#7827=ORIENTED_EDGE ( 'NONE', *, *, #8569, .F. ) ;
#7834=ORIENTED_EDGE ( 'NONE', *, *, #22102, .T. ) ;
#7835=EDGE_LOOP ( 'NONE', ( #20970, #30810, #15726, #4893 ) ) ;
#7839=CIRCLE ( 'NONE', #17201, 31.99999999999999645 ) ;
#7841=AXIS2_PLACEMENT_3D ( 'NONE', #48192, #40135, #40849 ) ;
#7845=DIRECTION ( 'NONE',  ( -1.000000000000000000, -0.000000000000000000, 0.000000000000000000 ) ) ;
#7850=CARTESIAN_POINT ( 'NONE',  ( 10.00000000000000000, 0.000000000000000000, 0.000000000000000000 ) ) ;
#7855=ORIENTED_EDGE ( 'NONE', *, *, #31745, .T. ) ;
#7856=CARTESIAN_POINT ( 'NONE',  ( 10.00000000000000000, 0.000000000000000000, 0.000000000000000000 ) ) ;
#7861=DIRECTION ( 'NONE',  ( 0.000000000000000000, 1.000000000000000000, 3.491481338843133355E-15 ) ) ;
#7862=DIRECTION ( 'NONE',  ( -1.000000000000000000, -0.000000000000000000, -0.000000000000000000 ) ) ;
#7867=AXIS2_PLACEMENT_3D ( 'NONE', #8413, #12575, #38041 ) ;
#7868=AXIS2_PLACEMENT_3D ( 'NONE', #21455, #43501, #14356 ) ;
#7871=DIRECTION ( 'NONE',  ( -1.000000000000000000, 0.000000000000000000, 0.000000000000000000 ) ) ;
#7883=ADVANCED_FACE ( 'NONE', ( #18448 ), #30204, .T. ) ;
#7884=DIRECTION ( 'NONE',  ( -1.000000000000000000, 0.000000000000000000, 0.000000000000000000 ) ) ;
#7889=ORIENTED_EDGE ( 'NONE', *, *, #9119, .F. ) ;
#7893=EDGE_CURVE ( 'NONE', #31795, #15510, #26509, .T. ) ;
#7896=CIRCLE ( 'NONE', #16546, 82.00000000000000000 ) ;
#7902=AXIS2_PLACEMENT_3D ( 'NONE', #39098, #23678, #23434 ) ;
#7906=FACE_OUTER_BOUND ( 'NONE', #8036, .T. ) ;
#7912=EDGE_LOOP ( 'NONE', ( #31298, #30088, #42262, #1675 ) ) ;
#7915=ADVANCED_FACE ( 'NONE', ( #7906 ), #15275, .T. ) ;
#7916=CARTESIAN_POINT ( 'NONE',  ( 5.000000000000000000, -44.99326035066101781, 68.55367621811127776 ) ) ;
#7918=DIRECTION ( 'NONE',  ( -1.000000000000000000, -0.000000000000000000, -0.000000000000000000 ) ) ;
#7921=DIRECTION ( 'NONE',  ( 0.000000000000000000, 0.000000000000000000, -1.000000000000000000 ) ) ;
#7923=CYLINDRICAL_SURFACE ( 'NONE', #4877, 31.99999999999999289 ) ;
#7925=DIRECTION ( 'NONE',  ( 0.000000000000000000, -0.9969173337331287410, 0.07845909572783486829 ) ) ;
#7929=FACE_OUTER_BOUND ( 'NONE', #22353, .T. ) ;
#7932=CARTESIAN_POINT ( 'NONE',  ( 10.00000000000000000, -44.88180994100421373, 63.18004540533011948 ) ) ;
#7937=EDGE_CURVE ( 'NONE', #15723, #13395, #11106, .T. ) ;
#7941=DIRECTION ( 'NONE',  ( 0.000000000000000000, 0.000000000000000000, 1.000000000000000000 ) ) ;
#7949=EDGE_CURVE ( 'NONE', #30385, #17705, #21806, .T. ) ;
#7952=DIRECTION ( 'NONE',  ( 0.000000000000000000, 0.000000000000000000, 1.000000000000000000 ) ) ;
#7954=DIRECTION ( 'NONE',  ( -1.000000000000000000, -0.000000000000000000, -0.000000000000000000 ) ) ;
#7956=ORIENTED_EDGE ( 'NONE', *, *, #6468, .F. ) ;
#7965=CIRCLE ( 'NONE', #4070, 31.99999999999999289 ) ;
#7967=CARTESIAN_POINT ( 'NONE',  ( 5.000000000000000000, -60.67117009219098378, -55.16347631943106933 ) ) ;
#7981=DIRECTION ( 'NONE',  ( 0.000000000000000000, 0.000000000000000000, 1.000000000000000000 ) ) ;
#7984=CARTESIAN_POINT ( 'NONE',  ( 10.00000000000000000, -73.73191006444561424, -14.66109333815538918 ) ) ;
#7989=ORIENTED_EDGE ( 'NONE', *, *, #43653, .T. ) ;
#7999=VERTEX_POINT ( 'NONE', #37645 ) ;
#8000=AXIS2_PLACEMENT_3D ( 'NONE', #5887, #31597, #38436 ) ;
#8005=ORIENTED_EDGE ( 'NONE', *, *, #5466, .F. ) ;
#8007=ADVANCED_FACE ( 'NONE', ( #8015 ), #22953, .T. ) ;
#8010=CARTESIAN_POINT ( 'NONE',  ( 10.00000000000000000, -54.21277698773636899, -55.38113227695839669 ) ) ;
#8012=ORIENTED_EDGE ( 'NONE', *, *, #40747, .F. ) ;
#8015=FACE_OUTER_BOUND ( 'NONE', #44822, .T. ) ;
#8023=ORIENTED_EDGE ( 'NONE', *, *, #16406, .F. ) ;
#8027=CIRCLE ( 'NONE', #44787, 31.99999999999999289 ) ;
#8029=ORIENTED_EDGE ( 'NONE', *, *, #45262, .T. ) ;
#8033=CARTESIAN_POINT ( 'NONE',  ( 10.00000000000000000, 0.000000000000000000, 0.000000000000000000 ) ) ;
#8036=EDGE_LOOP ( 'NONE', ( #5073, #5212, #47604, #26094 ) ) ;
#8037=CYLINDRICAL_SURFACE ( 'NONE', #42389, 31.99999999999999289 ) ;
#8039=AXIS2_PLACEMENT_3D ( 'NONE', #33493, #23211, #10986 ) ;
#8040=CARTESIAN_POINT ( 'NONE',  ( 0.000000000000000000, 0.000000000000000000, 0.000000000000000000 ) ) ;
#8050=FACE_OUTER_BOUND ( 'NONE', #42475, .T. ) ;
#8055=CYLINDRICAL_SURFACE ( 'NONE', #11355, 32.00000000000000000 ) ;
#8061=EDGE_CURVE ( 'NONE', #2237, #1729, #18670, .T. ) ;
#8066=VERTEX_POINT ( 'NONE', #15856 ) ;
#8067=ADVANCED_FACE ( 'NONE', ( #30795 ), #4374, .T. ) ;
#8068=AXIS2_PLACEMENT_3D ( 'NONE', #38905, #19786, #42084 ) ;
#8070=DIRECTION ( 'NONE',  ( 0.000000000000000000, 0.000000000000000000, 1.000000000000000000 ) ) ;
#8074=VECTOR ( 'NONE', #22906, 1000.000000000000000 ) ;
#8078=CIRCLE ( 'NONE', #25263, 77.49900000000000944 ) ;
#8079=EDGE_CURVE ( 'NONE', #33302, #47783, #48375, .T. ) ;
#8081=CIRCLE ( 'NONE', #294, 31.99999999999999289 ) ;
#8088=ORIENTED_EDGE ( 'NONE', *, *, #4752, .T. ) ;
#8091=VECTOR ( 'NONE', #28501, 1000.000000000000000 ) ;
#8093=FACE_OUTER_BOUND ( 'NONE', #44689, .T. ) ;
#8102=DIRECTION ( 'NONE',  ( 0.000000000000000000, 0.000000000000000000, 1.000000000000000000 ) ) ;
#8106=CARTESIAN_POINT ( 'NONE',  ( 0.000000000000000000, 0.000000000000000000, 0.000000000000000000 ) ) ;
#8111=EDGE_LOOP ( 'NONE', ( #32022, #22349, #9963, #45949 ) ) ;
#8113=DIRECTION ( 'NONE',  ( 0.000000000000000000, -0.9510565162951500895, -0.3090169943749583870 ) ) ;
#8115=EDGE_CURVE ( 'NONE', #33547, #27354, #24932, .T. ) ;
#8118=CIRCLE ( 'NONE', #32378, 82.00000000000000000 ) ;
#8127=VECTOR ( 'NONE', #36648, 1000.000000000000000 ) ;
#8129=EDGE_CURVE ( 'NONE', #16510, #13135, #9212, .T. ) ;
#8135=AXIS2_PLACEMENT_3D ( 'NONE', #27084, #38329, #24354 ) ;
#8142=EDGE_CURVE ( 'NONE', #45131, #26885, #4634, .T. ) ;
#8143=DIRECTION ( 'NONE',  ( -1.000000000000000000, -0.000000000000000000, -0.000000000000000000 ) ) ;
#8148=AXIS2_PLACEMENT_3D ( 'NONE', #14522, #10845, #44372 ) ;
#8151=EDGE_CURVE ( 'NONE', #22099, #9073, #28019, .T. ) ;
#8156=EDGE_CURVE ( 'NONE', #45983, #17444, #35805, .T. ) ;
#8158=AXIS2_PLACEMENT_3D ( 'NONE', #9227, #9954, #39091 ) ;
#8165=CARTESIAN_POINT ( 'NONE',  ( 5.000000000000002665, 15.33399622253600292, -80.55351364060572905 ) ) ;
#8169=DIRECTION ( 'NONE',  ( -1.000000000000000000, -0.000000000000000000, -0.000000000000000000 ) ) ;
#8176=LINE ( 'NONE', #32150, #15343 ) ;
#8179=LINE ( 'NONE', #15299, #48170 ) ;
#8180=EDGE_CURVE ( 'NONE', #42173, #7626, #42532, .T. ) ;
#8181=DIRECTION ( 'NONE',  ( -1.000000000000000000, 0.000000000000000000, 0.000000000000000000 ) ) ;
#8186=DIRECTION ( 'NONE',  ( -1.000000000000000000, -0.000000000000000000, 0.000000000000000000 ) ) ;
#8188=VERTEX_POINT ( 'NONE', #35168 ) ;
#8190=VECTOR ( 'NONE', #2095, 1000.000000000000000 ) ;
#8191=CIRCLE ( 'NONE', #12126, 32.00000000000000711 ) ;
#8194=EDGE_LOOP ( 'NONE', ( #8279, #5665, #19281, #18654 ) ) ;
#8196=AXIS2_PLACEMENT_3D ( 'NONE', #45034, #42758, #11508 ) ;
#8206=DIRECTION ( 'NONE',  ( -1.000000000000000000, 0.000000000000000000, 0.000000000000000000 ) ) ;
#8212=CARTESIAN_POINT ( 'NONE',  ( 10.00000000000000000, -77.19088730480528682, 6.903761155837488062 ) ) ;
#8214=CIRCLE ( 'NONE', #35583, 32.00000000000000000 ) ;
#8216=EDGE_LOOP ( 'NONE', ( #13312, #19118, #36608, #13400 ) ) ;
#8218=VERTEX_POINT ( 'NONE', #6060 ) ;
#8219=CIRCLE ( 'NONE', #35587, 32.00000000000000000 ) ;
#8241=EDGE_CURVE ( 'NONE', #6805, #43019, #37379, .T. ) ;
#8242=CIRCLE ( 'NONE', #18406, 82.00000000000000000 ) ;
#8244=CIRCLE ( 'NONE', #16847, 82.00000000000000000 ) ;
#8252=EDGE_CURVE ( 'NONE', #10514, #29685, #20179, .T. ) ;
#8254=ADVANCED_FACE ( 'NONE', ( #31528 ), #1165, .T. ) ;
#8259=CIRCLE ( 'NONE', #41874, 82.00000000000000000 ) ;
#8260=ORIENTED_EDGE ( 'NONE', *, *, #46212, .T. ) ;
#8261=ORIENTED_EDGE ( 'NONE', *, *, #13856, .T. ) ;
#8264=ORIENTED_EDGE ( 'NONE', *, *, #4491, .T. ) ;
#8272=DIRECTION ( 'NONE',  ( -1.000000000000000000, -0.000000000000000000, -0.000000000000000000 ) ) ;
#8273=VERTEX_POINT ( 'NONE', #45963 ) ;
#8277=AXIS2_PLACEMENT_3D ( 'NONE', #11625, #45158, #4292 ) ;
#8279=ORIENTED_EDGE ( 'NONE', *, *, #34927, .T. ) ;
#8281=DIRECTION ( 'NONE',  ( 0.000000000000000000, 0.000000000000000000, 1.000000000000000000 ) ) ;
#8283=CARTESIAN_POINT ( 'NONE',  ( 0.000000000000000000, 0.000000000000000000, 0.000000000000000000 ) ) ;
#8287=ORIENTED_EDGE ( 'NONE', *, *, #41130, .F. ) ;
#8288=CYLINDRICAL_SURFACE ( 'NONE', #3182, 77.49899999999999523 ) ;
#8290=DIRECTION ( 'NONE',  ( -1.000000000000000000, -0.000000000000000000, 0.000000000000000000 ) ) ;
#8292=DIRECTION ( 'NONE',  ( -1.000000000000000000, 0.000000000000000000, 0.000000000000000000 ) ) ;
#8293=ORIENTED_EDGE ( 'NONE', *, *, #44474, .F. ) ;
#8295=DIRECTION ( 'NONE',  ( 0.000000000000000000, -0.3090169943749548342, 0.9510565162951510887 ) ) ;
#8299=CIRCLE ( 'NONE', #46608, 32.00000000000000000 ) ;
#8303=FACE_OUTER_BOUND ( 'NONE', #39962, .T. ) ;
#8307=AXIS2_PLACEMENT_3D ( 'NONE', #13067, #17430, #6201 ) ;
#8310=DIRECTION ( 'NONE',  ( 0.000000000000000000, 0.000000000000000000, 1.000000000000000000 ) ) ;
#8320=ORIENTED_EDGE ( 'NONE', *, *, #15276, .T. ) ;
#8321=CIRCLE ( 'NONE', #4421, 82.00000000000000000 ) ;
#8323=ORIENTED_EDGE ( 'NONE', *, *, #10407, .F. ) ;
#8330=CARTESIAN_POINT ( 'NONE',  ( 10.00000000000000000, -46.21855187248583974, -62.20884554314070414 ) ) ;
#8335=CARTESIAN_POINT ( 'NONE',  ( 10.00000000000000000, -77.16300072079640415, -27.74655509720751567 ) ) ;
#8342=DIRECTION ( 'NONE',  ( -1.000000000000000000, 0.000000000000000000, 0.000000000000000000 ) ) ;
#8350=ORIENTED_EDGE ( 'NONE', *, *, #21488, .T. ) ;
#8355=DIRECTION ( 'NONE',  ( 1.000000000000000000, -0.000000000000000000, -0.000000000000000000 ) ) ;
#8359=AXIS2_PLACEMENT_3D ( 'NONE', #39376, #31080, #38902 ) ;
#8361=ORIENTED_EDGE ( 'NONE', *, *, #47210, .T. ) ;
#8367=ORIENTED_EDGE ( 'NONE', *, *, #11208, .F. ) ;
#8378=CARTESIAN_POINT ( 'NONE',  ( 0.000000000000000000, -36.72794159290197769, -65.59268652807249111 ) ) ;
#8379=CYLINDRICAL_SURFACE ( 'NONE', #32316, 31.99999999999999289 ) ;
#8380=ORIENTED_EDGE ( 'NONE', *, *, #32603, .T. ) ;
#8381=CIRCLE ( 'NONE', #2890, 31.99999999999999289 ) ;
#8382=DIRECTION ( 'NONE',  ( 0.000000000000000000, 0.000000000000000000, 1.000000000000000000 ) ) ;
#8383=ORIENTED_EDGE ( 'NONE', *, *, #24710, .T. ) ;
#8384=AXIS2_PLACEMENT_3D ( 'NONE', #42755, #9207, #31257 ) ;
#8385=DIRECTION ( 'NONE',  ( 0.000000000000000000, -0.8090169943749403458, -0.5877852522924830181 ) ) ;
#8386=ORIENTED_EDGE ( 'NONE', *, *, #197, .T. ) ;
#8388=DIRECTION ( 'NONE',  ( -1.000000000000000000, -0.000000000000000000, -0.000000000000000000 ) ) ;
#8393=ADVANCED_FACE ( 'NONE', ( #2594 ), #17534, .T. ) ;
#8397=ADVANCED_FACE ( 'NONE', ( #28800 ), #43731, .T. ) ;
#8402=EDGE_LOOP ( 'NONE', ( #19914, #40047, #5077, #6636 ) ) ;
#8408=DIRECTION ( 'NONE',  ( -1.000000000000000000, -0.000000000000000000, -0.000000000000000000 ) ) ;
#8411=LINE ( 'NONE', #23573, #43307 ) ;
#8413=CARTESIAN_POINT ( 'NONE',  ( 10.00000000000000000, 0.000000000000000000, 0.000000000000000000 ) ) ;
#8416=CARTESIAN_POINT ( 'NONE',  ( 10.00000000000000000, 55.19960302592066625, 51.03279382321107249 ) ) ;
#8422=CARTESIAN_POINT ( 'NONE',  ( 10.00000000000000000, 66.50666863322055633, -39.78640506895536078 ) ) ;
#8423=ORIENTED_EDGE ( 'NONE', *, *, #32008, .F. ) ;
#8426=DIRECTION ( 'NONE',  ( -1.000000000000000000, 0.000000000000000000, -0.000000000000000000 ) ) ;
#8432=ADVANCED_FACE ( 'NONE', ( #22177 ), #15555, .T. ) ;
#8434=EDGE_LOOP ( 'NONE', ( #17523, #46083, #6402, #47218, #19111, #43637, #34686, #29647, #22538, #1641, #7724, #10375, #5394, #36918, #17700, #40728, #26200, #1189, #8617, #34568, #9362, #25688, #28181, #2402, #43059, #32336, #8323, #35498, #42089, #12021, #11587, #5130, #7314, #39887, #46268, #25883, #9175, #21205, #17601, #28588, #20291, #17406, #1239, #2479, #38150, #32126, #37596, #41427, #42341, #3883, #42725, #19263, #3494, #19684, #18855, #47992, #24583, #39047, #40469, #40777, #19324, #47995, #32169, #37818, #4065, #4665, #17278, #3303, #5253, #38823, #47398, #32335, #4376, #26416, #47241, #32661, #15823, #13084, #4782, #37494, #45283, #18438, #15490, #40917, #42833, #40029, #19484, #26788, #30192, #44671, #47812, #23988, #19922, #13140, #18770, #29056, #1205, #7294, #24171, #19175, #23295, #22198, #43149, #25782, #46357, #47408, #35378, #25750, #8012, #14972, #7504, #24443, #35167, #34441, #5858, #44638, #16055, #36665, #23729, #29074, #40853, #34950, #31261, #5456, #34424, #1057, #16191, #2523, #43076, #2846, #7366, #35581, #39237, #43624, #14883, #37713, #17417, #14047, #41876, #2765, #21563, #22414, #46686, #15317, #24003, #19952, #1845, #1023, #29624, #32813, #7956, #16415, #3879, #26384, #4671, #23438, #19024, #46354, #5279, #17764, #44673, #40059, #20673, #40405, #27975, #46900, #46701, #13386, #23291, #12144, #34353, #36622, #41320, #7889, #12363, #36369, #26931, #12795, #31160, #5667, #33295, #33130, #1042, #6645, #19052, #6345, #3732, #35971, #3850, #28919, #4584, #26461, #5989, #26597, #4669, #3326, #10241, #2573, #43373, #40509, #36196, #16390, #1471, #25501, #32535, #3681, #43547, #42416, #44523, #27112, #9691, #5759, #40443, #1253, #45451, #34294, #45846, #12674, #15385, #24956, #20296, #23840, #3492, #34771, #24380, #43123, #28993, #38811, #8293, #40160, #23604, #17078, #12215, #46452, #28251, #32235, #36088, #6272, #35803, #36499, #31388, #12534, #5337, #21923, #14055, #5230, #16563, #32738, #34574, #20443, #29327, #44881, #48240, #24731, #12076, #46142, #47090, #12668, #42679, #20393, #15939, #42155, #2411, #23885, #5011, #44435, #45831, #37300, #47629, #40442, #43380, #21435, #23507, #19447, #45849, #9243, #9528, #33403, #22445, #25766, #11640, #40477, #20293, #45385, #34255, #42726, #2972, #13106, #523, #37690, #19275, #42353, #4616, #17653, #25182, #4126, #24322, #11561, #11925, #15806, #14836, #8927, #42100, #46016, #9034, #25118, #12592, #45062, #18782, #48345, #12204, #35723, #47149, #22484, #46369, #29545, #28970, #23637, #41311, #21513, #41692, #26124, #24750, #38004, #14767 ) ) ;
#8435=AXIS2_PLACEMENT_3D ( 'NONE', #34787, #27459, #8834 ) ;
#8436=VERTEX_POINT ( 'NONE', #41752 ) ;
#8437=ORIENTED_EDGE ( 'NONE', *, *, #22763, .T. ) ;
#8463=CARTESIAN_POINT ( 'NONE',  ( 10.00000000000000000, -46.11716303203136391, -67.80270845531937596 ) ) ;
#8464=DIRECTION ( 'NONE',  ( -1.000000000000000000, 0.000000000000000000, 0.000000000000000000 ) ) ;
#8489=VERTEX_POINT ( 'NONE', #8212 ) ;
#8491=ORIENTED_EDGE ( 'NONE', *, *, #29950, .F. ) ;
#8492=VECTOR ( 'NONE', #11027, 1000.000000000000000 ) ;
#8493=EDGE_CURVE ( 'NONE', #33708, #1101, #31140, .T. ) ;
#8494=CARTESIAN_POINT ( 'NONE',  ( 10.00000000000000000, 0.000000000000000000, 0.000000000000000000 ) ) ;
#8499=EDGE_CURVE ( 'NONE', #33124, #2120, #30737, .T. ) ;
#8505=CYLINDRICAL_SURFACE ( 'NONE', #47399, 32.00000000000000000 ) ;
#8508=ADVANCED_FACE ( 'NONE', ( #37589 ), #14841, .T. ) ;
#8512=EDGE_CURVE ( 'NONE', #33790, #39605, #26442, .T. ) ;
#8514=CARTESIAN_POINT ( 'NONE',  ( 10.00000000000000000, 8.830959090343430518, -74.65491531819107252 ) ) ;
#8521=CARTESIAN_POINT ( 'NONE',  ( 10.00000000000000000, 39.78640506895700213, -66.50666863321957578 ) ) ;
#8522=VERTEX_POINT ( 'NONE', #30009 ) ;
#8524=ADVANCED_FACE ( 'NONE', ( #386 ), #33664, .T. ) ;
#8526=DIRECTION ( 'NONE',  ( 0.000000000000000000, -0.3090169943749349613, -0.9510565162951576390 ) ) ;
#8527=DIRECTION ( 'NONE',  ( -1.000000000000000000, -0.000000000000000000, 0.000000000000000000 ) ) ;
#8539=CIRCLE ( 'NONE', #39063, 77.49900000000000944 ) ;
#8542=EDGE_CURVE ( 'NONE', #31426, #29904, #38987, .T. ) ;
#8554=EDGE_CURVE ( 'NONE', #17812, #22693, #34878, .T. ) ;
#8555=CIRCLE ( 'NONE', #26561, 31.99999999999999289 ) ;
#8562=AXIS2_PLACEMENT_3D ( 'NONE', #32929, #3302, #9947 ) ;
#8563=LINE ( 'NONE', #45794, #1967 ) ;
#8564=DIRECTION ( 'NONE',  ( -1.000000000000000000, 0.000000000000000000, -0.000000000000000000 ) ) ;
#8566=AXIS2_PLACEMENT_3D ( 'NONE', #11441, #22446, #15097 ) ;
#8569=EDGE_CURVE ( 'NONE', #24221, #45052, #25647, .T. ) ;
#8576=EDGE_LOOP ( 'NONE', ( #47107, #22613, #2916, #19950 ) ) ;
#8578=DIRECTION ( 'NONE',  ( 0.000000000000000000, 0.7604059656000276002, 0.6494480483301876550 ) ) ;
#8590=CARTESIAN_POINT ( 'NONE',  ( -10.00000000000000000, 0.000000000000000000, 0.000000000000000000 ) ) ;
#8592=LINE ( 'NONE', #5192, #30373 ) ;
#8593=ORIENTED_EDGE ( 'NONE', *, *, #41506, .F. ) ;
#8600=DIRECTION ( 'NONE',  ( -1.000000000000000000, -0.000000000000000000, 0.000000000000000000 ) ) ;
#8603=DIRECTION ( 'NONE',  ( -1.000000000000000000, -0.000000000000000000, 0.000000000000000000 ) ) ;
#8605=ORIENTED_EDGE ( 'NONE', *, *, #29405, .F. ) ;
#8609=ORIENTED_EDGE ( 'NONE', *, *, #13421, .T. ) ;
#8611=EDGE_CURVE ( 'NONE', #2989, #19224, #19395, .T. ) ;
#8614=CARTESIAN_POINT ( 'NONE',  ( 10.00000000000000000, 68.27212725128275395, -31.46837873495001503 ) ) ;
#8617=ORIENTED_EDGE ( 'NONE', *, *, #8979, .F. ) ;
#8620=DIRECTION ( 'NONE',  ( 0.000000000000000000, 0.2334453638558990907, 0.9723699203976781114 ) ) ;
#8629=EDGE_LOOP ( 'NONE', ( #33098, #26635, #46131, #20117 ) ) ;
#8641=CARTESIAN_POINT ( 'NONE',  ( 10.00000000000000000, -14.66109333815513160, 73.73191006444567108 ) ) ;
#8649=ORIENTED_EDGE ( 'NONE', *, *, #1281, .F. ) ;
#8650=ORIENTED_EDGE ( 'NONE', *, *, #38413, .T. ) ;
#8651=FACE_OUTER_BOUND ( 'NONE', #35846, .T. ) ;
#8653=VERTEX_POINT ( 'NONE', #38312 ) ;
#8658=ORIENTED_EDGE ( 'NONE', *, *, #42899, .T. ) ;
#8661=ADVANCED_FACE ( 'NONE', ( #45910 ), #19944, .F. ) ;
#8667=EDGE_LOOP ( 'NONE', ( #18612, #30705, #2496, #38149 ) ) ;
#8669=AXIS2_PLACEMENT_3D ( 'NONE', #31610, #13005, #16193 ) ;
#8671=EDGE_CURVE ( 'NONE', #28806, #27309, #35059, .T. ) ;
#8677=EDGE_LOOP ( 'NONE', ( #10822, #36712, #25684, #32910 ) ) ;
#8680=DIRECTION ( 'NONE',  ( 0.000000000000000000, 0.000000000000000000, 1.000000000000000000 ) ) ;
#8685=DIRECTION ( 'NONE',  ( -1.000000000000000000, -0.000000000000000000, 0.000000000000000000 ) ) ;
#8688=DIRECTION ( 'NONE',  ( -1.000000000000000000, 0.000000000000000000, 0.000000000000000000 ) ) ;
#8690=DIRECTION ( 'NONE',  ( -1.000000000000000000, 0.000000000000000000, 0.000000000000000000 ) ) ;
#8692=CYLINDRICAL_SURFACE ( 'NONE', #22156, 82.00000000000000000 ) ;
#8698=CARTESIAN_POINT ( 'NONE',  ( 10.00000000000000000, 0.000000000000000000, 0.000000000000000000 ) ) ;
#8699=DIRECTION ( 'NONE',  ( 1.000000000000000000, 0.000000000000000000, 0.000000000000000000 ) ) ;
#8714=ORIENTED_EDGE ( 'NONE', *, *, #34854, .T. ) ;
#8715=VECTOR ( 'NONE', #44168, 1000.000000000000000 ) ;
#8716=EDGE_CURVE ( 'NONE', #20085, #29267, #29575, .T. ) ;
#8718=ADVANCED_FACE ( 'NONE', ( #21146 ), #14291, .T. ) ;
#8721=DIRECTION ( 'NONE',  ( 0.000000000000000000, 0.000000000000000000, 1.000000000000000000 ) ) ;
#8723=EDGE_CURVE ( 'NONE', #13379, #46560, #15536, .T. ) ;
#8725=VERTEX_POINT ( 'NONE', #44158 ) ;
#8726=ADVANCED_FACE ( 'NONE', ( #2539 ), #35841, .T. ) ;
#8727=ORIENTED_EDGE ( 'NONE', *, *, #19769, .F. ) ;
#8735=ORIENTED_EDGE ( 'NONE', *, *, #25170, .T. ) ;
#8744=ORIENTED_EDGE ( 'NONE', *, *, #20169, .T. ) ;
#8745=ORIENTED_EDGE ( 'NONE', *, *, #33379, .T. ) ;
#8750=FACE_OUTER_BOUND ( 'NONE', #18319, .T. ) ;
#8751=VECTOR ( 'NONE', #21262, 1000.000000000000000 ) ;
#8763=ORIENTED_EDGE ( 'NONE', *, *, #35644, .T. ) ;
#8764=CYLINDRICAL_SURFACE ( 'NONE', #13679, 82.00000000000000000 ) ;
#8765=LINE ( 'NONE', #23702, #23191 ) ;
#8775=CARTESIAN_POINT ( 'NONE',  ( 5.000000000000000000, -55.16347631943085617, 60.67117009219118273 ) ) ;
#8779=CARTESIAN_POINT ( 'NONE',  ( 5.000000000000002665, 16.65972982745046238, -80.28980883073738539 ) ) ;
#8783=EDGE_CURVE ( 'NONE', #17824, #18426, #27245, .T. ) ;
#8786=ORIENTED_EDGE ( 'NONE', *, *, #11684, .F. ) ;
#8796=DIRECTION ( 'NONE',  ( 0.000000000000000000, -0.4539904997395350916, -0.8910065241883738940 ) ) ;
#8799=DIRECTION ( 'NONE',  ( -1.000000000000000000, -0.000000000000000000, -0.000000000000000000 ) ) ;
#8803=AXIS2_PLACEMENT_3D ( 'NONE', #8283, #19043, #33976 ) ;
#8812=VERTEX_POINT ( 'NONE', #25057 ) ;
#8813=AXIS2_PLACEMENT_3D ( 'NONE', #22130, #18462, #7686 ) ;
#8823=FACE_OUTER_BOUND ( 'NONE', #1033, .T. ) ;
#8827=CARTESIAN_POINT ( 'NONE',  ( 10.00000000000000000, 73.72996012237440766, 14.67089635893739619 ) ) ;
#8829=CYLINDRICAL_SURFACE ( 'NONE', #30981, 82.00000000000000000 ) ;
#8834=DIRECTION ( 'NONE',  ( 0.000000000000000000, -0.3826834323650969427, 0.9238795325112838519 ) ) ;
#8835=AXIS2_PLACEMENT_3D ( 'NONE', #19078, #3174, #18105 ) ;
#8837=CARTESIAN_POINT ( 'NONE',  ( 0.000000000000000000, -2.956366410621191765, 75.11725578898467859 ) ) ;
#8840=ADVANCED_FACE ( 'NONE', ( #21641 ), #13571, .T. ) ;
#8841=CIRCLE ( 'NONE', #27615, 31.99999999999999289 ) ;
#8852=AXIS2_PLACEMENT_3D ( 'NONE', #12406, #9929, #42983 ) ;
#8854=AXIS2_PLACEMENT_3D ( 'NONE', #17708, #16753, #6223 ) ;
#8857=DIRECTION ( 'NONE',  ( -1.000000000000000000, -0.000000000000000000, -0.000000000000000000 ) ) ;
#8861=CARTESIAN_POINT ( 'NONE',  ( 0.000000000000000000, -73.95703589263990807, 23.16143007188399139 ) ) ;
#8871=EDGE_CURVE ( 'NONE', #22698, #3669, #6145, .T. ) ;
#8884=ADVANCED_FACE ( 'NONE', ( #3757 ), #33607, .T. ) ;
#8890=ADVANCED_FACE ( 'NONE', ( #19396 ), #30203, .T. ) ;
#8892=FACE_OUTER_BOUND ( 'NONE', #25756, .T. ) ;
#8894=LINE ( 'NONE', #27032, #34050 ) ;
#8897=CARTESIAN_POINT ( 'NONE',  ( 0.000000000000000000, 5.256550761632864166, 77.32052557432842832 ) ) ;
#8899=CIRCLE ( 'NONE', #13579, 82.00000000000000000 ) ;
#8906=EDGE_CURVE ( 'NONE', #10059, #38187, #37857, .T. ) ;
#8911=ORIENTED_EDGE ( 'NONE', *, *, #9427, .T. ) ;
#8917=ORIENTED_EDGE ( 'NONE', *, *, #44607, .T. ) ;
#8918=ORIENTED_EDGE ( 'NONE', *, *, #4588, .F. ) ;
#8920=AXIS2_PLACEMENT_3D ( 'NONE', #30043, #44000, #14872 ) ;
#8927=ORIENTED_EDGE ( 'NONE', *, *, #22610, .F. ) ;
#8929=VERTEX_POINT ( 'NONE', #26024 ) ;
#8933=CARTESIAN_POINT ( 'NONE',  ( 10.00000000000000000, -44.99326035066101781, 68.55367621811129197 ) ) ;
#8934=CARTESIAN_POINT ( 'NONE',  ( 10.00000000000000000, -74.65374052328644439, -8.840884882375878107 ) ) ;
#8941=DIRECTION ( 'NONE',  ( 0.000000000000000000, 0.000000000000000000, 1.000000000000000000 ) ) ;
#8948=LINE ( 'NONE', #39054, #47903 ) ;
#8951=ORIENTED_EDGE ( 'NONE', *, *, #27096, .T. ) ;
#8953=CARTESIAN_POINT ( 'NONE',  ( 0.000000000000000000, 20.41045688087824317, 72.35160999960824313 ) ) ;
#8955=LINE ( 'NONE', #1864, #1178 ) ;
#8958=DIRECTION ( 'NONE',  ( 0.000000000000000000, 0.3826834323650907810, -0.9238795325112864054 ) ) ;
#8970=EDGE_CURVE ( 'NONE', #2830, #1792, #45567, .T. ) ;
#8972=AXIS2_PLACEMENT_3D ( 'NONE', #44240, #18996, #22678 ) ;
#8979=EDGE_CURVE ( 'NONE', #11742, #708, #22239, .T. ) ;
#8986=DIRECTION ( 'NONE',  ( 0.000000000000000000, 0.3826834323650841752, 0.9238795325112891810 ) ) ;
#8988=DIRECTION ( 'NONE',  ( -1.000000000000000000, 0.000000000000000000, 0.000000000000000000 ) ) ;
#8989=ORIENTED_EDGE ( 'NONE', *, *, #43655, .T. ) ;
#8992=DIRECTION ( 'NONE',  ( 0.000000000000000000, 0.000000000000000000, 1.000000000000000000 ) ) ;
#8997=VECTOR ( 'NONE', #6982, 1000.000000000000000 ) ;
#8998=ORIENTED_EDGE ( 'NONE', *, *, #8079, .T. ) ;
#9002=FACE_OUTER_BOUND ( 'NONE', #35009, .T. ) ;
#9003=FACE_OUTER_BOUND ( 'NONE', #7835, .T. ) ;
#9006=CIRCLE ( 'NONE', #36361, 31.99999999999998934 ) ;
#9011=VECTOR ( 'NONE', #38323, 1000.000000000000000 ) ;
#9013=EDGE_CURVE ( 'NONE', #10088, #27708, #12845, .T. ) ;
#9015=ORIENTED_EDGE ( 'NONE', *, *, #40835, .F. ) ;
#9020=ADVANCED_FACE ( 'NONE', ( #23809 ), #31659, .T. ) ;
#9025=CYLINDRICAL_SURFACE ( 'NONE', #12851, 82.00000000000000000 ) ;
#9026=VECTOR ( 'NONE', #22011, 1000.000000000000000 ) ;
#9030=CIRCLE ( 'NONE', #18375, 31.99999999999999289 ) ;
#9034=ORIENTED_EDGE ( 'NONE', *, *, #23213, .F. ) ;
#9036=ORIENTED_EDGE ( 'NONE', *, *, #6152, .F. ) ;
#9039=CIRCLE ( 'NONE', #36391, 31.99999999999999289 ) ;
#9045=AXIS2_PLACEMENT_3D ( 'NONE', #14559, #85, #25550 ) ;
#9049=DIRECTION ( 'NONE',  ( 0.000000000000000000, 0.4539904997395477482, -0.8910065241883674547 ) ) ;
#9057=CARTESIAN_POINT ( 'NONE',  ( 0.000000000000000000, -46.54456581323762521, -59.03342792756313884 ) ) ;
#9058=ORIENTED_EDGE ( 'NONE', *, *, #34614, .F. ) ;
#9063=CARTESIAN_POINT ( 'NONE',  ( 10.00000000000000000, 0.000000000000000000, 0.000000000000000000 ) ) ;
#9064=EDGE_CURVE ( 'NONE', #37275, #42611, #18201, .T. ) ;
#9072=DIRECTION ( 'NONE',  ( 0.000000000000000000, 0.000000000000000000, 1.000000000000000000 ) ) ;
#9073=VERTEX_POINT ( 'NONE', #23322 ) ;
#9077=EDGE_CURVE ( 'NONE', #46520, #22527, #27701, .T. ) ;
#9092=AXIS2_PLACEMENT_3D ( 'NONE', #28719, #33093, #36295 ) ;
#9094=CARTESIAN_POINT ( 'NONE',  ( 0.000000000000000000, 0.000000000000000000, 0.000000000000000000 ) ) ;
#9098=FACE_OUTER_BOUND ( 'NONE', #13812, .T. ) ;
#9102=FACE_OUTER_BOUND ( 'NONE', #10221, .T. ) ;
#9110=( NAMED_UNIT ( * ) SI_UNIT ( $, .STERADIAN. ) SOLID_ANGLE_UNIT ( ) );
#9116=EDGE_CURVE ( 'NONE', #38558, #40145, #15739, .T. ) ;
#9117=CARTESIAN_POINT ( 'NONE',  ( 10.00000000000000000, 69.42325613327489009, -34.44570377933524696 ) ) ;
#9119=EDGE_CURVE ( 'NONE', #48250, #3237, #5834, .T. ) ;
#9128=VERTEX_POINT ( 'NONE', #19878 ) ;
#9137=LINE ( 'NONE', #19646, #3973 ) ;
#9141=CARTESIAN_POINT ( 'NONE',  ( 10.00000000000000000, 39.78640506895604290, 66.50666863322015843 ) ) ;
#9146=DIRECTION ( 'NONE',  ( -1.000000000000000000, 0.000000000000000000, -0.000000000000000000 ) ) ;
#9155=ORIENTED_EDGE ( 'NONE', *, *, #27304, .F. ) ;
#9160=EDGE_CURVE ( 'NONE', #24887, #48217, #4252, .T. ) ;
#9163=CARTESIAN_POINT ( 'NONE',  ( 5.000000000000000000, -33.71516098798685590, -74.74816331893465815 ) ) ;
#9165=ORIENTED_EDGE ( 'NONE', *, *, #19290, .F. ) ;
#9172=CIRCLE ( 'NONE', #28720, 77.49900000000000944 ) ;
#9175=ORIENTED_EDGE ( 'NONE', *, *, #15756, .F. ) ;
#9178=DIRECTION ( 'NONE',  ( 0.000000000000000000, -0.5224985647159379187, -0.8526401643540989506 ) ) ;
#9179=DIRECTION ( 'NONE',  ( -1.000000000000000000, 0.000000000000000000, -0.000000000000000000 ) ) ;
#9181=ORIENTED_EDGE ( 'NONE', *, *, #37677, .T. ) ;
#9187=LINE ( 'NONE', #24120, #11362 ) ;
#9188=CARTESIAN_POINT ( 'NONE',  ( 10.00000000000000000, -73.95703589263990807, 23.16143007188399139 ) ) ;
#9189=DIRECTION ( 'NONE',  ( -1.000000000000000000, -0.000000000000000000, 0.000000000000000000 ) ) ;
#9198=CARTESIAN_POINT ( 'NONE',  ( 10.00000000000000000, 68.26794271651262136, 31.47745569255165066 ) ) ;
#9201=CARTESIAN_POINT ( 'NONE',  ( 10.00000000000000000, 75.11764819372149304, -2.946379043146603482 ) ) ;
#9205=CARTESIAN_POINT ( 'NONE',  ( 10.00000000000000000, 8.830959090342393125, 74.65491531819122883 ) ) ;
#9206=VECTOR ( 'NONE', #25006, 1000.000000000000000 ) ;
#9207=DIRECTION ( 'NONE',  ( -1.000000000000000000, -0.000000000000000000, -0.000000000000000000 ) ) ;
#9212=CIRCLE ( 'NONE', #36559, 31.99999999999999289 ) ;
#9215=CARTESIAN_POINT ( 'NONE',  ( 10.00000000000000000, 51.02545421589402252, -55.20638768913705263 ) ) ;
#9220=VERTEX_POINT ( 'NONE', #25230 ) ;
#9223=VERTEX_POINT ( 'NONE', #36017 ) ;
#9227=CARTESIAN_POINT ( 'NONE',  ( 10.00000000000000000, -74.65491531819111515, -8.830959090343204920 ) ) ;
#9229=ORIENTED_EDGE ( 'NONE', *, *, #43837, .T. ) ;
#9231=ADVANCED_FACE ( 'NONE', ( #16946 ), #17409, .T. ) ;
#9236=DIRECTION ( 'NONE',  ( 0.000000000000000000, 0.000000000000000000, 1.000000000000000000 ) ) ;
#9237=ORIENTED_EDGE ( 'NONE', *, *, #29796, .F. ) ;
#9243=ORIENTED_EDGE ( 'NONE', *, *, #47891, .F. ) ;
#9244=AXIS2_PLACEMENT_3D ( 'NONE', #24176, #30808, #34945 ) ;
#9248=VECTOR ( 'NONE', #5561, 1000.000000000000000 ) ;
#9249=EDGE_LOOP ( 'NONE', ( #33005, #37416, #17371, #10781 ) ) ;
#9251=CYLINDRICAL_SURFACE ( 'NONE', #32889, 82.00000000000000000 ) ;
#9254=ORIENTED_EDGE ( 'NONE', *, *, #39396, .T. ) ;
#9255=CARTESIAN_POINT ( 'NONE',  ( 10.00000000000000000, -56.15606465354917987, -59.75363087400133111 ) ) ;
#9267=DIRECTION ( 'NONE',  ( 0.000000000000000000, 0.5224985647159500202, -0.8526401643540915121 ) ) ;
#9270=ORIENTED_EDGE ( 'NONE', *, *, #24636, .T. ) ;
#9277=AXIS2_PLACEMENT_3D ( 'NONE', #20190, #35111, #13099 ) ;
#9279=EDGE_CURVE ( 'NONE', #7784, #31833, #40128, .T. ) ;
#9285=ORIENTED_EDGE ( 'NONE', *, *, #16635, .F. ) ;
#9299=DIRECTION ( 'NONE',  ( 1.000000000000000000, -0.000000000000000000, 0.000000000000000000 ) ) ;
#9301=CARTESIAN_POINT ( 'NONE',  ( 10.00000000000000000, 0.000000000000000000, 0.000000000000000000 ) ) ;
#9308=VERTEX_POINT ( 'NONE', #22546 ) ;
#9317=EDGE_CURVE ( 'NONE', #11779, #45199, #29182, .T. ) ;
#9321=VERTEX_POINT ( 'NONE', #37476 ) ;
#9324=DIRECTION ( 'NONE',  ( -1.000000000000000000, 0.000000000000000000, 0.000000000000000000 ) ) ;
#9330=CARTESIAN_POINT ( 'NONE',  ( -10.00000000000000000, 0.000000000000000000, 0.000000000000000000 ) ) ;
#9334=EDGE_CURVE ( 'NONE', #19886, #43803, #1050, .T. ) ;
#9337=EDGE_CURVE ( 'NONE', #29279, #34549, #21810, .T. ) ;
#9338=VECTOR ( 'NONE', #25504, 1000.000000000000000 ) ;
#9344=( LENGTH_UNIT ( ) NAMED_UNIT ( * ) SI_UNIT ( .MILLI., .METRE. ) );
#9345=CARTESIAN_POINT ( 'NONE',  ( 0.000000000000000000, 44.99326035066149387, -68.55367621811095091 ) ) ;
#9349=DIRECTION ( 'NONE',  ( 1.000000000000000000, 0.000000000000000000, 0.000000000000000000 ) ) ;
#9352=VERTEX_POINT ( 'NONE', #3945 ) ;
#9356=CARTESIAN_POINT ( 'NONE',  ( 0.000000000000000000, 58.39081064771823293, -50.95692526931266286 ) ) ;
#9362=ORIENTED_EDGE ( 'NONE', *, *, #38916, .F. ) ;
#9363=DIRECTION ( 'NONE',  ( -1.000000000000000000, 0.000000000000000000, 0.000000000000000000 ) ) ;
#9367=CARTESIAN_POINT ( 'NONE',  ( 0.000000000000000000, 39.47590169984944453, -71.87247863392373404 ) ) ;
#9370=DIRECTION ( 'NONE',  ( 0.000000000000000000, 0.000000000000000000, 1.000000000000000000 ) ) ;
#9372=VECTOR ( 'NONE', #44771, 1000.000000000000000 ) ;
#9373=CIRCLE ( 'NONE', #44551, 31.99999999999999289 ) ;
#9376=CYLINDRICAL_SURFACE ( 'NONE', #31040, 32.00000000000000000 ) ;
#9377=AXIS2_PLACEMENT_3D ( 'NONE', #41868, #30124, #38422 ) ;
#9379=CYLINDRICAL_SURFACE ( 'NONE', #33895, 77.49899999999999523 ) ;
#9380=CIRCLE ( 'NONE', #36725, 31.99999999999999645 ) ;
#9386=CARTESIAN_POINT ( 'NONE',  ( 10.00000000000000000, -71.27951684758005513, -30.41916302227188851 ) ) ;
#9389=ORIENTED_EDGE ( 'NONE', *, *, #42255, .T. ) ;
#9397=CARTESIAN_POINT ( 'NONE',  ( -10.00000000000000000, 0.000000000000000000, 0.000000000000000000 ) ) ;
#9400=AXIS2_PLACEMENT_3D ( 'NONE', #25554, #17962, #40501 ) ;
#9401=CIRCLE ( 'NONE', #36763, 31.99999999999999645 ) ;
#9404=CARTESIAN_POINT ( 'NONE',  ( 10.00000000000000000, 0.000000000000000000, 0.000000000000000000 ) ) ;
#9405=ORIENTED_EDGE ( 'NONE', *, *, #2913, .F. ) ;
#9406=ORIENTED_EDGE ( 'NONE', *, *, #24489, .T. ) ;
#9409=CARTESIAN_POINT ( 'NONE',  ( 10.00000000000000000, 0.000000000000000000, 0.000000000000000000 ) ) ;
#9410=AXIS2_PLACEMENT_3D ( 'NONE', #1790, #42422, #1055 ) ;
#9414=CIRCLE ( 'NONE', #4745, 77.49900000000000944 ) ;
#9418=CARTESIAN_POINT ( 'NONE',  ( 0.000000000000000000, 71.91182617369187824, 28.89263327155772387 ) ) ;
#9422=CYLINDRICAL_SURFACE ( 'NONE', #31492, 77.49899999999999523 ) ;
#9424=DIRECTION ( 'NONE',  ( 1.000000000000000000, 0.000000000000000000, 0.000000000000000000 ) ) ;
#9427=EDGE_CURVE ( 'NONE', #44447, #4582, #48248, .T. ) ;
#9431=FACE_OUTER_BOUND ( 'NONE', #19223, .T. ) ;
#9433=EDGE_CURVE ( 'NONE', #5603, #42611, #13, .T. ) ;
#9437=DIRECTION ( 'NONE',  ( -1.000000000000000000, -0.000000000000000000, 0.000000000000000000 ) ) ;
#9440=ORIENTED_EDGE ( 'NONE', *, *, #317, .T. ) ;
#9441=DIRECTION ( 'NONE',  ( 0.000000000000000000, 0.000000000000000000, -1.000000000000000000 ) ) ;
#9444=EDGE_LOOP ( 'NONE', ( #34766, #16410, #35822, #4305 ) ) ;
#9445=EDGE_CURVE ( 'NONE', #36193, #30385, #23687, .T. ) ;
#9446=DIRECTION ( 'NONE',  ( 0.000000000000000000, 0.000000000000000000, 1.000000000000000000 ) ) ;
#9451=ORIENTED_EDGE ( 'NONE', *, *, #12425, .F. ) ;
#9454=ORIENTED_EDGE ( 'NONE', *, *, #40118, .F. ) ;
#9459=DIRECTION ( 'NONE',  ( -1.000000000000000000, 0.000000000000000000, 0.000000000000000000 ) ) ;
#9463=ORIENTED_EDGE ( 'NONE', *, *, #28954, .F. ) ;
#9464=DIRECTION ( 'NONE',  ( -1.000000000000000000, -0.000000000000000000, 0.000000000000000000 ) ) ;
#9470=EDGE_LOOP ( 'NONE', ( #31667, #7250, #45533, #44943 ) ) ;
#9472=ORIENTED_EDGE ( 'NONE', *, *, #43262, .T. ) ;
#9481=ORIENTED_EDGE ( 'NONE', *, *, #17819, .T. ) ;
#9482=EDGE_CURVE ( 'NONE', #26885, #31737, #23699, .T. ) ;
#9486=VERTEX_POINT ( 'NONE', #23946 ) ;
#9491=LINE ( 'NONE', #27623, #38704 ) ;
#9499=ORIENTED_EDGE ( 'NONE', *, *, #47840, .T. ) ;
#9502=DIRECTION ( 'NONE',  ( -1.000000000000000000, 0.000000000000000000, 0.000000000000000000 ) ) ;
#9503=DIRECTION ( 'NONE',  ( -1.000000000000000000, -0.000000000000000000, -0.000000000000000000 ) ) ;
#9505=EDGE_CURVE ( 'NONE', #38979, #10399, #24411, .T. ) ;
#9510=DIRECTION ( 'NONE',  ( 0.000000000000000000, 0.000000000000000000, 1.000000000000000000 ) ) ;
#9515=DIRECTION ( 'NONE',  ( -1.000000000000000000, -0.000000000000000000, -0.000000000000000000 ) ) ;
#9516=AXIS2_PLACEMENT_3D ( 'NONE', #6590, #10253, #40127 ) ;
#9517=VERTEX_POINT ( 'NONE', #38641 ) ;
#9519=VERTEX_POINT ( 'NONE', #35183 ) ;
#9524=ORIENTED_EDGE ( 'NONE', *, *, #6143, .F. ) ;
#9526=DIRECTION ( 'NONE',  ( -1.000000000000000000, -0.000000000000000000, -0.000000000000000000 ) ) ;
#9528=ORIENTED_EDGE ( 'NONE', *, *, #18463, .F. ) ;
#9531=AXIS2_PLACEMENT_3D ( 'NONE', #29725, #44422, #37070 ) ;
#9535=ORIENTED_EDGE ( 'NONE', *, *, #31745, .F. ) ;
#9537=DIRECTION ( 'NONE',  ( 0.000000000000000000, 0.5224985647159500202, -0.8526401643540915121 ) ) ;
#9539=ORIENTED_EDGE ( 'NONE', *, *, #2701, .F. ) ;
#9549=CARTESIAN_POINT ( 'NONE',  ( 10.00000000000000000, 2.956366410620650420, 75.11725578898469280 ) ) ;
#9550=LINE ( 'NONE', #46541, #4415 ) ;
#9551=VECTOR ( 'NONE', #7221, 1000.000000000000000 ) ;
#9553=FACE_OUTER_BOUND ( 'NONE', #39754, .T. ) ;
#9562=CIRCLE ( 'NONE', #43186, 82.00000000000000000 ) ;
#9572=CIRCLE ( 'NONE', #36170, 77.49899999999999523 ) ;
#9576=CARTESIAN_POINT ( 'NONE',  ( 5.000000000000000000, 67.80270845531956070, -46.11716303203112943 ) ) ;
#9580=CYLINDRICAL_SURFACE ( 'NONE', #21543, 32.00000000000000000 ) ;
#9588=DIRECTION ( 'NONE',  ( -1.000000000000000000, -0.000000000000000000, -0.000000000000000000 ) ) ;
#9590=CARTESIAN_POINT ( 'NONE',  ( 5.000000000000000000, 59.75363087400153006, -56.15606465354897381 ) ) ;
#9602=CARTESIAN_POINT ( 'NONE',  ( 10.00000000000000000, 0.000000000000000000, 0.000000000000000000 ) ) ;
#9605=AXIS2_PLACEMENT_3D ( 'NONE', #2451, #36227, #43582 ) ;
#9607=CARTESIAN_POINT ( 'NONE',  ( 10.00000000000000000, 0.8261519478431083030, 77.49459641780886443 ) ) ;
#9619=FACE_OUTER_BOUND ( 'NONE', #42705, .T. ) ;
#9624=DIRECTION ( 'NONE',  ( -1.000000000000000000, -0.000000000000000000, -0.000000000000000000 ) ) ;
#9630=ORIENTED_EDGE ( 'NONE', *, *, #17748, .F. ) ;
#9634=DIRECTION ( 'NONE',  ( -1.000000000000000000, 0.000000000000000000, 0.000000000000000000 ) ) ;
#9635=ORIENTED_EDGE ( 'NONE', *, *, #4805, .F. ) ;
#9637=VECTOR ( 'NONE', #29240, 1000.000000000000000 ) ;
#9641=ORIENTED_EDGE ( 'NONE', *, *, #23582, .T. ) ;
#9643=AXIS2_PLACEMENT_3D ( 'NONE', #17597, #10751, #7060 ) ;
#9651=AXIS2_PLACEMENT_3D ( 'NONE', #46959, #5855, #21004 ) ;
#9652=AXIS2_PLACEMENT_3D ( 'NONE', #47383, #17750, #5780 ) ;
#9657=AXIS2_PLACEMENT_3D ( 'NONE', #44586, #23041, #41180 ) ;
#9661=CARTESIAN_POINT ( 'NONE',  ( 10.00000000000000000, 0.000000000000000000, 0.000000000000000000 ) ) ;
#9665=CYLINDRICAL_SURFACE ( 'NONE', #37814, 82.00000000000000000 ) ;
#9666=AXIS2_PLACEMENT_3D ( 'NONE', #9894, #42459, #35103 ) ;
#9667=CARTESIAN_POINT ( 'NONE',  ( 10.00000000000000000, 0.000000000000000000, 0.000000000000000000 ) ) ;
#9668=DIRECTION ( 'NONE',  ( -1.000000000000000000, 0.000000000000000000, 0.000000000000000000 ) ) ;
#9673=CARTESIAN_POINT ( 'NONE',  ( 0.000000000000000000, 0.000000000000000000, 0.000000000000000000 ) ) ;
#9690=CARTESIAN_POINT ( 'NONE',  ( 10.00000000000000000, 41.76937507738875155, -62.50329211542393892 ) ) ;
#9691=ORIENTED_EDGE ( 'NONE', *, *, #8156, .F. ) ;
#9693=VECTOR ( 'NONE', #27899, 1000.000000000000000 ) ;
#9705=ORIENTED_EDGE ( 'NONE', *, *, #46405, .T. ) ;
#9710=AXIS2_PLACEMENT_3D ( 'NONE', #31367, #47003, #35015 ) ;
#9713=ORIENTED_EDGE ( 'NONE', *, *, #46259, .F. ) ;
#9719=LINE ( 'NONE', #16589, #38528 ) ;
#9720=CARTESIAN_POINT ( 'NONE',  ( 10.00000000000000000, 23.16143007188426850, 73.95703589263983702 ) ) ;
#9726=CYLINDRICAL_SURFACE ( 'NONE', #29750, 31.99999999999999289 ) ;
#9729=AXIS2_PLACEMENT_3D ( 'NONE', #47014, #42636, #28658 ) ;
#9738=DIRECTION ( 'NONE',  ( -1.000000000000000000, -0.000000000000000000, 0.000000000000000000 ) ) ;
#9743=ORIENTED_EDGE ( 'NONE', *, *, #18908, .T. ) ;
#9745=DIRECTION ( 'NONE',  ( -1.000000000000000000, 0.000000000000000000, -0.000000000000000000 ) ) ;
#9749=CARTESIAN_POINT ( 'NONE',  ( 0.000000000000000000, 0.000000000000000000, 0.000000000000000000 ) ) ;
#9756=CIRCLE ( 'NONE', #30100, 82.00000000000000000 ) ;
#9757=CIRCLE ( 'NONE', #23070, 31.99999999999999289 ) ;
#9760=ORIENTED_EDGE ( 'NONE', *, *, #36543, .F. ) ;
#9766=VERTEX_POINT ( 'NONE', #638 ) ;
#9772=DIRECTION ( 'NONE',  ( 0.000000000000000000, 0.000000000000000000, -1.000000000000000000 ) ) ;
#9774=CARTESIAN_POINT ( 'NONE',  ( 10.00000000000000000, 3.894527615417895383, 81.90746397400390322 ) ) ;
#9776=CARTESIAN_POINT ( 'NONE',  ( 10.00000000000000000, 0.000000000000000000, 0.000000000000000000 ) ) ;
#9780=ORIENTED_EDGE ( 'NONE', *, *, #22471, .T. ) ;
#9786=CIRCLE ( 'NONE', #12151, 77.49899999999999523 ) ;
#9788=ORIENTED_EDGE ( 'NONE', *, *, #3455, .T. ) ;
#9791=CIRCLE ( 'NONE', #37150, 77.49899999999999523 ) ;
#9794=DIRECTION ( 'NONE',  ( -1.000000000000000000, -0.000000000000000000, -0.000000000000000000 ) ) ;
#9800=CIRCLE ( 'NONE', #39516, 32.00000000000000000 ) ;
#9804=VECTOR ( 'NONE', #4026, 1000.000000000000000 ) ;
#9805=DIRECTION ( 'NONE',  ( -1.000000000000000000, -0.000000000000000000, -0.000000000000000000 ) ) ;
#9806=CARTESIAN_POINT ( 'NONE',  ( 0.000000000000000000, 0.000000000000000000, 0.000000000000000000 ) ) ;
#9807=DIRECTION ( 'NONE',  ( 0.000000000000000000, 0.9876883405951371042, 0.1564344650402347547 ) ) ;
#9819=ORIENTED_EDGE ( 'NONE', *, *, #40840, .T. ) ;
#9820=AXIS2_PLACEMENT_3D ( 'NONE', #16428, #17372, #46782 ) ;
#9821=EDGE_CURVE ( 'NONE', #15030, #28496, #34661, .T. ) ;
#9826=VERTEX_POINT ( 'NONE', #12160 ) ;
#9827=CARTESIAN_POINT ( 'NONE',  ( 10.00000000000000000, -71.87247863392443037, 39.47590169984818687 ) ) ;
#9828=EDGE_CURVE ( 'NONE', #24169, #45521, #13565, .T. ) ;
#9830=DIRECTION ( 'NONE',  ( -1.000000000000000000, 0.000000000000000000, 0.000000000000000000 ) ) ;
#9833=CARTESIAN_POINT ( 'NONE',  ( 10.00000000000000000, -20.40083707022829174, -72.35432306680507963 ) ) ;
#9834=VERTEX_POINT ( 'NONE', #41285 ) ;
#9844=DIRECTION ( 'NONE',  ( 0.000000000000000000, -0.6494480483301741103, -0.7604059656000390355 ) ) ;
#9847=DIRECTION ( 'NONE',  ( -1.000000000000000000, -0.000000000000000000, -0.000000000000000000 ) ) ;
#9852=DIRECTION ( 'NONE',  ( -1.000000000000000000, -0.000000000000000000, 0.000000000000000000 ) ) ;
#9853=AXIS2_PLACEMENT_3D ( 'NONE', #23641, #34178, #4806 ) ;
#9857=CARTESIAN_POINT ( 'NONE',  ( 10.00000000000000000, 59.46389618802034960, -49.70050353004825894 ) ) ;
#9861=CARTESIAN_POINT ( 'NONE',  ( 10.00000000000000000, 8.830959090342393125, 74.65491531819122883 ) ) ;
#9864=DIRECTION ( 'NONE',  ( -1.000000000000000000, -0.000000000000000000, 0.000000000000000000 ) ) ;
#9865=ORIENTED_EDGE ( 'NONE', *, *, #35820, .F. ) ;
#9866=CARTESIAN_POINT ( 'NONE',  ( 0.000000000000000000, 12.93880638057426502, -76.41127070299258150 ) ) ;
#9869=CARTESIAN_POINT ( 'NONE',  ( 10.00000000000000000, -24.73286445877653961, -73.44644590900085745 ) ) ;
#9870=CYLINDRICAL_SURFACE ( 'NONE', #46308, 31.99999999999998579 ) ;
#9874=ORIENTED_EDGE ( 'NONE', *, *, #37986, .T. ) ;
#9879=AXIS2_PLACEMENT_3D ( 'NONE', #43579, #21050, #5655 ) ;
#9894=CARTESIAN_POINT ( 'NONE',  ( 0.000000000000000000, 0.000000000000000000, 0.000000000000000000 ) ) ;
#9895=EDGE_CURVE ( 'NONE', #36949, #45729, #19800, .T. ) ;
#9896=DIRECTION ( 'NONE',  ( 0.000000000000000000, 0.000000000000000000, 1.000000000000000000 ) ) ;
#9903=CARTESIAN_POINT ( 'NONE',  ( 0.000000000000000000, 0.000000000000000000, 0.000000000000000000 ) ) ;
#9904=LINE ( 'NONE', #44159, #44241 ) ;
#9907=AXIS2_PLACEMENT_3D ( 'NONE', #30491, #16056, #18976 ) ;
#9912=DIRECTION ( 'NONE',  ( -1.000000000000000000, 0.000000000000000000, -0.000000000000000000 ) ) ;
#9915=CARTESIAN_POINT ( 'NONE',  ( 10.00000000000000000, 71.87247863392413194, 39.47590169984869135 ) ) ;
#9916=DIRECTION ( 'NONE',  ( -1.000000000000000000, -0.000000000000000000, 0.000000000000000000 ) ) ;
#9918=DIRECTION ( 'NONE',  ( -1.000000000000000000, 0.000000000000000000, -0.000000000000000000 ) ) ;
#9921=CARTESIAN_POINT ( 'NONE',  ( 0.000000000000000000, -71.91182617369166508, -28.89263327155821770 ) ) ;
#9926=VERTEX_POINT ( 'NONE', #35369 ) ;
#9929=DIRECTION ( 'NONE',  ( -1.000000000000000000, 0.000000000000000000, 0.000000000000000000 ) ) ;
#9932=CIRCLE ( 'NONE', #4483, 77.49899999999998101 ) ;
#9933=EDGE_CURVE ( 'NONE', #7367, #42453, #31965, .T. ) ;
#9937=LINE ( 'NONE', #24859, #19129 ) ;
#9944=EDGE_LOOP ( 'NONE', ( #23082, #8649, #40611, #17050 ) ) ;
#9947=DIRECTION ( 'NONE',  ( 0.000000000000000000, -0.9510565162951499785, -0.3090169943749582204 ) ) ;
#9950=VERTEX_POINT ( 'NONE', #38574 ) ;
#9951=AXIS2_PLACEMENT_3D ( 'NONE', #26977, #7871, #19366 ) ;
#9952=ADVANCED_FACE ( 'NONE', ( #28267 ), #39052, .T. ) ;
#9954=DIRECTION ( 'NONE',  ( -1.000000000000000000, 0.000000000000000000, 0.000000000000000000 ) ) ;
#9963=ORIENTED_EDGE ( 'NONE', *, *, #19467, .F. ) ;
#9968=DIRECTION ( 'NONE',  ( -1.000000000000000000, 0.000000000000000000, 0.000000000000000000 ) ) ;
#9972=CARTESIAN_POINT ( 'NONE',  ( 10.00000000000000000, 75.11764819372149304, 29.05362095685338986 ) ) ;
#9976=CARTESIAN_POINT ( 'NONE',  ( 0.000000000000000000, 0.000000000000000000, 0.000000000000000000 ) ) ;
#9980=CARTESIAN_POINT ( 'NONE',  ( 10.00000000000000000, 12.93880638057426502, -76.41127070299258150 ) ) ;
#9998=EDGE_CURVE ( 'NONE', #29279, #17516, #11269, .T. ) ;
#9999=CARTESIAN_POINT ( 'NONE',  ( 10.00000000000000000, 63.18004540533029001, 44.88180994100400767 ) ) ;
#10005=CIRCLE ( 'NONE', #6871, 32.00000000000000000 ) ;
#10008=EDGE_CURVE ( 'NONE', #27618, #26885, #46159, .T. ) ;
#10009=VERTEX_POINT ( 'NONE', #28043 ) ;
#10021=EDGE_LOOP ( 'NONE', ( #15617, #1885, #38367, #27965 ) ) ;
#10022=CYLINDRICAL_SURFACE ( 'NONE', #47756, 32.00000000000000000 ) ;
#10023=VERTEX_POINT ( 'NONE', #1608 ) ;
#10024=AXIS2_PLACEMENT_3D ( 'NONE', #15712, #30644, #45558 ) ;
#10026=CARTESIAN_POINT ( 'NONE',  ( 10.00000000000000000, 0.000000000000000000, 0.000000000000000000 ) ) ;
#10027=EDGE_LOOP ( 'NONE', ( #34751, #5204, #31875, #26669 ) ) ;
#10036=CARTESIAN_POINT ( 'NONE',  ( 10.00000000000000000, -31.47745569255092235, -68.26794271651296242 ) ) ;
#10040=DIRECTION ( 'NONE',  ( 0.000000000000000000, 0.2334453638559058908, -0.9723699203976764460 ) ) ;
#10041=EDGE_CURVE ( 'NONE', #39882, #10420, #2350, .T. ) ;
#10046=CARTESIAN_POINT ( 'NONE',  ( 0.000000000000000000, 0.000000000000000000, 0.000000000000000000 ) ) ;
#10049=EDGE_CURVE ( 'NONE', #690, #17289, #13410, .T. ) ;
#10056=ORIENTED_EDGE ( 'NONE', *, *, #37699, .T. ) ;
#10058=DIRECTION ( 'NONE',  ( 0.000000000000000000, 0.000000000000000000, 1.000000000000000000 ) ) ;
#10059=VERTEX_POINT ( 'NONE', #17239 ) ;
#10063=ORIENTED_EDGE ( 'NONE', *, *, #7305, .T. ) ;
#10068=CYLINDRICAL_SURFACE ( 'NONE', #22723, 31.99999999999999289 ) ;
#10070=VERTEX_POINT ( 'NONE', #36809 ) ;
#10071=CARTESIAN_POINT ( 'NONE',  ( 0.000000000000000000, -75.11725578898470701, 2.956366410620372864 ) ) ;
#10074=DIRECTION ( 'NONE',  ( -1.000000000000000000, 0.000000000000000000, 0.000000000000000000 ) ) ;
#10075=ORIENTED_EDGE ( 'NONE', *, *, #47559, .T. ) ;
#10081=CARTESIAN_POINT ( 'NONE',  ( 0.000000000000000000, -54.21277698773636899, -55.38113227695839669 ) ) ;
#10083=EDGE_LOOP ( 'NONE', ( #48110, #12964, #29712, #17525 ) ) ;
#10086=CARTESIAN_POINT ( 'NONE',  ( 5.000000000000002665, -76.69515212746036070, 29.01471420065537643 ) ) ;
#10087=ORIENTED_EDGE ( 'NONE', *, *, #32887, .T. ) ;
#10088=VERTEX_POINT ( 'NONE', #9915 ) ;
#10098=CARTESIAN_POINT ( 'NONE',  ( 10.00000000000000000, 0.000000000000000000, 0.000000000000000000 ) ) ;
#10106=FACE_OUTER_BOUND ( 'NONE', #17070, .T. ) ;
#10114=VECTOR ( 'NONE', #41183, 1000.000000000000000 ) ;
#10123=EDGE_CURVE ( 'NONE', #38585, #33302, #7839, .T. ) ;
#10128=ORIENTED_EDGE ( 'NONE', *, *, #24401, .F. ) ;
#10141=VECTOR ( 'NONE', #36075, 1000.000000000000000 ) ;
#10143=VERTEX_POINT ( 'NONE', #10389 ) ;
#10146=AXIS2_PLACEMENT_3D ( 'NONE', #33536, #25209, #32578 ) ;
#10150=DIRECTION ( 'NONE',  ( 0.000000000000000000, 0.000000000000000000, 1.000000000000000000 ) ) ;
#10158=AXIS2_PLACEMENT_3D ( 'NONE', #2038, #39721, #16714 ) ;
#10161=DIRECTION ( 'NONE',  ( -1.000000000000000000, 0.000000000000000000, 0.000000000000000000 ) ) ;
#10162=DIRECTION ( 'NONE',  ( -1.000000000000000000, 0.000000000000000000, 0.000000000000000000 ) ) ;
#10163=CARTESIAN_POINT ( 'NONE',  ( 0.000000000000000000, -3.894527615418464705, 81.90746397400387480 ) ) ;
#10167=EDGE_CURVE ( 'NONE', #28423, #48250, #16447, .T. ) ;
#10172=EDGE_CURVE ( 'NONE', #32236, #33332, #10645, .T. ) ;
#10177=ORIENTED_EDGE ( 'NONE', *, *, #31969, .T. ) ;
#10178=CIRCLE ( 'NONE', #16441, 31.99999999999999289 ) ;
#10185=ORIENTED_EDGE ( 'NONE', *, *, #47774, .F. ) ;
#10189=CARTESIAN_POINT ( 'NONE',  ( 10.00000000000000000, 50.95692526931328104, 58.39081064771769292 ) ) ;
#10194=CARTESIAN_POINT ( 'NONE',  ( -10.00000000000000000, 0.000000000000000000, 0.000000000000000000 ) ) ;
#10201=ORIENTED_EDGE ( 'NONE', *, *, #1665, .F. ) ;
#10208=DIRECTION ( 'NONE',  ( -1.000000000000000000, 0.000000000000000000, 0.000000000000000000 ) ) ;
#10211=EDGE_CURVE ( 'NONE', #10070, #19886, #28948, .T. ) ;
#10216=CARTESIAN_POINT ( 'NONE',  ( 10.00000000000000000, 34.94270380257741948, -74.18225833017854143 ) ) ;
#10217=DIRECTION ( 'NONE',  ( -1.000000000000000000, 0.000000000000000000, 0.000000000000000000 ) ) ;
#10220=CIRCLE ( 'NONE', #47, 31.99999999999999289 ) ;
#10221=EDGE_LOOP ( 'NONE', ( #32229, #31143, #14541, #18015 ) ) ;
#10225=AXIS2_PLACEMENT_3D ( 'NONE', #27616, #43269, #12451 ) ;
#10230=ORIENTED_EDGE ( 'NONE', *, *, #893, .T. ) ;
#10235=ORIENTED_EDGE ( 'NONE', *, *, #37463, .T. ) ;
#10236=EDGE_CURVE ( 'NONE', #37895, #32575, #22694, .T. ) ;
#10237=AXIS2_PLACEMENT_3D ( 'NONE', #37104, #18508, #43732 ) ;
#10241=ORIENTED_EDGE ( 'NONE', *, *, #10330, .F. ) ;
#10248=CARTESIAN_POINT ( 'NONE',  ( 10.00000000000000000, -31.46837873495025306, 68.27212725128265447 ) ) ;
#10251=CYLINDRICAL_SURFACE ( 'NONE', #36427, 82.00000000000000000 ) ;
#10253=DIRECTION ( 'NONE',  ( -1.000000000000000000, 0.000000000000000000, 0.000000000000000000 ) ) ;
#10272=DIRECTION ( 'NONE',  ( -1.000000000000000000, 0.000000000000000000, 0.000000000000000000 ) ) ;
#10276=DIRECTION ( 'NONE',  ( -1.000000000000000000, 0.000000000000000000, 0.000000000000000000 ) ) ;
#10284=DIRECTION ( 'NONE',  ( -1.000000000000000000, 0.000000000000000000, -0.000000000000000000 ) ) ;
#10285=DIRECTION ( 'NONE',  ( -1.000000000000000000, 0.000000000000000000, -0.000000000000000000 ) ) ;
#10288=ORIENTED_EDGE ( 'NONE', *, *, #26691, .T. ) ;
#10296=ORIENTED_EDGE ( 'NONE', *, *, #43226, .T. ) ;
#10298=AXIS2_PLACEMENT_3D ( 'NONE', #31017, #17022, #12886 ) ;
#10302=DIRECTION ( 'NONE',  ( -1.000000000000000000, 0.000000000000000000, -0.000000000000000000 ) ) ;
#10303=ORIENTED_EDGE ( 'NONE', *, *, #15599, .T. ) ;
#10306=EDGE_CURVE ( 'NONE', #11779, #42231, #4271, .T. ) ;
#10311=AXIS2_PLACEMENT_3D ( 'NONE', #9198, #24131, #46890 ) ;
#10314=DIRECTION ( 'NONE',  ( 1.000000000000000000, 0.000000000000000000, 0.000000000000000000 ) ) ;
#10316=VERTEX_POINT ( 'NONE', #22850 ) ;
#10319=ORIENTED_EDGE ( 'NONE', *, *, #23644, .T. ) ;
#10321=DIRECTION ( 'NONE',  ( 0.000000000000000000, 0.000000000000000000, 1.000000000000000000 ) ) ;
#10323=VECTOR ( 'NONE', #17832, 1000.000000000000000 ) ;
#10324=DIRECTION ( 'NONE',  ( 0.000000000000000000, -0.9876883405951359940, -0.1564344650402420267 ) ) ;
#10325=DIRECTION ( 'NONE',  ( 0.000000000000000000, 0.000000000000000000, 1.000000000000000000 ) ) ;
#10328=EDGE_CURVE ( 'NONE', #34129, #36599, #47021, .T. ) ;
#10330=EDGE_CURVE ( 'NONE', #25379, #31758, #25898, .T. ) ;
#10332=DIRECTION ( 'NONE',  ( 0.000000000000000000, 0.3090169943749480619, -0.9510565162951533091 ) ) ;
#10335=CARTESIAN_POINT ( 'NONE',  ( 0.000000000000000000, -35.91791733033426226, -68.67312586195033930 ) ) ;
#10336=LINE ( 'NONE', #2275, #3558 ) ;
#10337=DIRECTION ( 'NONE',  ( -1.000000000000000000, -0.000000000000000000, -0.000000000000000000 ) ) ;
#10347=VERTEX_POINT ( 'NONE', #37783 ) ;
#10348=CIRCLE ( 'NONE', #15065, 31.99999999999999289 ) ;
#10360=AXIS2_PLACEMENT_3D ( 'NONE', #23655, #31029, #34664 ) ;
#10365=DIRECTION ( 'NONE',  ( 0.000000000000000000, 0.000000000000000000, 1.000000000000000000 ) ) ;
#10371=ORIENTED_EDGE ( 'NONE', *, *, #18887, .T. ) ;
#10372=CARTESIAN_POINT ( 'NONE',  ( 0.000000000000000000, -34.94270380257693631, 74.18225833017875459 ) ) ;
#10375=ORIENTED_EDGE ( 'NONE', *, *, #41446, .F. ) ;
#10389=CARTESIAN_POINT ( 'NONE',  ( 0.000000000000000000, 74.18225833017888249, 34.94270380257665209 ) ) ;
#10396=DIRECTION ( 'NONE',  ( -1.000000000000000000, 0.000000000000000000, 0.000000000000000000 ) ) ;
#10399=VERTEX_POINT ( 'NONE', #46592 ) ;
#10400=AXIS2_PLACEMENT_3D ( 'NONE', #9602, #24304, #17427 ) ;
#10402=DIRECTION ( 'NONE',  ( -1.000000000000000000, -0.000000000000000000, -0.000000000000000000 ) ) ;
#10403=AXIS2_PLACEMENT_3D ( 'NONE', #1341, #45895, #34131 ) ;
#10407=EDGE_CURVE ( 'NONE', #8188, #40043, #14142, .T. ) ;
#10412=CIRCLE ( 'NONE', #20576, 77.49900000000000944 ) ;
#10420=VERTEX_POINT ( 'NONE', #13057 ) ;
#10427=AXIS2_PLACEMENT_3D ( 'NONE', #20820, #28396, #35747 ) ;
#10433=FACE_OUTER_BOUND ( 'NONE', #24106, .T. ) ;
#10434=EDGE_LOOP ( 'NONE', ( #4529, #14508, #36398, #9440 ) ) ;
#10436=EDGE_CURVE ( 'NONE', #23140, #33476, #34833, .T. ) ;
#10442=ORIENTED_EDGE ( 'NONE', *, *, #5131, .T. ) ;
#10449=VERTEX_POINT ( 'NONE', #31914 ) ;
#10452=DIRECTION ( 'NONE',  ( 0.000000000000000000, 0.000000000000000000, 1.000000000000000000 ) ) ;
#10455=AXIS2_PLACEMENT_3D ( 'NONE', #2396, #13675, #43762 ) ;
#10459=EDGE_CURVE ( 'NONE', #45965, #10316, #39929, .T. ) ;
#10460=CARTESIAN_POINT ( 'NONE',  ( 10.00000000000000000, 0.000000000000000000, 0.000000000000000000 ) ) ;
#10465=CARTESIAN_POINT ( 'NONE',  ( 10.00000000000000000, -71.27951684758046724, 30.41916302227088309 ) ) ;
#10476=AXIS2_PLACEMENT_3D ( 'NONE', #24979, #6391, #25459 ) ;
#10477=CARTESIAN_POINT ( 'NONE',  ( 0.000000000000000000, -75.11764819372145041, -2.946379043147127064 ) ) ;
#10486=VECTOR ( 'NONE', #16727, 1000.000000000000000 ) ;
#10492=PRODUCT ( 'big gear_ISO - Spur gear 2M 80T 20PA 10FW ---S80A75H50L20.0N', 'big gear_ISO - Spur gear 2M 80T 20PA 10FW ---S80A75H50L20.0N', '', ( #45329 ) ) ;
#10499=ORIENTED_EDGE ( 'NONE', *, *, #47869, .F. ) ;
#10500=CARTESIAN_POINT ( 'NONE',  ( 5.000000000000002665, 34.94270380257639630, 74.18225833017899618 ) ) ;
#10502=VERTEX_POINT ( 'NONE', #32607 ) ;
#10503=AXIS2_PLACEMENT_3D ( 'NONE', #12402, #4569, #26602 ) ;
#10514=VERTEX_POINT ( 'NONE', #39489 ) ;
#10516=FACE_OUTER_BOUND ( 'NONE', #29643, .T. ) ;
#10523=ORIENTED_EDGE ( 'NONE', *, *, #12779, .T. ) ;
#10525=DIRECTION ( 'NONE',  ( -1.000000000000000000, 0.000000000000000000, 0.000000000000000000 ) ) ;
#10529=DIRECTION ( 'NONE',  ( 0.000000000000000000, -0.7071067811865388020, -0.7071067811865561215 ) ) ;
#10534=CARTESIAN_POINT ( 'NONE',  ( 0.000000000000000000, 0.000000000000000000, 0.000000000000000000 ) ) ;
#10535=ORIENTED_EDGE ( 'NONE', *, *, #31522, .T. ) ;
#10536=ORIENTED_EDGE ( 'NONE', *, *, #10436, .T. ) ;
#10538=ORIENTED_EDGE ( 'NONE', *, *, #36519, .F. ) ;
#10539=EDGE_CURVE ( 'NONE', #46560, #41161, #27423, .T. ) ;
#10546=VECTOR ( 'NONE', #24, 1000.000000000000000 ) ;
#10549=VERTEX_POINT ( 'NONE', #2499 ) ;
#10557=DIRECTION ( 'NONE',  ( -1.000000000000000000, -0.000000000000000000, -0.000000000000000000 ) ) ;
#10560=AXIS2_PLACEMENT_3D ( 'NONE', #44418, #37066, #13414 ) ;
#10561=DIRECTION ( 'NONE',  ( 0.000000000000000000, 1.000000000000000000, 3.491481338843133355E-15 ) ) ;
#10562=ORIENTED_EDGE ( 'NONE', *, *, #31766, .T. ) ;
#10563=ADVANCED_FACE ( 'NONE', ( #21823 ), #2981, .T. ) ;
#10566=VECTOR ( 'NONE', #22124, 1000.000000000000000 ) ;
#10567=CARTESIAN_POINT ( 'NONE',  ( -10.00000000000000000, 0.000000000000000000, 0.000000000000000000 ) ) ;
#10574=CARTESIAN_POINT ( 'NONE',  ( 0.000000000000000000, 0.000000000000000000, 0.000000000000000000 ) ) ;
#10575=ORIENTED_EDGE ( 'NONE', *, *, #5566, .T. ) ;
#10578=CIRCLE ( 'NONE', #12966, 82.00000000000000000 ) ;
#10579=ORIENTED_EDGE ( 'NONE', *, *, #25018, .F. ) ;
#10584=DIRECTION ( 'NONE',  ( 1.000000000000000000, 0.000000000000000000, 0.000000000000000000 ) ) ;
#10598=DIRECTION ( 'NONE',  ( 0.000000000000000000, 0.000000000000000000, 1.000000000000000000 ) ) ;
#10604=FACE_OUTER_BOUND ( 'NONE', #31453, .T. ) ;
#10605=CYLINDRICAL_SURFACE ( 'NONE', #34215, 31.99999999999999289 ) ;
#10614=ORIENTED_EDGE ( 'NONE', *, *, #40289, .F. ) ;
#10619=ADVANCED_FACE ( 'NONE', ( #14007 ), #33081, .T. ) ;
#10624=VERTEX_POINT ( 'NONE', #35801 ) ;
#10629=LINE ( 'NONE', #17469, #42653 ) ;
#10634=DIRECTION ( 'NONE',  ( 0.000000000000000000, 0.000000000000000000, 1.000000000000000000 ) ) ;
#10638=EDGE_LOOP ( 'NONE', ( #29815, #24937, #12881, #37631 ) ) ;
#10642=CARTESIAN_POINT ( 'NONE',  ( 10.00000000000000000, 0.000000000000000000, 0.000000000000000000 ) ) ;
#10643=EDGE_CURVE ( 'NONE', #44958, #16459, #16487, .T. ) ;
#10645=LINE ( 'NONE', #2319, #8715 ) ;
#10650=DIRECTION ( 'NONE',  ( -1.000000000000000000, 0.000000000000000000, -0.000000000000000000 ) ) ;
#10651=CARTESIAN_POINT ( 'NONE',  ( 0.000000000000000000, 0.000000000000000000, 0.000000000000000000 ) ) ;
#10655=ORIENTED_EDGE ( 'NONE', *, *, #42878, .F. ) ;
#10657=AXIS2_PLACEMENT_3D ( 'NONE', #10829, #25739, #7151 ) ;
#10658=CARTESIAN_POINT ( 'NONE',  ( 10.00000000000000000, -68.67312586194971402, -35.91791733033549860 ) ) ;
#10661=EDGE_CURVE ( 'NONE', #43536, #31088, #3980, .T. ) ;
#10669=CIRCLE ( 'NONE', #29430, 82.00000000000000000 ) ;
#10676=ADVANCED_FACE ( 'NONE', ( #531 ), #14739, .T. ) ;
#10686=ORIENTED_EDGE ( 'NONE', *, *, #10976, .F. ) ;
#10687=AXIS2_PLACEMENT_3D ( 'NONE', #21772, #10525, #14922 ) ;
#10688=DIRECTION ( 'NONE',  ( 0.000000000000000000, 0.000000000000000000, 1.000000000000000000 ) ) ;
#10690=EDGE_LOOP ( 'NONE', ( #4317, #47839, #24053, #28957 ) ) ;
#10695=CARTESIAN_POINT ( 'NONE',  ( 10.00000000000000000, 81.34940948281335693, 10.30890764327412690 ) ) ;
#10696=ORIENTED_EDGE ( 'NONE', *, *, #772, .F. ) ;
#10703=PLANE ( 'NONE',  #23701 ) ;
#10708=LINE ( 'NONE', #13650, #4013 ) ;
#10709=AXIS2_PLACEMENT_3D ( 'NONE', #5786, #9437, #16318 ) ;
#10719=EDGE_CURVE ( 'NONE', #46082, #22693, #45369, .T. ) ;
#10724=AXIS2_PLACEMENT_3D ( 'NONE', #41593, #31317, #22987 ) ;
#10737=EDGE_CURVE ( 'NONE', #37330, #30853, #44829, .T. ) ;
#10745=FACE_OUTER_BOUND ( 'NONE', #33530, .T. ) ;
#10748=ORIENTED_EDGE ( 'NONE', *, *, #3021, .T. ) ;
#10751=DIRECTION ( 'NONE',  ( -1.000000000000000000, 0.000000000000000000, 0.000000000000000000 ) ) ;
#10754=ORIENTED_EDGE ( 'NONE', *, *, #38296, .T. ) ;
#10755=DIRECTION ( 'NONE',  ( -1.000000000000000000, -0.000000000000000000, 0.000000000000000000 ) ) ;
#10757=CIRCLE ( 'NONE', #27963, 31.99999999999999645 ) ;
#10759=ORIENTED_EDGE ( 'NONE', *, *, #47774, .T. ) ;
#10769=AXIS2_PLACEMENT_3D ( 'NONE', #28408, #35758, #47017 ) ;
#10772=CARTESIAN_POINT ( 'NONE',  ( 5.000000000000002665, 44.99326035066052043, 68.55367621811159040 ) ) ;
#10781=ORIENTED_EDGE ( 'NONE', *, *, #15216, .T. ) ;
#10782=VERTEX_POINT ( 'NONE', #1497 ) ;
#10783=AXIS2_PLACEMENT_3D ( 'NONE', #7856, #11778, #26710 ) ;
#10784=EDGE_CURVE ( 'NONE', #41873, #13148, #46982, .T. ) ;
#10787=LINE ( 'NONE', #29388, #19057 ) ;
#10791=FACE_OUTER_BOUND ( 'NONE', #8667, .T. ) ;
#10793=CARTESIAN_POINT ( 'NONE',  ( 10.00000000000000000, 0.000000000000000000, 0.000000000000000000 ) ) ;
#10794=VERTEX_POINT ( 'NONE', #16420 ) ;
#10799=EDGE_CURVE ( 'NONE', #47158, #44507, #12282, .T. ) ;
#10801=ORIENTED_EDGE ( 'NONE', *, *, #29941, .F. ) ;
#10802=ORIENTED_EDGE ( 'NONE', *, *, #6572, .T. ) ;
#10811=DIRECTION ( 'NONE',  ( 0.000000000000000000, -0.5877852522924802425, 0.8090169943749422332 ) ) ;
#10812=ORIENTED_EDGE ( 'NONE', *, *, #3866, .F. ) ;
#10814=ORIENTED_EDGE ( 'NONE', *, *, #39805, .F. ) ;
#10816=ORIENTED_EDGE ( 'NONE', *, *, #24427, .T. ) ;
#10822=ORIENTED_EDGE ( 'NONE', *, *, #47579, .F. ) ;
#10825=ORIENTED_EDGE ( 'NONE', *, *, #34124, .F. ) ;
#10826=AXIS2_PLACEMENT_3D ( 'NONE', #28747, #25541, #47808 ) ;
#10829=CARTESIAN_POINT ( 'NONE',  ( 10.00000000000000000, -41.76937507738831812, 62.50329211542423025 ) ) ;
#10830=ORIENTED_EDGE ( 'NONE', *, *, #33225, .F. ) ;
#10831=CYLINDRICAL_SURFACE ( 'NONE', #16098, 32.00000000000000000 ) ;
#10832=CARTESIAN_POINT ( 'NONE',  ( 10.00000000000000000, -2.543863470248951320, 81.96053171279901051 ) ) ;
#10833=CARTESIAN_POINT ( 'NONE',  ( 0.000000000000000000, 72.35160999960844208, -20.41045688087747223 ) ) ;
#10838=DIRECTION ( 'NONE',  ( 0.000000000000000000, 0.000000000000000000, 1.000000000000000000 ) ) ;
#10841=DIRECTION ( 'NONE',  ( 1.000000000000000000, 0.000000000000000000, 0.000000000000000000 ) ) ;
#10842=EDGE_CURVE ( 'NONE', #23745, #2128, #38390, .T. ) ;
#10844=EDGE_LOOP ( 'NONE', ( #35824, #34921, #22420, #1538 ) ) ;
#10845=DIRECTION ( 'NONE',  ( -1.000000000000000000, 0.000000000000000000, -0.000000000000000000 ) ) ;
#10846=ORIENTED_EDGE ( 'NONE', *, *, #39456, .T. ) ;
#10847=EDGE_CURVE ( 'NONE', #40486, #25055, #2415, .T. ) ;
#10854=EDGE_LOOP ( 'NONE', ( #983, #14089, #6999, #13904 ) ) ;
#10862=LINE ( 'NONE', #40972, #16832 ) ;
#10867=DIRECTION ( 'NONE',  ( 0.000000000000000000, 0.000000000000000000, 1.000000000000000000 ) ) ;
#10869=DIRECTION ( 'NONE',  ( -1.000000000000000000, 0.000000000000000000, 0.000000000000000000 ) ) ;
#10873=VERTEX_POINT ( 'NONE', #1735 ) ;
#10874=CARTESIAN_POINT ( 'NONE',  ( 0.000000000000000000, -44.99326035066101781, 68.55367621811127776 ) ) ;
#10878=VERTEX_POINT ( 'NONE', #16662 ) ;
#10887=CARTESIAN_POINT ( 'NONE',  ( 10.00000000000000000, -70.52718814184240159, -26.02418014898383802 ) ) ;
#10888=DIRECTION ( 'NONE',  ( -1.000000000000000000, -0.000000000000000000, 0.000000000000000000 ) ) ;
#10895=FACE_OUTER_BOUND ( 'NONE', #19159, .T. ) ;
#10903=LINE ( 'NONE', #114, #9551 ) ;
#10907=DIRECTION ( 'NONE',  ( -1.000000000000000000, -0.000000000000000000, 0.000000000000000000 ) ) ;
#10909=AXIS2_PLACEMENT_3D ( 'NONE', #33572, #29659, #7147 ) ;
#10911=VECTOR ( 'NONE', #1901, 1000.000000000000000 ) ;
#10913=DIRECTION ( 'NONE',  ( -1.000000000000000000, -0.000000000000000000, -0.000000000000000000 ) ) ;
#10915=ORIENTED_EDGE ( 'NONE', *, *, #39126, .F. ) ;
#10917=ORIENTED_EDGE ( 'NONE', *, *, #46973, .F. ) ;
#10919=ORIENTED_EDGE ( 'NONE', *, *, #44262, .F. ) ;
#10932=CARTESIAN_POINT ( 'NONE',  ( 5.000000000000002665, 81.50828551894227303, 8.966570791700979370 ) ) ;
#10955=AXIS2_PLACEMENT_3D ( 'NONE', #37456, #16164, #4885 ) ;
#10968=CYLINDRICAL_SURFACE ( 'NONE', #20668, 82.00000000000000000 ) ;
#10976=EDGE_CURVE ( 'NONE', #17725, #21364, #35979, .T. ) ;
#10980=ORIENTED_EDGE ( 'NONE', *, *, #39463, .T. ) ;
#10981=CYLINDRICAL_SURFACE ( 'NONE', #18906, 31.99999999999998579 ) ;
#10983=CIRCLE ( 'NONE', #3139, 31.99999999999999289 ) ;
#10986=DIRECTION ( 'NONE',  ( 0.000000000000000000, 0.000000000000000000, -1.000000000000000000 ) ) ;
#10993=CYLINDRICAL_SURFACE ( 'NONE', #18062, 32.00000000000000000 ) ;
#10994=VERTEX_POINT ( 'NONE', #43805 ) ;
#10995=AXIS2_PLACEMENT_3D ( 'NONE', #36682, #10755, #44035 ) ;
#11008=DIRECTION ( 'NONE',  ( 0.000000000000000000, 0.000000000000000000, -1.000000000000000000 ) ) ;
#11009=CARTESIAN_POINT ( 'NONE',  ( 0.000000000000000000, -41.76106447765533147, 62.50884508063410294 ) ) ;
#11013=FACE_OUTER_BOUND ( 'NONE', #13867, .T. ) ;
#11022=CARTESIAN_POINT ( 'NONE',  ( 0.000000000000000000, 27.74655509720779634, -77.16300072079631889 ) ) ;
#11027=DIRECTION ( 'NONE',  ( 1.000000000000000000, 0.000000000000000000, -0.000000000000000000 ) ) ;
#11029=CARTESIAN_POINT ( 'NONE',  ( 10.00000000000000000, -0.8261519478425671803, -77.49459641780887864 ) ) ;
#11032=ORIENTED_EDGE ( 'NONE', *, *, #26572, .T. ) ;
#11033=DIRECTION ( 'NONE',  ( -1.000000000000000000, -0.000000000000000000, -0.000000000000000000 ) ) ;
#11041=LINE ( 'NONE', #40655, #901 ) ;
#11042=ADVANCED_FACE ( 'NONE', ( #3897 ), #26422, .T. ) ;
#11047=CIRCLE ( 'NONE', #7129, 32.00000000000000000 ) ;
#11053=ORIENTED_EDGE ( 'NONE', *, *, #33419, .F. ) ;
#11054=ORIENTED_EDGE ( 'NONE', *, *, #44897, .T. ) ;
#11059=CARTESIAN_POINT ( 'NONE',  ( 10.00000000000000000, 0.000000000000000000, 0.000000000000000000 ) ) ;
#11061=CARTESIAN_POINT ( 'NONE',  ( 0.000000000000000000, 0.000000000000000000, 0.000000000000000000 ) ) ;
#11077=CYLINDRICAL_SURFACE ( 'NONE', #42555, 31.99999999999999289 ) ;
#11083=VERTEX_POINT ( 'NONE', #30337 ) ;
#11088=AXIS2_PLACEMENT_3D ( 'NONE', #18281, #14383, #1993 ) ;
#11100=EDGE_LOOP ( 'NONE', ( #39952, #17539, #35827, #9472 ) ) ;
#11105=DIRECTION ( 'NONE',  ( -1.000000000000000000, 0.000000000000000000, 0.000000000000000000 ) ) ;
#11106=LINE ( 'NONE', #41216, #19463 ) ;
#11111=EDGE_CURVE ( 'NONE', #14894, #41873, #19060, .T. ) ;
#11114=ORIENTED_EDGE ( 'NONE', *, *, #45721, .T. ) ;
#11125=CIRCLE ( 'NONE', #7202, 31.99999999999999645 ) ;
#11139=CYLINDRICAL_SURFACE ( 'NONE', #40205, 31.99999999999999289 ) ;
#11141=DIRECTION ( 'NONE',  ( -1.000000000000000000, -0.000000000000000000, 0.000000000000000000 ) ) ;
#11142=CIRCLE ( 'NONE', #26789, 32.00000000000000000 ) ;
#11145=VERTEX_POINT ( 'NONE', #33019 ) ;
#11158=FACE_OUTER_BOUND ( 'NONE', #15604, .T. ) ;
#11160=DIRECTION ( 'NONE',  ( -1.000000000000000000, -0.000000000000000000, -0.000000000000000000 ) ) ;
#11163=EDGE_CURVE ( 'NONE', #6523, #14170, #8765, .T. ) ;
#11176=CIRCLE ( 'NONE', #18173, 31.99999999999999289 ) ;
#11180=FACE_OUTER_BOUND ( 'NONE', #24376, .T. ) ;
#11184=DIRECTION ( 'NONE',  ( -1.000000000000000000, 0.000000000000000000, 0.000000000000000000 ) ) ;
#11186=ORIENTED_EDGE ( 'NONE', *, *, #26696, .F. ) ;
#11187=FACE_OUTER_BOUND ( 'NONE', #12485, .T. ) ;
#11188=VERTEX_POINT ( 'NONE', #700 ) ;
#11191=AXIS2_PLACEMENT_3D ( 'NONE', #29923, #26264, #44854 ) ;
#11193=CARTESIAN_POINT ( 'NONE',  ( 10.00000000000000000, 0.000000000000000000, 0.000000000000000000 ) ) ;
#11203=FACE_OUTER_BOUND ( 'NONE', #10027, .T. ) ;
#11204=VERTEX_POINT ( 'NONE', #19523 ) ;
#11205=ORIENTED_EDGE ( 'NONE', *, *, #47365, .T. ) ;
#11207=AXIS2_PLACEMENT_3D ( 'NONE', #45330, #8603, #37754 ) ;
#11208=EDGE_CURVE ( 'NONE', #12844, #32530, #30232, .T. ) ;
#11217=ORIENTED_EDGE ( 'NONE', *, *, #18721, .T. ) ;
#11220=DIRECTION ( 'NONE',  ( -1.000000000000000000, 0.000000000000000000, 0.000000000000000000 ) ) ;
#11221=EDGE_CURVE ( 'NONE', #45989, #6258, #45073, .T. ) ;
#11224=ORIENTED_EDGE ( 'NONE', *, *, #7937, .F. ) ;
#11225=CARTESIAN_POINT ( 'NONE',  ( 0.000000000000000000, 26.01480285779837232, 70.53064760720326376 ) ) ;
#11229=DIRECTION ( 'NONE',  ( -1.000000000000000000, 0.000000000000000000, 0.000000000000000000 ) ) ;
#11232=VECTOR ( 'NONE', #7884, 1000.000000000000000 ) ;
#11239=DIRECTION ( 'NONE',  ( 0.000000000000000000, 0.000000000000000000, 1.000000000000000000 ) ) ;
#11245=DIRECTION ( 'NONE',  ( 0.000000000000000000, 0.000000000000000000, -1.000000000000000000 ) ) ;
#11248=LINE ( 'NONE', #3894, #26924 ) ;
#11258=CARTESIAN_POINT ( 'NONE',  ( 10.00000000000000000, -41.76937507738745836, -62.50329211542482710 ) ) ;
#11260=CARTESIAN_POINT ( 'NONE',  ( 10.00000000000000000, 49.70050353004977239, -59.46389618801908483 ) ) ;
#11262=DIRECTION ( 'NONE',  ( -1.000000000000000000, -0.000000000000000000, -0.000000000000000000 ) ) ;
#11269=CIRCLE ( 'NONE', #38635, 31.99999999999999645 ) ;
#11277=AXIS2_PLACEMENT_3D ( 'NONE', #16496, #13308, #31441 ) ;
#11281=ORIENTED_EDGE ( 'NONE', *, *, #1829, .T. ) ;
#11284=ORIENTED_EDGE ( 'NONE', *, *, #46359, .F. ) ;
#11290=CARTESIAN_POINT ( 'NONE',  ( 0.000000000000000000, 78.73519480814985627, -22.90783923731548910 ) ) ;
#11291=ORIENTED_EDGE ( 'NONE', *, *, #14369, .T. ) ;
#11292=VERTEX_POINT ( 'NONE', #34463 ) ;
#11299=EDGE_LOOP ( 'NONE', ( #41693, #29207, #10915, #39092 ) ) ;
#11304=CARTESIAN_POINT ( 'NONE',  ( 0.000000000000000000, 36.72794159290334903, -65.59268652807170952 ) ) ;
#11314=VERTEX_POINT ( 'NONE', #37068 ) ;
#11319=AXIS2_PLACEMENT_3D ( 'NONE', #48303, #14781, #29696 ) ;
#11320=CARTESIAN_POINT ( 'NONE',  ( 10.00000000000000000, -28.89263327155693517, -71.91182617369219088 ) ) ;
#11324=VECTOR ( 'NONE', #21291, 1000.000000000000000 ) ;
#11325=CARTESIAN_POINT ( 'NONE',  ( 0.000000000000000000, -0.8261519478436571973, 77.49459641780886443 ) ) ;
#11329=AXIS2_PLACEMENT_3D ( 'NONE', #3621, #44987, #26389 ) ;
#11330=CIRCLE ( 'NONE', #26161, 31.99999999999999289 ) ;
#11334=CARTESIAN_POINT ( 'NONE',  ( 10.00000000000000000, 0.000000000000000000, 0.000000000000000000 ) ) ;
#11343=DIRECTION ( 'NONE',  ( -1.000000000000000000, 0.000000000000000000, 0.000000000000000000 ) ) ;
#11344=EDGE_CURVE ( 'NONE', #13511, #26518, #13809, .T. ) ;
#11352=EDGE_CURVE ( 'NONE', #13398, #773, #44420, .T. ) ;
#11353=EDGE_CURVE ( 'NONE', #17893, #40687, #13661, .T. ) ;
#11355=AXIS2_PLACEMENT_3D ( 'NONE', #41850, #26671, #30576 ) ;
#11360=ORIENTED_EDGE ( 'NONE', *, *, #4927, .F. ) ;
#11362=VECTOR ( 'NONE', #4553, 1000.000000000000000 ) ;
#11363=AXIS2_PLACEMENT_3D ( 'NONE', #40189, #21579, #47993 ) ;
#11370=CARTESIAN_POINT ( 'NONE',  ( 10.00000000000000000, 74.74816331893477184, -33.71516098798658589 ) ) ;
#11374=DIRECTION ( 'NONE',  ( 1.000000000000000000, 0.000000000000000000, 0.000000000000000000 ) ) ;
#11377=CARTESIAN_POINT ( 'NONE',  ( 50.00005079999999680, 0.000000000000000000, 0.000000000000000000 ) ) ;
#11380=DIRECTION ( 'NONE',  ( 0.000000000000000000, 0.000000000000000000, 1.000000000000000000 ) ) ;
#11389=DIRECTION ( 'NONE',  ( 0.000000000000000000, 0.07845909572783797692, 0.9969173337331285190 ) ) ;
#11392=CIRCLE ( 'NONE', #26228, 77.49899999999999523 ) ;
#11393=CIRCLE ( 'NONE', #5133, 77.49900000000000944 ) ;
#11394=DIRECTION ( 'NONE',  ( 1.000000000000000000, -0.000000000000000000, 0.000000000000000000 ) ) ;
#11395=DIRECTION ( 'NONE',  ( -1.000000000000000000, -0.000000000000000000, -0.000000000000000000 ) ) ;
#11396=DIRECTION ( 'NONE',  ( 0.000000000000000000, 0.000000000000000000, 1.000000000000000000 ) ) ;
#11404=ORIENTED_EDGE ( 'NONE', *, *, #9445, .T. ) ;
#11406=EDGE_CURVE ( 'NONE', #9950, #38308, #28654, .T. ) ;
#11416=DIRECTION ( 'NONE',  ( 0.000000000000000000, 0.1564344650402244019, 0.9876883405951387696 ) ) ;
#11420=ORIENTED_EDGE ( 'NONE', *, *, #19794, .F. ) ;
#11435=CARTESIAN_POINT ( 'NONE',  ( 0.000000000000000000, -71.21200624218768382, -40.65526001592689909 ) ) ;
#11437=DIRECTION ( 'NONE',  ( 1.000000000000000000, 0.000000000000000000, 0.000000000000000000 ) ) ;
#11440=ORIENTED_EDGE ( 'NONE', *, *, #1721, .T. ) ;
#11441=CARTESIAN_POINT ( 'NONE',  ( 10.00000000000000000, -74.65491531819124305, 8.830959090342128448 ) ) ;
#11444=ADVANCED_FACE ( 'NONE', ( #35694 ), #2165, .T. ) ;
#11449=CARTESIAN_POINT ( 'NONE',  ( 10.00000000000000000, 0.000000000000000000, 0.000000000000000000 ) ) ;
#11456=EDGE_LOOP ( 'NONE', ( #27915, #38120, #48078, #902 ) ) ;
#11464=ORIENTED_EDGE ( 'NONE', *, *, #29500, .T. ) ;
#11476=CARTESIAN_POINT ( 'NONE',  ( 10.00000000000000000, 0.000000000000000000, 0.000000000000000000 ) ) ;
#11481=CARTESIAN_POINT ( 'NONE',  ( 0.000000000000000000, 0.000000000000000000, 0.000000000000000000 ) ) ;
#11491=ORIENTED_EDGE ( 'NONE', *, *, #16751, .F. ) ;
#11495=DIRECTION ( 'NONE',  ( 0.000000000000000000, 0.000000000000000000, 1.000000000000000000 ) ) ;
#11501=DIRECTION ( 'NONE',  ( 0.000000000000000000, 0.7071067811865439090, 0.7071067811865512365 ) ) ;
#11506=EDGE_CURVE ( 'NONE', #29530, #32691, #8179, .T. ) ;
#11508=DIRECTION ( 'NONE',  ( 0.000000000000000000, 0.2334453638559058630, -0.9723699203976765570 ) ) ;
#11509=EDGE_CURVE ( 'NONE', #12571, #2183, #37276, .T. ) ;
#11524=CIRCLE ( 'NONE', #17762, 82.00000000000000000 ) ;
#11525=ORIENTED_EDGE ( 'NONE', *, *, #9895, .T. ) ;
#11533=FACE_OUTER_BOUND ( 'NONE', #40103, .T. ) ;
#11534=EDGE_LOOP ( 'NONE', ( #39173, #26273, #685, #14694 ) ) ;
#11543=EDGE_CURVE ( 'NONE', #10449, #26599, #38085, .T. ) ;
#11547=ORIENTED_EDGE ( 'NONE', *, *, #27524, .F. ) ;
#11548=ORIENTED_EDGE ( 'NONE', *, *, #45217, .T. ) ;
#11550=CYLINDRICAL_SURFACE ( 'NONE', #27859, 32.00000000000000000 ) ;
#11553=DIRECTION ( 'NONE',  ( -1.000000000000000000, 0.000000000000000000, 0.000000000000000000 ) ) ;
#11556=EDGE_CURVE ( 'NONE', #21364, #37807, #16978, .T. ) ;
#11561=ORIENTED_EDGE ( 'NONE', *, *, #26666, .F. ) ;
#11568=CYLINDRICAL_SURFACE ( 'NONE', #24585, 82.00000000000000000 ) ;
#11572=ADVANCED_FACE ( 'NONE', ( #26305 ), #4748, .T. ) ;
#11578=DIRECTION ( 'NONE',  ( -1.000000000000000000, 0.000000000000000000, -0.000000000000000000 ) ) ;
#11579=VERTEX_POINT ( 'NONE', #7461 ) ;
#11583=CIRCLE ( 'NONE', #7563, 31.99999999999998934 ) ;
#11587=ORIENTED_EDGE ( 'NONE', *, *, #18908, .F. ) ;
#11588=ORIENTED_EDGE ( 'NONE', *, *, #28674, .T. ) ;
#11589=VECTOR ( 'NONE', #2691, 1000.000000000000000 ) ;
#11599=VERTEX_POINT ( 'NONE', #39010 ) ;
#11603=DIRECTION ( 'NONE',  ( -1.000000000000000000, -0.000000000000000000, 0.000000000000000000 ) ) ;
#11604=CARTESIAN_POINT ( 'NONE',  ( 10.00000000000000000, 0.000000000000000000, 0.000000000000000000 ) ) ;
#11615=DIRECTION ( 'NONE',  ( 0.000000000000000000, -0.7071067811865537900, 0.7071067811865413555 ) ) ;
#11619=DIRECTION ( 'NONE',  ( 0.000000000000000000, 0.8910065241883690090, -0.4539904997395446395 ) ) ;
#11624=CARTESIAN_POINT ( 'NONE',  ( 0.000000000000000000, 0.000000000000000000, 0.000000000000000000 ) ) ;
#11625=CARTESIAN_POINT ( 'NONE',  ( 10.00000000000000000, 75.11725578898467859, 2.956366410620910656 ) ) ;
#11629=AXIS2_PLACEMENT_3D ( 'NONE', #36085, #43190, #47570 ) ;
#11631=ORIENTED_EDGE ( 'NONE', *, *, #13550, .T. ) ;
#11634=LINE ( 'NONE', #29745, #17160 ) ;
#11636=AXIS2_PLACEMENT_3D ( 'NONE', #13959, #6619, #3667 ) ;
#11638=DIRECTION ( 'NONE',  ( 0.000000000000000000, 0.9723699203976773342, -0.2334453638559023381 ) ) ;
#11640=ORIENTED_EDGE ( 'NONE', *, *, #17521, .F. ) ;
#11642=CARTESIAN_POINT ( 'NONE',  ( 0.000000000000000000, 0.000000000000000000, 0.000000000000000000 ) ) ;
#11647=CARTESIAN_POINT ( 'NONE',  ( 10.00000000000000000, 74.74816331893428867, 33.71516098798765881 ) ) ;
#11649=EDGE_LOOP ( 'NONE', ( #9254, #42339, #29232, #7727 ) ) ;
#11666=CARTESIAN_POINT ( 'NONE',  ( 5.000000000000002665, 81.90746397400393164, -3.894527615416986333 ) ) ;
#11671=VERTEX_POINT ( 'NONE', #2276 ) ;
#11677=ADVANCED_FACE ( 'NONE', ( #31195 ), #9376, .T. ) ;
#11680=DIRECTION ( 'NONE',  ( -1.000000000000000000, 0.000000000000000000, 0.000000000000000000 ) ) ;
#11683=DIRECTION ( 'NONE',  ( -1.000000000000000000, 0.000000000000000000, -0.000000000000000000 ) ) ;
#11684=EDGE_CURVE ( 'NONE', #40419, #13689, #28002, .T. ) ;
#11686=ORIENTED_EDGE ( 'NONE', *, *, #47022, .F. ) ;
#11696=DIRECTION ( 'NONE',  ( 0.000000000000000000, 0.000000000000000000, 1.000000000000000000 ) ) ;
#11700=DIRECTION ( 'NONE',  ( 0.000000000000000000, 0.000000000000000000, 1.000000000000000000 ) ) ;
#11713=DIRECTION ( 'NONE',  ( 0.000000000000000000, -0.9969173337331270757, -0.07845909572785580988 ) ) ;
#11721=ORIENTED_EDGE ( 'NONE', *, *, #13450, .T. ) ;
#11725=CARTESIAN_POINT ( 'NONE',  ( 10.00000000000000000, 14.67089635893713684, 73.72996012237443608 ) ) ;
#11728=CIRCLE ( 'NONE', #27383, 82.00000000000000000 ) ;
#11742=VERTEX_POINT ( 'NONE', #40220 ) ;
#11743=EDGE_CURVE ( 'NONE', #33332, #9321, #13077, .T. ) ;
#11746=EDGE_CURVE ( 'NONE', #31534, #20915, #8381, .T. ) ;
#11747=CARTESIAN_POINT ( 'NONE',  ( 10.00000000000000000, 68.27212725128275395, -31.46837873495001503 ) ) ;
#11757=ORIENTED_EDGE ( 'NONE', *, *, #10236, .T. ) ;
#11763=CIRCLE ( 'NONE', #36772, 31.99999999999999289 ) ;
#11766=ADVANCED_FACE ( 'NONE', ( #2756 ), #36760, .T. ) ;
#11774=DIRECTION ( 'NONE',  ( -1.000000000000000000, 0.000000000000000000, -0.000000000000000000 ) ) ;
#11778=DIRECTION ( 'NONE',  ( -1.000000000000000000, -0.000000000000000000, 0.000000000000000000 ) ) ;
#11779=VERTEX_POINT ( 'NONE', #37003 ) ;
#11780=EDGE_CURVE ( 'NONE', #15249, #15994, #35736, .T. ) ;
#11782=DIRECTION ( 'NONE',  ( 0.000000000000000000, 0.000000000000000000, 1.000000000000000000 ) ) ;
#11783=ORIENTED_EDGE ( 'NONE', *, *, #12897, .T. ) ;
#11788=CARTESIAN_POINT ( 'NONE',  ( 5.000000000000002665, -10.30890764327441822, 81.34940948281332851 ) ) ;
#11794=CARTESIAN_POINT ( 'NONE',  ( 10.00000000000000000, 64.81221759200417409, -50.23322058963275794 ) ) ;
#11800=DIRECTION ( 'NONE',  ( 0.000000000000000000, 0.000000000000000000, 1.000000000000000000 ) ) ;
#11804=EDGE_CURVE ( 'NONE', #37445, #2183, #17917, .T. ) ;
#11808=VERTEX_POINT ( 'NONE', #21610 ) ;
#11814=DIRECTION ( 'NONE',  ( 1.000000000000000000, -0.000000000000000000, -0.000000000000000000 ) ) ;
#11819=AXIS2_PLACEMENT_3D ( 'NONE', #30738, #33906, #38083 ) ;
#11826=ADVANCED_FACE ( 'NONE', ( #6684 ), #14259, .T. ) ;
#11828=EDGE_CURVE ( 'NONE', #48063, #27309, #38860, .T. ) ;
#11829=ADVANCED_FACE ( 'NONE', ( #10106 ), #17693, .T. ) ;
#11842=EDGE_CURVE ( 'NONE', #24088, #30166, #19336, .T. ) ;
#11848=FACE_BOUND ( 'NONE', #16152, .T. ) ;
#11849=CARTESIAN_POINT ( 'NONE',  ( 0.000000000000000000, -81.96053171279901051, -2.543863470249246195 ) ) ;
#11852=DIRECTION ( 'NONE',  ( -1.000000000000000000, -0.000000000000000000, 0.000000000000000000 ) ) ;
#11862=AXIS2_PLACEMENT_3D ( 'NONE', #44878, #15742, #18680 ) ;
#11868=DIRECTION ( 'NONE',  ( -1.000000000000000000, 0.000000000000000000, 0.000000000000000000 ) ) ;
#11872=ORIENTED_EDGE ( 'NONE', *, *, #41610, .F. ) ;
#11876=FACE_OUTER_BOUND ( 'NONE', #34510, .T. ) ;
#11879=CARTESIAN_POINT ( 'NONE',  ( 0.000000000000000000, 0.000000000000000000, 0.000000000000000000 ) ) ;
#11881=LINE ( 'NONE', #26805, #31229 ) ;
#11883=ORIENTED_EDGE ( 'NONE', *, *, #13319, .F. ) ;
#11888=EDGE_CURVE ( 'NONE', #18503, #22588, #10757, .T. ) ;
#11899=CARTESIAN_POINT ( 'NONE',  ( 0.000000000000000000, 0.000000000000000000, 0.000000000000000000 ) ) ;
#11901=DIRECTION ( 'NONE',  ( -1.000000000000000000, 0.000000000000000000, 0.000000000000000000 ) ) ;
#11907=CARTESIAN_POINT ( 'NONE',  ( 10.00000000000000000, 11.30684508768339569, 76.66974797899841576 ) ) ;
#11911=CARTESIAN_POINT ( 'NONE',  ( 0.000000000000000000, 41.76106447765580043, -62.50884508063379741 ) ) ;
#11922=DIRECTION ( 'NONE',  ( -1.000000000000000000, 0.000000000000000000, 0.000000000000000000 ) ) ;
#11924=VECTOR ( 'NONE', #45018, 1000.000000000000000 ) ;
#11925=ORIENTED_EDGE ( 'NONE', *, *, #893, .F. ) ;
#11927=DIRECTION ( 'NONE',  ( -1.000000000000000000, -0.000000000000000000, 0.000000000000000000 ) ) ;
#11934=EDGE_CURVE ( 'NONE', #20915, #36021, #41416, .T. ) ;
#11939=EDGE_CURVE ( 'NONE', #14587, #43833, #43568, .T. ) ;
#11946=ADVANCED_FACE ( 'NONE', ( #37497 ), #762, .T. ) ;
#11951=DIRECTION ( 'NONE',  ( -1.000000000000000000, 0.000000000000000000, 0.000000000000000000 ) ) ;
#11957=CYLINDRICAL_SURFACE ( 'NONE', #44713, 77.49899999999999523 ) ;
#11963=VECTOR ( 'NONE', #35514, 1000.000000000000000 ) ;
#11964=EDGE_CURVE ( 'NONE', #45199, #44962, #45091, .T. ) ;
#11965=FACE_OUTER_BOUND ( 'NONE', #20160, .T. ) ;
#11968=DIRECTION ( 'NONE',  ( -1.000000000000000000, 0.000000000000000000, -0.000000000000000000 ) ) ;
#11973=CIRCLE ( 'NONE', #8803, 77.49900000000000944 ) ;
#11975=DIRECTION ( 'NONE',  ( -1.000000000000000000, -0.000000000000000000, -0.000000000000000000 ) ) ;
#11977=DIRECTION ( 'NONE',  ( -1.000000000000000000, 0.000000000000000000, 0.000000000000000000 ) ) ;
#11981=CARTESIAN_POINT ( 'NONE',  ( 10.00000000000000000, 5.256550761632864166, 77.32052557432842832 ) ) ;
#11994=DIRECTION ( 'NONE',  ( 0.000000000000000000, 0.000000000000000000, -1.000000000000000000 ) ) ;
#11996=VERTEX_POINT ( 'NONE', #5415 ) ;
#12006=ORIENTED_EDGE ( 'NONE', *, *, #31522, .F. ) ;
#12008=ORIENTED_EDGE ( 'NONE', *, *, #6951, .T. ) ;
#12012=ORIENTED_EDGE ( 'NONE', *, *, #13426, .T. ) ;
#12021=ORIENTED_EDGE ( 'NONE', *, *, #12830, .F. ) ;
#12028=DIRECTION ( 'NONE',  ( 1.000000000000000000, -0.000000000000000000, -0.000000000000000000 ) ) ;
#12038=DIRECTION ( 'NONE',  ( -1.000000000000000000, 0.000000000000000000, 0.000000000000000000 ) ) ;
#12041=FACE_OUTER_BOUND ( 'NONE', #46715, .T. ) ;
#12049=VERTEX_POINT ( 'NONE', #13014 ) ;
#12050=AXIS2_PLACEMENT_3D ( 'NONE', #4619, #3654, #11495 ) ;
#12054=CYLINDRICAL_SURFACE ( 'NONE', #36318, 82.00000000000000000 ) ;
#12059=ORIENTED_EDGE ( 'NONE', *, *, #11684, .T. ) ;
#12063=ORIENTED_EDGE ( 'NONE', *, *, #13856, .F. ) ;
#12065=EDGE_CURVE ( 'NONE', #14287, #46808, #34967, .T. ) ;
#12076=ORIENTED_EDGE ( 'NONE', *, *, #2373, .F. ) ;
#12080=AXIS2_PLACEMENT_3D ( 'NONE', #8040, #22978, #45486 ) ;
#12083=AXIS2_PLACEMENT_3D ( 'NONE', #22348, #2514, #17446 ) ;
#12086=DIRECTION ( 'NONE',  ( 0.000000000000000000, 0.000000000000000000, 1.000000000000000000 ) ) ;
#12087=DIRECTION ( 'NONE',  ( 0.000000000000000000, 0.000000000000000000, 1.000000000000000000 ) ) ;
#12090=AXIS2_PLACEMENT_3D ( 'NONE', #47622, #3313, #14106 ) ;
#12092=ORIENTED_EDGE ( 'NONE', *, *, #18944, .T. ) ;
#12095=VERTEX_POINT ( 'NONE', #42376 ) ;
#12096=CIRCLE ( 'NONE', #37089, 77.49900000000000944 ) ;
#12099=DIRECTION ( 'NONE',  ( -1.000000000000000000, -0.000000000000000000, 0.000000000000000000 ) ) ;
#12105=DIRECTION ( 'NONE',  ( 1.000000000000000000, 0.000000000000000000, 0.000000000000000000 ) ) ;
#12113=DIRECTION ( 'NONE',  ( 1.000000000000000000, -0.000000000000000000, -0.000000000000000000 ) ) ;
#12117=EDGE_LOOP ( 'NONE', ( #30264, #30142, #27790, #46096 ) ) ;
#12119=CIRCLE ( 'NONE', #26957, 77.49900000000002365 ) ;
#12120=FACE_OUTER_BOUND ( 'NONE', #40247, .T. ) ;
#12125=AXIS2_PLACEMENT_3D ( 'NONE', #28129, #14344, #47619 ) ;
#12126=AXIS2_PLACEMENT_3D ( 'NONE', #18657, #34070, #15481 ) ;
#12130=CIRCLE ( 'NONE', #31664, 31.99999999999998934 ) ;
#12134=VECTOR ( 'NONE', #27682, 1000.000000000000000 ) ;
#12138=ORIENTED_EDGE ( 'NONE', *, *, #30862, .F. ) ;
#12139=AXIS2_PLACEMENT_3D ( 'NONE', #39293, #15819, #30752 ) ;
#12140=CARTESIAN_POINT ( 'NONE',  ( 10.00000000000000000, 59.75363087400152295, -56.15606465354897381 ) ) ;
#12144=ORIENTED_EDGE ( 'NONE', *, *, #12620, .F. ) ;
#12151=AXIS2_PLACEMENT_3D ( 'NONE', #1065, #11852, #27512 ) ;
#12154=FACE_OUTER_BOUND ( 'NONE', #27805, .T. ) ;
#12158=DIRECTION ( 'NONE',  ( 1.000000000000000000, 0.000000000000000000, -0.000000000000000000 ) ) ;
#12160=CARTESIAN_POINT ( 'NONE',  ( 10.00000000000000000, -55.38113227695820484, 54.21277698773656084 ) ) ;
#12161=CYLINDRICAL_SURFACE ( 'NONE', #44667, 77.49899999999999523 ) ;
#12163=CYLINDRICAL_SURFACE ( 'NONE', #8135, 82.00000000000000000 ) ;
#12165=CYLINDRICAL_SURFACE ( 'NONE', #18900, 77.49899999999999523 ) ;
#12167=ADVANCED_FACE ( 'NONE', ( #27573 ), #45218, .T. ) ;
#12169=AXIS2_PLACEMENT_3D ( 'NONE', #29156, #36268, #44095 ) ;
#12176=FACE_OUTER_BOUND ( 'NONE', #5380, .T. ) ;
#12180=FACE_OUTER_BOUND ( 'NONE', #33719, .T. ) ;
#12182=DIRECTION ( 'NONE',  ( -1.000000000000000000, 0.000000000000000000, -0.000000000000000000 ) ) ;
#12185=LINE ( 'NONE', #27110, #47878 ) ;
#12186=EDGE_CURVE ( 'NONE', #33852, #22252, #16089, .T. ) ;
#12188=VERTEX_POINT ( 'NONE', #27336 ) ;
#12191=ORIENTED_EDGE ( 'NONE', *, *, #34361, .T. ) ;
#12204=ORIENTED_EDGE ( 'NONE', *, *, #23063, .F. ) ;
#12205=FACE_OUTER_BOUND ( 'NONE', #40763, .T. ) ;
#12209=CYLINDRICAL_SURFACE ( 'NONE', #3789, 31.99999999999998579 ) ;
#12210=ORIENTED_EDGE ( 'NONE', *, *, #31893, .T. ) ;
#12215=ORIENTED_EDGE ( 'NONE', *, *, #40153, .F. ) ;
#12223=DIRECTION ( 'NONE',  ( 0.000000000000000000, 0.000000000000000000, 1.000000000000000000 ) ) ;
#12230=CIRCLE ( 'NONE', #3612, 31.99999999999999289 ) ;
#12232=DIRECTION ( 'NONE',  ( 0.000000000000000000, 0.000000000000000000, 1.000000000000000000 ) ) ;
#12238=CARTESIAN_POINT ( 'NONE',  ( 0.000000000000000000, 0.000000000000000000, 12.50000000000000000 ) ) ;
#12243=AXIS2_PLACEMENT_3D ( 'NONE', #42564, #19775, #41837 ) ;
#12246=DIRECTION ( 'NONE',  ( 0.000000000000000000, 0.000000000000000000, 1.000000000000000000 ) ) ;
#12249=EDGE_CURVE ( 'NONE', #42351, #37895, #422, .T. ) ;
#12253=ORIENTED_EDGE ( 'NONE', *, *, #46995, .T. ) ;
#12271=CARTESIAN_POINT ( 'NONE',  ( 0.000000000000000000, 81.50828551894240093, -8.966570791699803422 ) ) ;
#12278=CARTESIAN_POINT ( 'NONE',  ( 10.00000000000000000, -51.02545421589285723, -55.20638768913812555 ) ) ;
#12280=EDGE_CURVE ( 'NONE', #2339, #37110, #45445, .T. ) ;
#12281=DIRECTION ( 'NONE',  ( -1.000000000000000000, -0.000000000000000000, -0.000000000000000000 ) ) ;
#12282=LINE ( 'NONE', #20091, #44635 ) ;
#12286=EDGE_CURVE ( 'NONE', #33476, #16326, #3734, .T. ) ;
#12296=CARTESIAN_POINT ( 'NONE',  ( 10.00000000000000000, -75.16055320797016748, -18.89407956138335365 ) ) ;
#12305=EDGE_CURVE ( 'NONE', #13689, #47062, #3423, .T. ) ;
#12307=AXIS2_PLACEMENT_3D ( 'NONE', #30828, #45752, #46231 ) ;
#12311=VECTOR ( 'NONE', #45551, 1000.000000000000000 ) ;
#12314=AXIS2_PLACEMENT_3D ( 'NONE', #7337, #36705, #29611 ) ;
#12322=CARTESIAN_POINT ( 'NONE',  ( 10.00000000000000000, 0.000000000000000000, 0.000000000000000000 ) ) ;
#12324=CARTESIAN_POINT ( 'NONE',  ( 0.000000000000000000, 68.26794271651262136, 31.47745569255165066 ) ) ;
#12325=CIRCLE ( 'NONE', #46744, 31.99999999999998934 ) ;
#12333=VECTOR ( 'NONE', #2998, 1000.000000000000000 ) ;
#12335=LINE ( 'NONE', #7916, #6649 ) ;
#12336=CARTESIAN_POINT ( 'NONE',  ( 10.00000000000000000, 0.000000000000000000, 0.000000000000000000 ) ) ;
#12340=CYLINDRICAL_SURFACE ( 'NONE', #18214, 82.00000000000000000 ) ;
#12343=CARTESIAN_POINT ( 'NONE',  ( 0.000000000000000000, 77.49459641780886443, -0.8261519478433788644 ) ) ;
#12350=CARTESIAN_POINT ( 'NONE',  ( 10.00000000000000000, -68.27212725128254078, -31.46837873495049465 ) ) ;
#12351=CARTESIAN_POINT ( 'NONE',  ( 50.00005079999999680, 0.000000000000000000, 0.000000000000000000 ) ) ;
#12362=EDGE_CURVE ( 'NONE', #31758, #41512, #2116, .T. ) ;
#12363=ORIENTED_EDGE ( 'NONE', *, *, #10167, .F. ) ;
#12367=AXIS2_PLACEMENT_3D ( 'NONE', #31779, #13388, #8992 ) ;
#12372=DIRECTION ( 'NONE',  ( 0.000000000000000000, 0.7071067811865487940, -0.7071067811865463515 ) ) ;
#12374=CARTESIAN_POINT ( 'NONE',  ( 10.00000000000000000, -14.67089635893764665, 73.72996012237435082 ) ) ;
#12379=CARTESIAN_POINT ( 'NONE',  ( 10.00000000000000000, 71.91182617369230456, -28.89263327155667938 ) ) ;
#12380=CIRCLE ( 'NONE', #22509, 82.00000000000000000 ) ;
#12392=DIRECTION ( 'NONE',  ( 0.000000000000000000, -0.3090169943749349057, -0.9510565162951577500 ) ) ;
#12400=DIRECTION ( 'NONE',  ( -1.000000000000000000, -0.000000000000000000, 0.000000000000000000 ) ) ;
#12402=CARTESIAN_POINT ( 'NONE',  ( 10.00000000000000000, 74.65374052328660071, -8.840884882374309583 ) ) ;
#12405=DIRECTION ( 'NONE',  ( -1.000000000000000000, 0.000000000000000000, 0.000000000000000000 ) ) ;
#12406=CARTESIAN_POINT ( 'NONE',  ( 10.00000000000000000, 51.03279382321088065, 55.19960302592086521 ) ) ;
#12409=CARTESIAN_POINT ( 'NONE',  ( 0.000000000000000000, 0.000000000000000000, 0.000000000000000000 ) ) ;
#12417=CIRCLE ( 'NONE', #39777, 31.99999999999999289 ) ;
#12422=VECTOR ( 'NONE', #22028, 1000.000000000000000 ) ;
#12425=EDGE_CURVE ( 'NONE', #22554, #32703, #42545, .T. ) ;
#12428=ORIENTED_EDGE ( 'NONE', *, *, #19467, .T. ) ;
#12433=EDGE_LOOP ( 'NONE', ( #25790, #21297, #8918, #9270 ) ) ;
#12437=VERTEX_POINT ( 'NONE', #42756 ) ;
#12442=DIRECTION ( 'NONE',  ( 0.000000000000000000, -0.5877852522924803536, 0.8090169943749422332 ) ) ;
#12443=CARTESIAN_POINT ( 'NONE',  ( 10.00000000000000000, 41.76937507738875155, -62.50329211542393892 ) ) ;
#12445=DIRECTION ( 'NONE',  ( 0.000000000000000000, 0.000000000000000000, 1.000000000000000000 ) ) ;
#12446=ORIENTED_EDGE ( 'NONE', *, *, #19334, .F. ) ;
#12448=ADVANCED_FACE ( 'NONE', ( #25807 ), #14580, .T. ) ;
#12451=DIRECTION ( 'NONE',  ( 0.000000000000000000, -0.4539904997395350361, -0.8910065241883738940 ) ) ;
#12454=FACE_OUTER_BOUND ( 'NONE', #23444, .T. ) ;
#12456=CYLINDRICAL_SURFACE ( 'NONE', #45714, 32.00000000000000000 ) ;
#12461=EDGE_LOOP ( 'NONE', ( #44220, #26448, #28866, #4788 ) ) ;
#12467=CARTESIAN_POINT ( 'NONE',  ( 10.00000000000000000, -23.16143007188376757, -73.95703589263997912 ) ) ;
#12472=CARTESIAN_POINT ( 'NONE',  ( 0.000000000000000000, 2.946379043147425492, -75.11764819372145041 ) ) ;
#12475=DIRECTION ( 'NONE',  ( -1.000000000000000000, 0.000000000000000000, -0.000000000000000000 ) ) ;
#12476=DIRECTION ( 'NONE',  ( 0.000000000000000000, 0.8910065241883690090, -0.4539904997395446395 ) ) ;
#12485=EDGE_LOOP ( 'NONE', ( #29353, #31179, #24058, #46017 ) ) ;
#12486=ORIENTED_EDGE ( 'NONE', *, *, #4368, .T. ) ;
#12488=EDGE_CURVE ( 'NONE', #1183, #18610, #313, .T. ) ;
#12489=CIRCLE ( 'NONE', #3887, 32.00000000000000000 ) ;
#12490=DIRECTION ( 'NONE',  ( 0.000000000000000000, 0.000000000000000000, 1.000000000000000000 ) ) ;
#12491=AXIS2_PLACEMENT_3D ( 'NONE', #26332, #37096, #7490 ) ;
#12499=ORIENTED_EDGE ( 'NONE', *, *, #47959, .T. ) ;
#12503=ADVANCED_FACE ( 'NONE', ( #18223 ), #11139, .T. ) ;
#12513=DIRECTION ( 'NONE',  ( -1.000000000000000000, 0.000000000000000000, -0.000000000000000000 ) ) ;
#12515=DIRECTION ( 'NONE',  ( 0.000000000000000000, 0.000000000000000000, 1.000000000000000000 ) ) ;
#12520=EDGE_CURVE ( 'NONE', #42057, #18546, #7471, .T. ) ;
#12529=VERTEX_POINT ( 'NONE', #15054 ) ;
#12530=ORIENTED_EDGE ( 'NONE', *, *, #22932, .F. ) ;
#12531=AXIS2_PLACEMENT_3D ( 'NONE', #14351, #11160, #48355 ) ;
#12534=ORIENTED_EDGE ( 'NONE', *, *, #4353, .F. ) ;
#12540=CIRCLE ( 'NONE', #37546, 77.49900000000000944 ) ;
#12541=AXIS2_PLACEMENT_3D ( 'NONE', #6725, #21652, #6960 ) ;
#12544=EDGE_CURVE ( 'NONE', #38965, #37445, #8118, .T. ) ;
#12547=LINE ( 'NONE', #9576, #44080 ) ;
#12568=FACE_OUTER_BOUND ( 'NONE', #11649, .T. ) ;
#12569=DIRECTION ( 'NONE',  ( -1.000000000000000000, 0.000000000000000000, 0.000000000000000000 ) ) ;
#12571=VERTEX_POINT ( 'NONE', #25571 ) ;
#12575=DIRECTION ( 'NONE',  ( -1.000000000000000000, 0.000000000000000000, -0.000000000000000000 ) ) ;
#12576=DIRECTION ( 'NONE',  ( 0.000000000000000000, 0.000000000000000000, 1.000000000000000000 ) ) ;
#12578=CARTESIAN_POINT ( 'NONE',  ( 0.000000000000000000, -69.42325613327466272, 34.44570377933573724 ) ) ;
#12579=DIRECTION ( 'NONE',  ( -1.000000000000000000, -0.000000000000000000, 0.000000000000000000 ) ) ;
#12580=LINE ( 'NONE', #31438, #40034 ) ;
#12583=DIRECTION ( 'NONE',  ( -1.000000000000000000, 0.000000000000000000, 0.000000000000000000 ) ) ;
#12585=ORIENTED_EDGE ( 'NONE', *, *, #42885, .T. ) ;
#12586=ORIENTED_EDGE ( 'NONE', *, *, #42517, .T. ) ;
#12592=ORIENTED_EDGE ( 'NONE', *, *, #3030, .F. ) ;
#12606=EDGE_CURVE ( 'NONE', #7073, #40831, #26889, .T. ) ;
#12607=CYLINDRICAL_SURFACE ( 'NONE', #46134, 82.00000000000000000 ) ;
#12614=CARTESIAN_POINT ( 'NONE',  ( -10.00000000000000000, 0.000000000000000000, 0.000000000000000000 ) ) ;
#12618=DIRECTION ( 'NONE',  ( -1.000000000000000000, 0.000000000000000000, 0.000000000000000000 ) ) ;
#12619=VERTEX_POINT ( 'NONE', #15306 ) ;
#12620=EDGE_CURVE ( 'NONE', #38853, #2339, #45637, .T. ) ;
#12621=DIRECTION ( 'NONE',  ( -1.000000000000000000, -0.000000000000000000, -0.000000000000000000 ) ) ;
#12624=CARTESIAN_POINT ( 'NONE',  ( 0.000000000000000000, 0.000000000000000000, 0.000000000000000000 ) ) ;
#12626=DIRECTION ( 'NONE',  ( 0.000000000000000000, 0.000000000000000000, 1.000000000000000000 ) ) ;
#12627=DIRECTION ( 'NONE',  ( 0.000000000000000000, 0.000000000000000000, 1.000000000000000000 ) ) ;
#12628=ORIENTED_EDGE ( 'NONE', *, *, #37290, .T. ) ;
#12630=LINE ( 'NONE', #19706, #23789 ) ;
#12632=DIRECTION ( 'NONE',  ( 0.000000000000000000, 0.000000000000000000, 1.000000000000000000 ) ) ;
#12636=ORIENTED_EDGE ( 'NONE', *, *, #30178, .F. ) ;
#12640=AXIS2_PLACEMENT_3D ( 'NONE', #24884, #25116, #43502 ) ;
#12651=ORIENTED_EDGE ( 'NONE', *, *, #1219, .T. ) ;
#12660=ADVANCED_FACE ( 'NONE', ( #8651 ), #15775, .T. ) ;
#12668=ORIENTED_EDGE ( 'NONE', *, *, #23476, .F. ) ;
#12670=AXIS2_PLACEMENT_3D ( 'NONE', #27513, #42689, #31193 ) ;
#12673=FACE_OUTER_BOUND ( 'NONE', #45099, .T. ) ;
#12674=ORIENTED_EDGE ( 'NONE', *, *, #6572, .F. ) ;
#12677=DIRECTION ( 'NONE',  ( -1.000000000000000000, 0.000000000000000000, 0.000000000000000000 ) ) ;
#12683=VERTEX_POINT ( 'NONE', #4999 ) ;
#12698=ORIENTED_EDGE ( 'NONE', *, *, #16321, .T. ) ;
#12699=CARTESIAN_POINT ( 'NONE',  ( 10.00000000000000000, -70.52718814184240159, -26.02418014898383802 ) ) ;
#12700=DIRECTION ( 'NONE',  ( 0.000000000000000000, -0.6494480483301903195, 0.7604059656000252687 ) ) ;
#12713=DIRECTION ( 'NONE',  ( 1.000000000000000000, 0.000000000000000000, 0.000000000000000000 ) ) ;
#12715=DIRECTION ( 'NONE',  ( -1.000000000000000000, 0.000000000000000000, -0.000000000000000000 ) ) ;
#12719=EDGE_CURVE ( 'NONE', #16993, #26599, #5830, .T. ) ;
#12728=CARTESIAN_POINT ( 'NONE',  ( 5.000000000000000000, -63.97538442413463855, 51.29473840253199768 ) ) ;
#12731=CYLINDRICAL_SURFACE ( 'NONE', #42695, 82.00000000000000000 ) ;
#12735=ADVANCED_FACE ( 'NONE', ( #9619 ), #21120, .T. ) ;
#12738=AXIS2_PLACEMENT_3D ( 'NONE', #35446, #30827, #30569 ) ;
#12739=EDGE_LOOP ( 'NONE', ( #17399, #40372, #9874, #39815 ) ) ;
#12742=DIRECTION ( 'NONE',  ( 0.000000000000000000, 0.000000000000000000, 1.000000000000000000 ) ) ;
#12743=DIRECTION ( 'NONE',  ( -1.000000000000000000, 0.000000000000000000, -0.000000000000000000 ) ) ;
#12755=CARTESIAN_POINT ( 'NONE',  ( 10.00000000000000000, 76.66974797899837313, 11.30684508768368524 ) ) ;
#12758=CARTESIAN_POINT ( 'NONE',  ( 10.00000000000000000, 0.000000000000000000, 0.000000000000000000 ) ) ;
#12760=DIRECTION ( 'NONE',  ( 0.000000000000000000, -0.6494480483301903195, 0.7604059656000252687 ) ) ;
#12767=EDGE_CURVE ( 'NONE', #23915, #11671, #34730, .T. ) ;
#12769=CIRCLE ( 'NONE', #40119, 31.99999999999999289 ) ;
#12779=EDGE_CURVE ( 'NONE', #37478, #6985, #13547, .T. ) ;
#12785=ORIENTED_EDGE ( 'NONE', *, *, #6757, .T. ) ;
#12786=FILL_AREA_STYLE ('',( #46313 ) ) ;
#12789=CARTESIAN_POINT ( 'NONE',  ( 0.000000000000000000, 18.89407956138362010, -75.16055320797013906 ) ) ;
#12793=LINE ( 'NONE', #9117, #7468 ) ;
#12795=ORIENTED_EDGE ( 'NONE', *, *, #22006, .F. ) ;
#12804=EDGE_LOOP ( 'NONE', ( #29222, #42099, #26290, #12808 ) ) ;
#12808=ORIENTED_EDGE ( 'NONE', *, *, #26666, .T. ) ;
#12810=FACE_OUTER_BOUND ( 'NONE', #9444, .T. ) ;
#12815=CARTESIAN_POINT ( 'NONE',  ( 0.000000000000000000, -24.73286445877757345, 73.44644590900053061 ) ) ;
#12817=DIRECTION ( 'NONE',  ( -1.000000000000000000, 0.000000000000000000, 0.000000000000000000 ) ) ;
#12823=DIRECTION ( 'NONE',  ( -1.000000000000000000, 0.000000000000000000, -0.000000000000000000 ) ) ;
#12826=VECTOR ( 'NONE', #38972, 1000.000000000000000 ) ;
#12830=EDGE_CURVE ( 'NONE', #37280, #12571, #42582, .T. ) ;
#12834=DIRECTION ( 'NONE',  ( -1.000000000000000000, 0.000000000000000000, -0.000000000000000000 ) ) ;
#12835=ORIENTED_EDGE ( 'NONE', *, *, #23805, .T. ) ;
#12837=DIRECTION ( 'NONE',  ( -1.000000000000000000, 0.000000000000000000, 0.000000000000000000 ) ) ;
#12844=VERTEX_POINT ( 'NONE', #13076 ) ;
#12845=CIRCLE ( 'NONE', #26150, 31.99999999999999289 ) ;
#12851=AXIS2_PLACEMENT_3D ( 'NONE', #34961, #11975, #27893 ) ;
#12858=AXIS2_PLACEMENT_3D ( 'NONE', #38175, #19541, #950 ) ;
#12863=ORIENTED_EDGE ( 'NONE', *, *, #30890, .F. ) ;
#12875=VERTEX_POINT ( 'NONE', #46612 ) ;
#12876=DIRECTION ( 'NONE',  ( 0.000000000000000000, -0.8526401643540970632, 0.5224985647159409163 ) ) ;
#12879=AXIS2_PLACEMENT_3D ( 'NONE', #38949, #42858, #35254 ) ;
#12881=ORIENTED_EDGE ( 'NONE', *, *, #24862, .T. ) ;
#12883=AXIS2_PLACEMENT_3D ( 'NONE', #37820, #30722, #4776 ) ;
#12884=AXIS2_PLACEMENT_3D ( 'NONE', #43170, #31933, #20164 ) ;
#12886=DIRECTION ( 'NONE',  ( 0.000000000000000000, 0.000000000000000000, 1.000000000000000000 ) ) ;
#12892=CIRCLE ( 'NONE', #21472, 82.00000000000000000 ) ;
#12895=DIRECTION ( 'NONE',  ( -1.000000000000000000, 0.000000000000000000, 0.000000000000000000 ) ) ;
#12897=EDGE_CURVE ( 'NONE', #13811, #28502, #41776, .T. ) ;
#12898=AXIS2_PLACEMENT_3D ( 'NONE', #25140, #32727, #47648 ) ;
#12900=CIRCLE ( 'NONE', #47271, 82.00000000000000000 ) ;
#12909=ORIENTED_EDGE ( 'NONE', *, *, #8241, .T. ) ;
#12911=ORIENTED_EDGE ( 'NONE', *, *, #47579, .T. ) ;
#12914=LINE ( 'NONE', #34930, #10911 ) ;
#12926=VERTEX_POINT ( 'NONE', #18161 ) ;
#12934=DIRECTION ( 'NONE',  ( 0.000000000000000000, -0.5877852522924803536, 0.8090169943749422332 ) ) ;
#12941=CARTESIAN_POINT ( 'NONE',  ( 5.000000000000002665, 80.55351364060611274, -15.33399622253396544 ) ) ;
#12944=ORIENTED_EDGE ( 'NONE', *, *, #48300, .T. ) ;
#12948=FACE_OUTER_BOUND ( 'NONE', #11534, .T. ) ;
#12961=EDGE_CURVE ( 'NONE', #29904, #36506, #38674, .T. ) ;
#12964=ORIENTED_EDGE ( 'NONE', *, *, #7177, .T. ) ;
#12966=AXIS2_PLACEMENT_3D ( 'NONE', #43620, #33072, #13282 ) ;
#12973=ORIENTED_EDGE ( 'NONE', *, *, #16747, .T. ) ;
#12980=CIRCLE ( 'NONE', #36416, 82.00000000000000000 ) ;
#12981=DIRECTION ( 'NONE',  ( 0.000000000000000000, 0.000000000000000000, -1.000000000000000000 ) ) ;
#12986=DIRECTION ( 'NONE',  ( 1.000000000000000000, -0.000000000000000000, -0.000000000000000000 ) ) ;
#12992=ORIENTED_EDGE ( 'NONE', *, *, #22877, .T. ) ;
#12993=LINE ( 'NONE', #42849, #21121 ) ;
#12994=CYLINDRICAL_SURFACE ( 'NONE', #6320, 77.49899999999999523 ) ;
#12996=FACE_OUTER_BOUND ( 'NONE', #44737, .T. ) ;
#12998=ORIENTED_EDGE ( 'NONE', *, *, #1281, .T. ) ;
#13005=DIRECTION ( 'NONE',  ( -1.000000000000000000, 0.000000000000000000, 0.000000000000000000 ) ) ;
#13008=ADVANCED_FACE ( 'NONE', ( #25037 ), #3495, .T. ) ;
#13010=DIRECTION ( 'NONE',  ( 0.000000000000000000, -0.9510565162951565288, 0.3090169943749384029 ) ) ;
#13014=CARTESIAN_POINT ( 'NONE',  ( 10.00000000000000000, 56.15606465354958488, 59.75363087400094031 ) ) ;
#13015=CARTESIAN_POINT ( 'NONE',  ( 0.000000000000000000, 27.74655509720669500, 77.16300072079670258 ) ) ;
#13017=AXIS2_PLACEMENT_3D ( 'NONE', #35024, #31866, #12760 ) ;
#13020=CARTESIAN_POINT ( 'NONE',  ( 0.000000000000000000, 50.23322058963348979, 64.81221759200361987 ) ) ;
#13026=CYLINDRICAL_SURFACE ( 'NONE', #15149, 82.00000000000000000 ) ;
#13034=AXIS2_PLACEMENT_3D ( 'NONE', #41647, #34288, #38954 ) ;
#13043=ORIENTED_EDGE ( 'NONE', *, *, #5466, .T. ) ;
#13047=EDGE_CURVE ( 'NONE', #36756, #15863, #8191, .T. ) ;
#13052=ORIENTED_EDGE ( 'NONE', *, *, #3603, .F. ) ;
#13053=DIRECTION ( 'NONE',  ( 0.000000000000000000, 0.000000000000000000, 1.000000000000000000 ) ) ;
#13056=CARTESIAN_POINT ( 'NONE',  ( 10.00000000000000000, 12.93880638057314059, 76.41127070299278046 ) ) ;
#13057=CARTESIAN_POINT ( 'NONE',  ( 0.000000000000000000, -79.10210256391353312, -21.60688246758668640 ) ) ;
#13059=ORIENTED_EDGE ( 'NONE', *, *, #2245, .T. ) ;
#13062=CARTESIAN_POINT ( 'NONE',  ( 10.00000000000000000, 75.11725578898472122, -2.956366410619845730 ) ) ;
#13067=CARTESIAN_POINT ( 'NONE',  ( 10.00000000000000000, 0.000000000000000000, 0.000000000000000000 ) ) ;
#13068=AXIS2_PLACEMENT_3D ( 'NONE', #22902, #4551, #23381 ) ;
#13070=CYLINDRICAL_SURFACE ( 'NONE', #21244, 31.99999999999999289 ) ;
#13071=DIRECTION ( 'NONE',  ( 0.000000000000000000, 0.000000000000000000, 1.000000000000000000 ) ) ;
#13076=CARTESIAN_POINT ( 'NONE',  ( 0.000000000000000000, 60.67117009219216328, -55.16347631942977614 ) ) ;
#13077=CIRCLE ( 'NONE', #29487, 77.49899999999998101 ) ;
#13078=EDGE_LOOP ( 'NONE', ( #17891, #26992, #46119, #14165 ) ) ;
#13082=CIRCLE ( 'NONE', #8384, 82.00000000000000000 ) ;
#13083=LINE ( 'NONE', #9163, #368 ) ;
#13084=ORIENTED_EDGE ( 'NONE', *, *, #31893, .F. ) ;
#13093=ORIENTED_EDGE ( 'NONE', *, *, #13205, .F. ) ;
#13097=EDGE_CURVE ( 'NONE', #9519, #26793, #41200, .T. ) ;
#13099=DIRECTION ( 'NONE',  ( 0.000000000000000000, -0.7604059656000369261, 0.6494480483301766638 ) ) ;
#13106=ORIENTED_EDGE ( 'NONE', *, *, #16689, .F. ) ;
#13116=EDGE_CURVE ( 'NONE', #34190, #46809, #45101, .T. ) ;
#13118=DIRECTION ( 'NONE',  ( 0.000000000000000000, 1.000000000000000000, 0.000000000000000000 ) ) ;
#13124=CYLINDRICAL_SURFACE ( 'NONE', #10298, 31.99999999999998579 ) ;
#13126=DIRECTION ( 'NONE',  ( 1.000000000000000000, 0.000000000000000000, 0.000000000000000000 ) ) ;
#13133=DIRECTION ( 'NONE',  ( -1.000000000000000000, 0.000000000000000000, 0.000000000000000000 ) ) ;
#13135=VERTEX_POINT ( 'NONE', #31144 ) ;
#13140=ORIENTED_EDGE ( 'NONE', *, *, #7660, .F. ) ;
#13142=ORIENTED_EDGE ( 'NONE', *, *, #23288, .T. ) ;
#13143=CIRCLE ( 'NONE', #3740, 77.49899999999999523 ) ;
#13144=VERTEX_POINT ( 'NONE', #31633 ) ;
#13147=ADVANCED_FACE ( 'NONE', ( #42879 ), #13026, .T. ) ;
#13148=VERTEX_POINT ( 'NONE', #46066 ) ;
#13153=ORIENTED_EDGE ( 'NONE', *, *, #40118, .T. ) ;
#13155=VERTEX_POINT ( 'NONE', #28173 ) ;
#13163=DIRECTION ( 'NONE',  ( 0.000000000000000000, 0.000000000000000000, 1.000000000000000000 ) ) ;
#13168=ORIENTED_EDGE ( 'NONE', *, *, #16492, .T. ) ;
#13172=ORIENTED_EDGE ( 'NONE', *, *, #46546, .F. ) ;
#13178=LINE ( 'NONE', #28106, #30076 ) ;
#13186=VERTEX_POINT ( 'NONE', #5197 ) ;
#13189=LINE ( 'NONE', #17091, #38769 ) ;
#13190=ORIENTED_EDGE ( 'NONE', *, *, #19572, .F. ) ;
#13194=VERTEX_POINT ( 'NONE', #16213 ) ;
#13196=AXIS2_PLACEMENT_3D ( 'NONE', #43740, #6537, #32952 ) ;
#13198=DIRECTION ( 'NONE',  ( -1.000000000000000000, -0.000000000000000000, -0.000000000000000000 ) ) ;
#13201=ORIENTED_EDGE ( 'NONE', *, *, #14653, .T. ) ;
#13205=EDGE_CURVE ( 'NONE', #34289, #31027, #34662, .T. ) ;
#13207=ORIENTED_EDGE ( 'NONE', *, *, #4353, .T. ) ;
#13217=EDGE_CURVE ( 'NONE', #10347, #11083, #47182, .T. ) ;
#13222=CARTESIAN_POINT ( 'NONE',  ( 10.00000000000000000, 75.11764819372142199, 2.946379043147685728 ) ) ;
#13223=EDGE_LOOP ( 'NONE', ( #30013, #9481, #20485, #13172 ) ) ;
#13224=DIRECTION ( 'NONE',  ( -1.000000000000000000, -0.000000000000000000, -0.000000000000000000 ) ) ;
#13232=CARTESIAN_POINT ( 'NONE',  ( 0.000000000000000000, 74.65374052328648702, 8.840884882375350529 ) ) ;
#13238=AXIS2_PLACEMENT_3D ( 'NONE', #37770, #37527, #18679 ) ;
#13242=DIRECTION ( 'NONE',  ( 0.000000000000000000, 0.000000000000000000, 1.000000000000000000 ) ) ;
#13244=CARTESIAN_POINT ( 'NONE',  ( 10.00000000000000000, -59.03961581697367933, -46.53671651294010303 ) ) ;
#13257=EDGE_LOOP ( 'NONE', ( #26573, #18526, #22155, #31131 ) ) ;
#13261=EDGE_CURVE ( 'NONE', #33075, #27936, #15909, .T. ) ;
#13265=AXIS2_PLACEMENT_3D ( 'NONE', #45170, #41738, #33892 ) ;
#13269=CARTESIAN_POINT ( 'NONE',  ( 0.000000000000000000, 60.67117009219135326, 55.16347631943062169 ) ) ;
#13271=EDGE_CURVE ( 'NONE', #17893, #12095, #22158, .T. ) ;
#13277=ADVANCED_FACE ( 'NONE', ( #11203 ), #33704, .T. ) ;
#13280=DIRECTION ( 'NONE',  ( -1.000000000000000000, 0.000000000000000000, 0.000000000000000000 ) ) ;
#13281=CARTESIAN_POINT ( 'NONE',  ( 0.000000000000000000, 34.94270380257741948, -74.18225833017852722 ) ) ;
#13282=DIRECTION ( 'NONE',  ( 0.000000000000000000, 0.000000000000000000, 1.000000000000000000 ) ) ;
#13292=ORIENTED_EDGE ( 'NONE', *, *, #15260, .T. ) ;
#13299=AXIS2_PLACEMENT_3D ( 'NONE', #10036, #39907, #21283 ) ;
#13307=CARTESIAN_POINT ( 'NONE',  ( 10.00000000000000000, 65.58780272294076497, 36.73666225445916211 ) ) ;
#13308=DIRECTION ( 'NONE',  ( -1.000000000000000000, 0.000000000000000000, -0.000000000000000000 ) ) ;
#13311=AXIS2_PLACEMENT_3D ( 'NONE', #11304, #10314, #14728 ) ;
#13312=ORIENTED_EDGE ( 'NONE', *, *, #39246, .F. ) ;
#13313=FACE_OUTER_BOUND ( 'NONE', #13257, .T. ) ;
#13315=DIRECTION ( 'NONE',  ( 0.000000000000000000, 0.000000000000000000, 1.000000000000000000 ) ) ;
#13319=EDGE_CURVE ( 'NONE', #19209, #36599, #29797, .T. ) ;
#13321=EDGE_CURVE ( 'NONE', #16029, #2989, #46422, .T. ) ;
#13326=CIRCLE ( 'NONE', #40680, 82.00000000000000000 ) ;
#13327=EDGE_CURVE ( 'NONE', #37807, #4251, #44841, .T. ) ;
#13330=VECTOR ( 'NONE', #34749, 1000.000000000000000 ) ;
#13339=DIRECTION ( 'NONE',  ( -1.000000000000000000, 0.000000000000000000, 0.000000000000000000 ) ) ;
#13346=DIRECTION ( 'NONE',  ( 0.000000000000000000, 0.000000000000000000, 1.000000000000000000 ) ) ;
#13348=DIRECTION ( 'NONE',  ( 0.000000000000000000, 0.000000000000000000, 1.000000000000000000 ) ) ;
#13349=CARTESIAN_POINT ( 'NONE',  ( 5.000000000000000000, -50.23322058963298531, -64.81221759200398935 ) ) ;
#13350=CARTESIAN_POINT ( 'NONE',  ( 0.000000000000000000, 76.41127070299290835, -12.93880638057231991 ) ) ;
#13355=CARTESIAN_POINT ( 'NONE',  ( 10.00000000000000000, -55.20638768913724448, -51.02545421589383068 ) ) ;
#13363=DIRECTION ( 'NONE',  ( 0.000000000000000000, 0.000000000000000000, 1.000000000000000000 ) ) ;
#13374=VECTOR ( 'NONE', #202, 1000.000000000000000 ) ;
#13375=ORIENTED_EDGE ( 'NONE', *, *, #31092, .T. ) ;
#13378=CARTESIAN_POINT ( 'NONE',  ( 5.000000000000002665, 3.894527615417891830, 81.90746397400390322 ) ) ;
#13379=VERTEX_POINT ( 'NONE', #33235 ) ;
#13381=EDGE_CURVE ( 'NONE', #10994, #5603, #2613, .T. ) ;
#13383=DIRECTION ( 'NONE',  ( 0.000000000000000000, 0.000000000000000000, 1.000000000000000000 ) ) ;
#13386=ORIENTED_EDGE ( 'NONE', *, *, #44607, .F. ) ;
#13387=ORIENTED_EDGE ( 'NONE', *, *, #5566, .F. ) ;
#13388=DIRECTION ( 'NONE',  ( -1.000000000000000000, -0.000000000000000000, -0.000000000000000000 ) ) ;
#13395=VERTEX_POINT ( 'NONE', #1399 ) ;
#13398=VERTEX_POINT ( 'NONE', #19260 ) ;
#13399=LINE ( 'NONE', #18191, #44500 ) ;
#13400=ORIENTED_EDGE ( 'NONE', *, *, #9337, .T. ) ;
#13403=DIRECTION ( 'NONE',  ( 0.000000000000000000, 0.8526401643540936215, -0.5224985647159469115 ) ) ;
#13410=CIRCLE ( 'NONE', #12541, 82.00000000000000000 ) ;
#13414=DIRECTION ( 'NONE',  ( 0.000000000000000000, 0.2334453638559060296, -0.9723699203976764460 ) ) ;
#13416=DIRECTION ( 'NONE',  ( 0.000000000000000000, -0.9723699203976740035, -0.2334453638559160216 ) ) ;
#13420=EDGE_LOOP ( 'NONE', ( #40786, #3390, #34381, #31026 ) ) ;
#13421=EDGE_CURVE ( 'NONE', #45038, #41084, #29183, .T. ) ;
#13424=DIRECTION ( 'NONE',  ( -1.000000000000000000, 0.000000000000000000, 0.000000000000000000 ) ) ;
#13426=EDGE_CURVE ( 'NONE', #7999, #31795, #19985, .T. ) ;
#13427=CARTESIAN_POINT ( 'NONE',  ( 10.00000000000000000, 76.41127070299273782, 12.93880638057342836 ) ) ;
#13435=CARTESIAN_POINT ( 'NONE',  ( 10.00000000000000000, 74.18225833017937987, -34.94270380257560049 ) ) ;
#13441=EDGE_CURVE ( 'NONE', #23235, #31274, #38602, .T. ) ;
#13445=CIRCLE ( 'NONE', #32219, 77.49899999999999523 ) ;
#13450=EDGE_CURVE ( 'NONE', #39014, #39398, #27566, .T. ) ;
#13460=VERTEX_POINT ( 'NONE', #45950 ) ;
#13462=DIRECTION ( 'NONE',  ( 0.000000000000000000, 0.000000000000000000, 1.000000000000000000 ) ) ;
#13464=ORIENTED_EDGE ( 'NONE', *, *, #44499, .F. ) ;
#13466=CARTESIAN_POINT ( 'NONE',  ( 0.000000000000000000, 40.65526001592612459, 71.21200624218811015 ) ) ;
#13467=VERTEX_POINT ( 'NONE', #34919 ) ;
#13475=CARTESIAN_POINT ( 'NONE',  ( 0.000000000000000000, 79.10210256391398786, -21.60688246758503084 ) ) ;
#13476=AXIS2_PLACEMENT_3D ( 'NONE', #9690, #13611, #28547 ) ;
#13486=DIRECTION ( 'NONE',  ( 0.000000000000000000, 0.000000000000000000, -1.000000000000000000 ) ) ;
#13496=EDGE_CURVE ( 'NONE', #21020, #28981, #12185, .T. ) ;
#13502=DIRECTION ( 'NONE',  ( 1.000000000000000000, -0.000000000000000000, -0.000000000000000000 ) ) ;
#13510=VECTOR ( 'NONE', #5258, 1000.000000000000000 ) ;
#13511=VERTEX_POINT ( 'NONE', #42760 ) ;
#13512=CARTESIAN_POINT ( 'NONE',  ( 0.000000000000000000, 0.000000000000000000, 0.000000000000000000 ) ) ;
#13513=DIRECTION ( 'NONE',  ( 0.000000000000000000, 0.000000000000000000, 1.000000000000000000 ) ) ;
#13516=CARTESIAN_POINT ( 'NONE',  ( 10.00000000000000000, -35.91791733033525702, 68.67312586194982771 ) ) ;
#13517=DIRECTION ( 'NONE',  ( -1.000000000000000000, 0.000000000000000000, -0.000000000000000000 ) ) ;
#13523=DIRECTION ( 'NONE',  ( -1.000000000000000000, 0.000000000000000000, -0.000000000000000000 ) ) ;
#13525=CARTESIAN_POINT ( 'NONE',  ( 0.000000000000000000, -72.35432306680469594, -20.40083707022958848 ) ) ;
#13532=ADVANCED_FACE ( 'NONE', ( #6271 ), #6040, .T. ) ;
#13533=CARTESIAN_POINT ( 'NONE',  ( 5.000000000000002665, -3.894527615417340272, -81.90746397400393164 ) ) ;
#13534=DIRECTION ( 'NONE',  ( -1.000000000000000000, 0.000000000000000000, -0.000000000000000000 ) ) ;
#13536=DIRECTION ( 'NONE',  ( -1.000000000000000000, -0.000000000000000000, -0.000000000000000000 ) ) ;
#13540=CIRCLE ( 'NONE', #36200, 31.99999999999999289 ) ;
#13547=LINE ( 'NONE', #24087, #20652 ) ;
#13550=EDGE_CURVE ( 'NONE', #1729, #47158, #16621, .T. ) ;
#13554=CIRCLE ( 'NONE', #9666, 77.49899999999999523 ) ;
#13559=EDGE_LOOP ( 'NONE', ( #10801, #41014, #15036, #45501 ) ) ;
#13560=CIRCLE ( 'NONE', #26844, 77.49900000000000944 ) ;
#13562=ORIENTED_EDGE ( 'NONE', *, *, #43709, .T. ) ;
#13565=CIRCLE ( 'NONE', #30807, 31.99999999999999645 ) ;
#13566=LINE ( 'NONE', #39032, #35558 ) ;
#13569=CIRCLE ( 'NONE', #9643, 77.49900000000000944 ) ;
#13571=CYLINDRICAL_SURFACE ( 'NONE', #48338, 31.99999999999999289 ) ;
#13572=CARTESIAN_POINT ( 'NONE',  ( 10.00000000000000000, 65.64334221924966073, -41.19522573413664190 ) ) ;
#13575=VECTOR ( 'NONE', #31397, 1000.000000000000000 ) ;
#13579=AXIS2_PLACEMENT_3D ( 'NONE', #33570, #45308, #28 ) ;
#13581=CIRCLE ( 'NONE', #38612, 31.99999999999999645 ) ;
#13584=DIRECTION ( 'NONE',  ( 0.000000000000000000, 0.000000000000000000, 1.000000000000000000 ) ) ;
#13591=DIRECTION ( 'NONE',  ( -1.000000000000000000, -0.000000000000000000, 0.000000000000000000 ) ) ;
#13593=FACE_OUTER_BOUND ( 'NONE', #48289, .T. ) ;
#13603=VERTEX_POINT ( 'NONE', #25097 ) ;
#13604=EDGE_CURVE ( 'NONE', #8489, #40628, #40830, .T. ) ;
#13608=AXIS2_PLACEMENT_3D ( 'NONE', #31754, #28288, #20222 ) ;
#13611=DIRECTION ( 'NONE',  ( -1.000000000000000000, 0.000000000000000000, -0.000000000000000000 ) ) ;
#13615=ORIENTED_EDGE ( 'NONE', *, *, #18288, .T. ) ;
#13650=CARTESIAN_POINT ( 'NONE',  ( 10.00000000000000000, 59.46389618802034960, -49.70050353004825894 ) ) ;
#13658=AXIS2_PLACEMENT_3D ( 'NONE', #19152, #8857, #8382 ) ;
#13661=LINE ( 'NONE', #3539, #40395 ) ;
#13665=ADVANCED_FACE ( 'NONE', ( #24381 ), #39314, .T. ) ;
#13666=VECTOR ( 'NONE', #16068, 1000.000000000000000 ) ;
#13667=ADVANCED_FACE ( 'NONE', ( #31992 ), #47136, .T. ) ;
#13669=CARTESIAN_POINT ( 'NONE',  ( 10.00000000000000000, 35.91791733033475253, 68.67312586195009771 ) ) ;
#13674=DIRECTION ( 'NONE',  ( -1.000000000000000000, 0.000000000000000000, -0.000000000000000000 ) ) ;
#13675=DIRECTION ( 'NONE',  ( -1.000000000000000000, -0.000000000000000000, 0.000000000000000000 ) ) ;
#13679=AXIS2_PLACEMENT_3D ( 'NONE', #34712, #16365, #35441 ) ;
#13689=VERTEX_POINT ( 'NONE', #32684 ) ;
#13692=ORIENTED_EDGE ( 'NONE', *, *, #15889, .F. ) ;
#13699=DIRECTION ( 'NONE',  ( -1.000000000000000000, 0.000000000000000000, 0.000000000000000000 ) ) ;
#13700=EDGE_CURVE ( 'NONE', #39957, #45900, #40072, .T. ) ;
#13701=CIRCLE ( 'NONE', #28553, 31.99999999999999289 ) ;
#13702=DIRECTION ( 'NONE',  ( 0.000000000000000000, 0.000000000000000000, -1.000000000000000000 ) ) ;
#13706=DIRECTION ( 'NONE',  ( 0.000000000000000000, 0.000000000000000000, 1.000000000000000000 ) ) ;
#13714=CARTESIAN_POINT ( 'NONE',  ( 0.000000000000000000, 80.28980883073758434, 16.65972982744963460 ) ) ;
#13716=ORIENTED_EDGE ( 'NONE', *, *, #197, .F. ) ;
#13718=LINE ( 'NONE', #21279, #42579 ) ;
#13723=EDGE_CURVE ( 'NONE', #40761, #8066, #10903, .T. ) ;
#13729=DIRECTION ( 'NONE',  ( 0.000000000000000000, 0.6494480483301793283, 0.7604059656000345946 ) ) ;
#13730=FACE_OUTER_BOUND ( 'NONE', #2633, .T. ) ;
#13731=CARTESIAN_POINT ( 'NONE',  ( 0.000000000000000000, -65.64334221924882229, -41.19522573413803457 ) ) ;
#13732=CARTESIAN_POINT ( 'NONE',  ( 5.000000000000002665, 15.33399622253481986, 80.55351364060595643 ) ) ;
#13733=CARTESIAN_POINT ( 'NONE',  ( 10.00000000000000000, -31.47745569255189224, 68.26794271651249346 ) ) ;
#13743=AXIS2_PLACEMENT_3D ( 'NONE', #35554, #20610, #8620 ) ;
#13749=ORIENTED_EDGE ( 'NONE', *, *, #27705, .F. ) ;
#13753=VECTOR ( 'NONE', #20541, 1000.000000000000000 ) ;
#13758=ORIENTED_EDGE ( 'NONE', *, *, #11964, .T. ) ;
#13765=CIRCLE ( 'NONE', #38755, 82.00000000000000000 ) ;
#13766=EDGE_CURVE ( 'NONE', #36599, #26190, #11142, .T. ) ;
#13769=CARTESIAN_POINT ( 'NONE',  ( 0.000000000000000000, -77.19088730480518734, -6.903761155838607166 ) ) ;
#13772=ORIENTED_EDGE ( 'NONE', *, *, #21101, .T. ) ;
#13774=VERTEX_POINT ( 'NONE', #3792 ) ;
#13779=DIRECTION ( 'NONE',  ( 0.000000000000000000, -0.2334453638559127742, 0.9723699203976748917 ) ) ;
#13790=DIRECTION ( 'NONE',  ( 0.000000000000000000, 0.000000000000000000, 1.000000000000000000 ) ) ;
#13794=CARTESIAN_POINT ( 'NONE',  ( -10.00000000000000000, 0.000000000000000000, 0.000000000000000000 ) ) ;
#13797=CARTESIAN_POINT ( 'NONE',  ( 0.000000000000000000, 0.8261519478441983200, -77.49459641780885022 ) ) ;
#13799=ORIENTED_EDGE ( 'NONE', *, *, #11939, .F. ) ;
#13805=CARTESIAN_POINT ( 'NONE',  ( 10.00000000000000000, 0.000000000000000000, 0.000000000000000000 ) ) ;
#13809=CIRCLE ( 'NONE', #26314, 77.49899999999999523 ) ;
#13811=VERTEX_POINT ( 'NONE', #25330 ) ;
#13812=EDGE_LOOP ( 'NONE', ( #28768, #12253, #39651, #46076 ) ) ;
#13822=ADVANCED_FACE ( 'NONE', ( #23122 ), #23358, .T. ) ;
#13827=DIRECTION ( 'NONE',  ( -1.000000000000000000, -0.000000000000000000, -0.000000000000000000 ) ) ;
#13830=EDGE_CURVE ( 'NONE', #41873, #12437, #36177, .T. ) ;
#13831=CIRCLE ( 'NONE', #33353, 77.49900000000000944 ) ;
#13832=ORIENTED_EDGE ( 'NONE', *, *, #32230, .T. ) ;
#13833=DIRECTION ( 'NONE',  ( -1.000000000000000000, 0.000000000000000000, -0.000000000000000000 ) ) ;
#13834=ORIENTED_EDGE ( 'NONE', *, *, #43653, .F. ) ;
#13835=ORIENTED_EDGE ( 'NONE', *, *, #34986, .T. ) ;
#13836=EDGE_CURVE ( 'NONE', #24941, #45240, #2565, .T. ) ;
#13844=CARTESIAN_POINT ( 'NONE',  ( 0.000000000000000000, -59.03342792756297541, 46.54456581323783126 ) ) ;
#13847=DIRECTION ( 'NONE',  ( 0.000000000000000000, 0.000000000000000000, -1.000000000000000000 ) ) ;
#13855=AXIS2_PLACEMENT_3D ( 'NONE', #12409, #38846, #17028 ) ;
#13856=EDGE_CURVE ( 'NONE', #15854, #23327, #4759, .T. ) ;
#13860=CYLINDRICAL_SURFACE ( 'NONE', #48052, 82.00000000000000000 ) ;
#13864=VERTEX_POINT ( 'NONE', #27523 ) ;
#13867=EDGE_LOOP ( 'NONE', ( #3098, #3444, #25159, #17655 ) ) ;
#13870=ORIENTED_EDGE ( 'NONE', *, *, #33417, .T. ) ;
#13872=AXIS2_PLACEMENT_3D ( 'NONE', #31134, #27950, #39187 ) ;
#13879=DIRECTION ( 'NONE',  ( 0.000000000000000000, 0.000000000000000000, 1.000000000000000000 ) ) ;
#13885=VERTEX_POINT ( 'NONE', #4525 ) ;
#13888=ADVANCED_FACE ( 'NONE', ( #30238 ), #607, .T. ) ;
#13892=DIRECTION ( 'NONE',  ( -1.000000000000000000, -0.000000000000000000, -0.000000000000000000 ) ) ;
#13897=ORIENTED_EDGE ( 'NONE', *, *, #13441, .F. ) ;
#13899=DIRECTION ( 'NONE',  ( 1.000000000000000000, 0.000000000000000000, -0.000000000000000000 ) ) ;
#13900=DIRECTION ( 'NONE',  ( -1.000000000000000000, 0.000000000000000000, 0.000000000000000000 ) ) ;
#13902=CARTESIAN_POINT ( 'NONE',  ( 10.00000000000000000, 0.000000000000000000, 0.000000000000000000 ) ) ;
#13904=ORIENTED_EDGE ( 'NONE', *, *, #24051, .T. ) ;
#13910=ORIENTED_EDGE ( 'NONE', *, *, #37128, .F. ) ;
#13917=CIRCLE ( 'NONE', #31130, 77.49899999999999523 ) ;
#13918=CARTESIAN_POINT ( 'NONE',  ( 0.000000000000000000, -39.47590169984898978, 71.87247863392400404 ) ) ;
#13937=CARTESIAN_POINT ( 'NONE',  ( 10.00000000000000000, -71.91182617369167929, -28.89263327155822481 ) ) ;
#13939=AXIS2_PLACEMENT_3D ( 'NONE', #21840, #29915, #3978 ) ;
#13943=ORIENTED_EDGE ( 'NONE', *, *, #48121, .T. ) ;
#13947=ORIENTED_EDGE ( 'NONE', *, *, #19485, .F. ) ;
#13953=DIRECTION ( 'NONE',  ( 0.000000000000000000, 0.000000000000000000, -1.000000000000000000 ) ) ;
#13956=DIRECTION ( 'NONE',  ( 0.000000000000000000, 0.9723699203976756689, 0.2334453638559095268 ) ) ;
#13959=CARTESIAN_POINT ( 'NONE',  ( 0.000000000000000000, 0.000000000000000000, 0.000000000000000000 ) ) ;
#13960=AXIS2_PLACEMENT_3D ( 'NONE', #1360, #20675, #24112 ) ;
#13961=CARTESIAN_POINT ( 'NONE',  ( 0.000000000000000000, 0.000000000000000000, 0.000000000000000000 ) ) ;
#13965=EDGE_CURVE ( 'NONE', #361, #29885, #29146, .T. ) ;
#13966=DIRECTION ( 'NONE',  ( -1.000000000000000000, 0.000000000000000000, -0.000000000000000000 ) ) ;
#13967=EDGE_CURVE ( 'NONE', #17338, #45908, #2289, .T. ) ;
#13972=CARTESIAN_POINT ( 'NONE',  ( 10.00000000000000000, 0.000000000000000000, 0.000000000000000000 ) ) ;
#13973=LINE ( 'NONE', #25468, #40171 ) ;
#13978=EDGE_CURVE ( 'NONE', #45131, #23071, #11176, .T. ) ;
#13981=ORIENTED_EDGE ( 'NONE', *, *, #32008, .T. ) ;
#13983=FACE_OUTER_BOUND ( 'NONE', #41170, .T. ) ;
#13987=CIRCLE ( 'NONE', #13196, 31.99999999999999289 ) ;
#13988=CIRCLE ( 'NONE', #39796, 77.49899999999999523 ) ;
#13992=DIRECTION ( 'NONE',  ( -1.000000000000000000, -0.000000000000000000, 0.000000000000000000 ) ) ;
#13995=EDGE_CURVE ( 'NONE', #25106, #43867, #7252, .T. ) ;
#14003=DIRECTION ( 'NONE',  ( -1.000000000000000000, 0.000000000000000000, -0.000000000000000000 ) ) ;
#14006=CARTESIAN_POINT ( 'NONE',  ( 10.00000000000000000, -59.03961581697367933, -46.53671651294010303 ) ) ;
#14007=FACE_OUTER_BOUND ( 'NONE', #28637, .T. ) ;
#14015=ORIENTED_EDGE ( 'NONE', *, *, #27478, .F. ) ;
#14016=DIRECTION ( 'NONE',  ( -1.000000000000000000, 0.000000000000000000, -0.000000000000000000 ) ) ;
#14018=CARTESIAN_POINT ( 'NONE',  ( 0.000000000000000000, 0.000000000000000000, 0.000000000000000000 ) ) ;
#14019=DIRECTION ( 'NONE',  ( 0.000000000000000000, -0.9238795325112821866, -0.3826834323651006065 ) ) ;
#14021=CARTESIAN_POINT ( 'NONE',  ( 10.00000000000000000, -36.72794159290288718, 65.59268652807197952 ) ) ;
#14023=VERTEX_POINT ( 'NONE', #21125 ) ;
#14028=CIRCLE ( 'NONE', #12491, 31.99999999999999645 ) ;
#14035=ORIENTED_EDGE ( 'NONE', *, *, #15434, .T. ) ;
#14036=AXIS2_PLACEMENT_3D ( 'NONE', #4257, #19170, #15743 ) ;
#14040=EDGE_CURVE ( 'NONE', #16500, #24955, #24091, .T. ) ;
#14044=EDGE_CURVE ( 'NONE', #15799, #3669, #47083, .T. ) ;
#14047=ORIENTED_EDGE ( 'NONE', *, *, #45937, .F. ) ;
#14050=DIRECTION ( 'NONE',  ( 0.000000000000000000, -0.3826834323650772363, -0.9238795325112919565 ) ) ;
#14055=ORIENTED_EDGE ( 'NONE', *, *, #1829, .F. ) ;
#14058=ORIENTED_EDGE ( 'NONE', *, *, #28283, .F. ) ;
#14061=AXIS2_PLACEMENT_3D ( 'NONE', #3800, #14594, #33423 ) ;
#14064=CARTESIAN_POINT ( 'NONE',  ( 10.00000000000000000, -0.8261519478436571973, 77.49459641780886443 ) ) ;
#14067=CARTESIAN_POINT ( 'NONE',  ( 10.00000000000000000, -68.26794271651239399, -31.47745569255214093 ) ) ;
#14069=DIRECTION ( 'NONE',  ( 1.000000000000000000, 0.000000000000000000, 0.000000000000000000 ) ) ;
#14073=VERTEX_POINT ( 'NONE', #47331 ) ;
#14077=DIRECTION ( 'NONE',  ( 0.000000000000000000, -0.07845909572785221553, 0.9969173337331274087 ) ) ;
#14079=CARTESIAN_POINT ( 'NONE',  ( 50.00005079999999680, 0.000000000000000000, 12.50000000000000000 ) ) ;
#14081=DIRECTION ( 'NONE',  ( -1.000000000000000000, -0.000000000000000000, -0.000000000000000000 ) ) ;
#14087=EDGE_CURVE ( 'NONE', #46808, #45623, #33030, .T. ) ;
#14089=ORIENTED_EDGE ( 'NONE', *, *, #44801, .F. ) ;
#14090=AXIS2_PLACEMENT_3D ( 'NONE', #12374, #5023, #34874 ) ;
#14093=AXIS2_PLACEMENT_3D ( 'NONE', #32584, #10302, #40427 ) ;
#14096=AXIS2_PLACEMENT_3D ( 'NONE', #27659, #5385, #46510 ) ;
#14097=DIRECTION ( 'NONE',  ( -1.000000000000000000, 0.000000000000000000, 0.000000000000000000 ) ) ;
#14105=DIRECTION ( 'NONE',  ( -1.000000000000000000, -0.000000000000000000, -0.000000000000000000 ) ) ;
#14106=DIRECTION ( 'NONE',  ( 0.000000000000000000, -0.3826834323650970537, 0.9238795325112838519 ) ) ;
#14124=VERTEX_POINT ( 'NONE', #36546 ) ;
#14127=CARTESIAN_POINT ( 'NONE',  ( 0.000000000000000000, -59.03342792756231461, -46.54456581323868392 ) ) ;
#14133=AXIS2_PLACEMENT_3D ( 'NONE', #37892, #26398, #19280 ) ;
#14134=CYLINDRICAL_SURFACE ( 'NONE', #17861, 32.00000000000000000 ) ;
#14138=CARTESIAN_POINT ( 'NONE',  ( 0.000000000000000000, -55.20638768913797634, 51.02545421589302777 ) ) ;
#14142=CIRCLE ( 'NONE', #31346, 77.49899999999999523 ) ;
#14145=LINE ( 'NONE', #30292, #26323 ) ;
#14147=CARTESIAN_POINT ( 'NONE',  ( 0.000000000000000000, 73.95703589264006439, -23.16143007188350822 ) ) ;
#14155=VERTEX_POINT ( 'NONE', #44379 ) ;
#14160=AXIS2_PLACEMENT_3D ( 'NONE', #535, #5412, #34287 ) ;
#14162=DIRECTION ( 'NONE',  ( 0.000000000000000000, 0.7071067811865487940, -0.7071067811865462405 ) ) ;
#14164=CIRCLE ( 'NONE', #18866, 82.00000000000000000 ) ;
#14165=ORIENTED_EDGE ( 'NONE', *, *, #1054, .T. ) ;
#14170=VERTEX_POINT ( 'NONE', #37024 ) ;
#14174=AXIS2_PLACEMENT_3D ( 'NONE', #46515, #39160, #20543 ) ;
#14177=ORIENTED_EDGE ( 'NONE', *, *, #8716, .F. ) ;
#14182=ORIENTED_EDGE ( 'NONE', *, *, #32861, .T. ) ;
#14184=DIRECTION ( 'NONE',  ( -1.000000000000000000, -0.000000000000000000, -0.000000000000000000 ) ) ;
#14186=ORIENTED_EDGE ( 'NONE', *, *, #40834, .F. ) ;
#14201=CARTESIAN_POINT ( 'NONE',  ( 5.000000000000000000, -59.75363087400035056, -56.15606465355021015 ) ) ;
#14202=AXIS2_PLACEMENT_3D ( 'NONE', #46160, #5288, #46884 ) ;
#14210=DIRECTION ( 'NONE',  ( -1.000000000000000000, -0.000000000000000000, -0.000000000000000000 ) ) ;
#14231=AXIS2_PLACEMENT_3D ( 'NONE', #34643, #30754, #15354 ) ;
#14237=EDGE_CURVE ( 'NONE', #7731, #34659, #21366, .T. ) ;
#14238=DIRECTION ( 'NONE',  ( -1.000000000000000000, -0.000000000000000000, 0.000000000000000000 ) ) ;
#14245=ORIENTED_EDGE ( 'NONE', *, *, #19334, .T. ) ;
#14246=AXIS2_PLACEMENT_3D ( 'NONE', #45731, #11229, #40841 ) ;
#14248=DIRECTION ( 'NONE',  ( 0.000000000000000000, -0.9969173337331271867, -0.07845909572785568498 ) ) ;
#14251=ORIENTED_EDGE ( 'NONE', *, *, #29680, .F. ) ;
#14252=ADVANCED_FACE ( 'NONE', ( #34544 ), #783, .T. ) ;
#14253=CARTESIAN_POINT ( 'NONE',  ( 10.00000000000000000, 0.8261519478441983200, -77.49459641780885022 ) ) ;
#14258=CARTESIAN_POINT ( 'NONE',  ( 10.00000000000000000, 0.000000000000000000, 77.49899999999999523 ) ) ;
#14259=CYLINDRICAL_SURFACE ( 'NONE', #6026, 82.00000000000000000 ) ;
#14263=DIRECTION ( 'NONE',  ( -1.000000000000000000, -0.000000000000000000, -0.000000000000000000 ) ) ;
#14265=CYLINDRICAL_SURFACE ( 'NONE', #13939, 82.00000000000000000 ) ;
#14276=AXIS2_PLACEMENT_3D ( 'NONE', #17189, #12817, #14440 ) ;
#14287=VERTEX_POINT ( 'NONE', #37510 ) ;
#14289=AXIS2_PLACEMENT_3D ( 'NONE', #35278, #2011, #1754 ) ;
#14291=CYLINDRICAL_SURFACE ( 'NONE', #11629, 31.99999999999999289 ) ;
#14299=VERTEX_POINT ( 'NONE', #15485 ) ;
#14301=DIRECTION ( 'NONE',  ( 0.000000000000000000, 0.000000000000000000, 1.000000000000000000 ) ) ;
#14306=DIRECTION ( 'NONE',  ( -1.000000000000000000, 0.000000000000000000, 0.000000000000000000 ) ) ;
#14307=EDGE_LOOP ( 'NONE', ( #24996, #36068, #20130, #30734 ) ) ;
#14309=ADVANCED_FACE ( 'NONE', ( #42147 ), #8379, .T. ) ;
#14318=CYLINDRICAL_SURFACE ( 'NONE', #1725, 31.99999999999999289 ) ;
#14320=EDGE_CURVE ( 'NONE', #15723, #44567, #47948, .T. ) ;
#14326=DIRECTION ( 'NONE',  ( 0.000000000000000000, 0.000000000000000000, 1.000000000000000000 ) ) ;
#14330=ORIENTED_EDGE ( 'NONE', *, *, #15794, .T. ) ;
#14334=ORIENTED_EDGE ( 'NONE', *, *, #30781, .F. ) ;
#14342=ORIENTED_EDGE ( 'NONE', *, *, #1776, .F. ) ;
#14344=DIRECTION ( 'NONE',  ( -1.000000000000000000, -0.000000000000000000, -0.000000000000000000 ) ) ;
#14348=DIRECTION ( 'NONE',  ( -1.000000000000000000, -0.000000000000000000, -0.000000000000000000 ) ) ;
#14351=CARTESIAN_POINT ( 'NONE',  ( 10.00000000000000000, 0.000000000000000000, 0.000000000000000000 ) ) ;
#14352=ORIENTED_EDGE ( 'NONE', *, *, #33644, .T. ) ;
#14356=DIRECTION ( 'NONE',  ( 0.000000000000000000, 0.000000000000000000, 1.000000000000000000 ) ) ;
#14363=EDGE_CURVE ( 'NONE', #39708, #29904, #16220, .T. ) ;
#14364=DIRECTION ( 'NONE',  ( -1.000000000000000000, 0.000000000000000000, -0.000000000000000000 ) ) ;
#14369=EDGE_CURVE ( 'NONE', #20061, #8653, #23066, .T. ) ;
#14370=EDGE_CURVE ( 'NONE', #32554, #42774, #301, .T. ) ;
#14383=DIRECTION ( 'NONE',  ( -1.000000000000000000, 0.000000000000000000, -0.000000000000000000 ) ) ;
#14384=CARTESIAN_POINT ( 'NONE',  ( -10.00000000000000000, 0.000000000000000000, 0.000000000000000000 ) ) ;
#14388=AXIS2_PLACEMENT_3D ( 'NONE', #37462, #11033, #45960 ) ;
#14389=CIRCLE ( 'NONE', #47977, 82.00000000000000000 ) ;
#14395=DIRECTION ( 'NONE',  ( -1.000000000000000000, 0.000000000000000000, 0.000000000000000000 ) ) ;
#14396=VECTOR ( 'NONE', #43376, 1000.000000000000000 ) ;
#14404=VERTEX_POINT ( 'NONE', #17152 ) ;
#14415=DIRECTION ( 'NONE',  ( 1.000000000000000000, -0.000000000000000000, -0.000000000000000000 ) ) ;
#14416=VERTEX_POINT ( 'NONE', #35769 ) ;
#14419=CARTESIAN_POINT ( 'NONE',  ( 5.000000000000002665, 79.10210256391398786, -21.60688246758503084 ) ) ;
#14422=CARTESIAN_POINT ( 'NONE',  ( 0.000000000000000000, -68.55367621811174672, 44.99326035066030727 ) ) ;
#14429=DIRECTION ( 'NONE',  ( 0.000000000000000000, -0.9969173337331287410, 0.07845909572783495156 ) ) ;
#14435=ORIENTED_EDGE ( 'NONE', *, *, #5634, .T. ) ;
#14437=CARTESIAN_POINT ( 'NONE',  ( 0.000000000000000000, -6.903761155837252694, -77.19088730480530103 ) ) ;
#14440=DIRECTION ( 'NONE',  ( 0.000000000000000000, -0.9723699203976789995, 0.2334453638558956212 ) ) ;
#14441=DIRECTION ( 'NONE',  ( 1.000000000000000000, 0.000000000000000000, 0.000000000000000000 ) ) ;
#14442=CARTESIAN_POINT ( 'NONE',  ( 10.00000000000000000, 0.000000000000000000, 0.000000000000000000 ) ) ;
#14444=LINE ( 'NONE', #36225, #37209 ) ;
#14450=DIRECTION ( 'NONE',  ( -1.000000000000000000, 0.000000000000000000, 0.000000000000000000 ) ) ;
#14452=ORIENTED_EDGE ( 'NONE', *, *, #12767, .T. ) ;
#14459=DIRECTION ( 'NONE',  ( -1.000000000000000000, 0.000000000000000000, -0.000000000000000000 ) ) ;
#14466=ORIENTED_EDGE ( 'NONE', *, *, #28280, .T. ) ;
#14469=AXIS2_PLACEMENT_3D ( 'NONE', #23234, #27900, #9267 ) ;
#14491=DIRECTION ( 'NONE',  ( 0.000000000000000000, -0.8910065241883722287, 0.4539904997395383113 ) ) ;
#14493=VERTEX_POINT ( 'NONE', #31394 ) ;
#14498=CYLINDRICAL_SURFACE ( 'NONE', #22197, 77.49899999999999523 ) ;
#14501=DIRECTION ( 'NONE',  ( 0.000000000000000000, 0.07845909572783790753, 0.9969173337331285190 ) ) ;
#14505=VECTOR ( 'NONE', #13702, 1000.000000000000000 ) ;
#14507=DIRECTION ( 'NONE',  ( -1.000000000000000000, 0.000000000000000000, -0.000000000000000000 ) ) ;
#14508=ORIENTED_EDGE ( 'NONE', *, *, #37693, .T. ) ;
#14509=FACE_OUTER_BOUND ( 'NONE', #39628, .T. ) ;
#14519=EDGE_CURVE ( 'NONE', #47251, #1792, #17386, .T. ) ;
#14520=ORIENTED_EDGE ( 'NONE', *, *, #13496, .F. ) ;
#14522=CARTESIAN_POINT ( 'NONE',  ( 0.000000000000000000, 62.50329211542435104, 41.76937507738811917 ) ) ;
#14527=EDGE_LOOP ( 'NONE', ( #6876, #6107, #23873, #21487 ) ) ;
#14541=ORIENTED_EDGE ( 'NONE', *, *, #18381, .T. ) ;
#14543=VECTOR ( 'NONE', #5754, 1000.000000000000000 ) ;
#14546=VECTOR ( 'NONE', #44424, 1000.000000000000000 ) ;
#14553=DIRECTION ( 'NONE',  ( -1.000000000000000000, 0.000000000000000000, -0.000000000000000000 ) ) ;
#14555=VERTEX_POINT ( 'NONE', #6632 ) ;
#14557=ORIENTED_EDGE ( 'NONE', *, *, #40876, .F. ) ;
#14559=CARTESIAN_POINT ( 'NONE',  ( 0.000000000000000000, -36.73666225445940370, 65.58780272294062286 ) ) ;
#14562=DIRECTION ( 'NONE',  ( 0.000000000000000000, 0.6494480483301849905, -0.7604059656000299317 ) ) ;
#14564=VERTEX_POINT ( 'NONE', #32574 ) ;
#14573=DIRECTION ( 'NONE',  ( -1.000000000000000000, 0.000000000000000000, 0.000000000000000000 ) ) ;
#14575=VECTOR ( 'NONE', #3222, 1000.000000000000000 ) ;
#14577=DIRECTION ( 'NONE',  ( -1.000000000000000000, -0.000000000000000000, 0.000000000000000000 ) ) ;
#14579=CYLINDRICAL_SURFACE ( 'NONE', #45115, 32.00000000000000000 ) ;
#14580=CYLINDRICAL_SURFACE ( 'NONE', #23772, 77.49899999999999523 ) ;
#14581=CIRCLE ( 'NONE', #39604, 77.49899999999999523 ) ;
#14582=ORIENTED_EDGE ( 'NONE', *, *, #4386, .T. ) ;
#14585=VECTOR ( 'NONE', #29154, 1000.000000000000000 ) ;
#14587=VERTEX_POINT ( 'NONE', #39926 ) ;
#14594=DIRECTION ( 'NONE',  ( -1.000000000000000000, -0.000000000000000000, 0.000000000000000000 ) ) ;
#14596=EDGE_CURVE ( 'NONE', #43657, #39094, #10787, .T. ) ;
#14598=CIRCLE ( 'NONE', #20848, 77.49899999999999523 ) ;
#14600=CYLINDRICAL_SURFACE ( 'NONE', #25755, 32.00000000000000000 ) ;
#14602=ORIENTED_EDGE ( 'NONE', *, *, #44353, .T. ) ;
#14603=AXIS2_PLACEMENT_3D ( 'NONE', #38460, #31373, #38719 ) ;
#14604=CARTESIAN_POINT ( 'NONE',  ( 0.000000000000000000, 28.89263327155850192, -71.91182617369156560 ) ) ;
#14607=ORIENTED_EDGE ( 'NONE', *, *, #37157, .F. ) ;
#14614=AXIS2_PLACEMENT_3D ( 'NONE', #17080, #39622, #6084 ) ;
#14615=ORIENTED_EDGE ( 'NONE', *, *, #15612, .T. ) ;
#14625=CARTESIAN_POINT ( 'NONE',  ( 10.00000000000000000, 46.21855187248629449, 62.20884554314036308 ) ) ;
#14626=EDGE_CURVE ( 'NONE', #6523, #39094, #46433, .T. ) ;
#14634=CARTESIAN_POINT ( 'NONE',  ( 0.000000000000000000, -65.64334221924939072, 41.19522573413710376 ) ) ;
#14635=DIRECTION ( 'NONE',  ( 1.000000000000000000, 0.000000000000000000, -0.000000000000000000 ) ) ;
#14646=AXIS2_PLACEMENT_3D ( 'NONE', #32844, #44119, #2993 ) ;
#14647=VERTEX_POINT ( 'NONE', #11022 ) ;
#14653=EDGE_CURVE ( 'NONE', #37233, #30791, #26902, .T. ) ;
#14656=ORIENTED_EDGE ( 'NONE', *, *, #44544, .T. ) ;
#14657=EDGE_CURVE ( 'NONE', #22595, #9308, #21302, .T. ) ;
#14665=DIRECTION ( 'NONE',  ( 0.000000000000000000, 0.000000000000000000, -1.000000000000000000 ) ) ;
#14670=EDGE_LOOP ( 'NONE', ( #25100, #29975, #25892, #43002 ) ) ;
#14685=FACE_OUTER_BOUND ( 'NONE', #7912, .T. ) ;
#14688=CARTESIAN_POINT ( 'NONE',  ( 10.00000000000000000, -76.66974797899844418, 11.30684508768314522 ) ) ;
#14691=CARTESIAN_POINT ( 'NONE',  ( 0.000000000000000000, -33.71516098798792171, 74.74816331893418919 ) ) ;
#14692=CARTESIAN_POINT ( 'NONE',  ( 10.00000000000000000, 49.70050353004889132, 59.46389618801982380 ) ) ;
#14693=DIRECTION ( 'NONE',  ( 0.000000000000000000, -0.9876883405951359940, -0.1564344650402420822 ) ) ;
#14694=ORIENTED_EDGE ( 'NONE', *, *, #43702, .F. ) ;
#14695=EDGE_LOOP ( 'NONE', ( #18555, #2090, #37933, #44013 ) ) ;
#14696=AXIS2_PLACEMENT_3D ( 'NONE', #22670, #36870, #3835 ) ;
#14697=EDGE_CURVE ( 'NONE', #17725, #14023, #47980, .T. ) ;
#14701=DIRECTION ( 'NONE',  ( -1.000000000000000000, -0.000000000000000000, -0.000000000000000000 ) ) ;
#14702=AXIS2_PLACEMENT_3D ( 'NONE', #44684, #45181, #26575 ) ;
#14704=EDGE_CURVE ( 'NONE', #10878, #42173, #13581, .T. ) ;
#14707=CARTESIAN_POINT ( 'NONE',  ( 10.00000000000000000, 34.44570377933598593, 69.42325613327452061 ) ) ;
#14709=DIRECTION ( 'NONE',  ( -1.000000000000000000, -0.000000000000000000, -0.000000000000000000 ) ) ;
#14714=FACE_OUTER_BOUND ( 'NONE', #30592, .T. ) ;
#14720=DIRECTION ( 'NONE',  ( -1.000000000000000000, -0.000000000000000000, 0.000000000000000000 ) ) ;
#14722=DIRECTION ( 'NONE',  ( 0.000000000000000000, 1.000000000000000000, 0.000000000000000000 ) ) ;
#14725=CARTESIAN_POINT ( 'NONE',  ( 10.00000000000000000, 6.903761155837774943, 77.19088730480525840 ) ) ;
#14726=CARTESIAN_POINT ( 'NONE',  ( 0.000000000000000000, -63.18004540532994184, -44.88180994100446952 ) ) ;
#14728=DIRECTION ( 'NONE',  ( 0.000000000000000000, 0.000000000000000000, -1.000000000000000000 ) ) ;
#14739=CYLINDRICAL_SURFACE ( 'NONE', #41469, 31.99999999999998579 ) ;
#14740=LINE ( 'NONE', #3715, #298 ) ;
#14755=DIRECTION ( 'NONE',  ( -1.000000000000000000, 0.000000000000000000, 0.000000000000000000 ) ) ;
#14756=ORIENTED_EDGE ( 'NONE', *, *, #13261, .T. ) ;
#14757=CIRCLE ( 'NONE', #26453, 82.00000000000000000 ) ;
#14759=ORIENTED_EDGE ( 'NONE', *, *, #45088, .F. ) ;
#14767=ORIENTED_EDGE ( 'NONE', *, *, #5145, .F. ) ;
#14768=CIRCLE ( 'NONE', #15634, 77.49900000000000944 ) ;
#14771=AXIS2_PLACEMENT_3D ( 'NONE', #24207, #12713, #4881 ) ;
#14781=DIRECTION ( 'NONE',  ( -1.000000000000000000, 0.000000000000000000, -0.000000000000000000 ) ) ;
#14789=ORIENTED_EDGE ( 'NONE', *, *, #35644, .F. ) ;
#14796=DIRECTION ( 'NONE',  ( 0.000000000000000000, 0.000000000000000000, 1.000000000000000000 ) ) ;
#14803=CYLINDRICAL_SURFACE ( 'NONE', #1155, 31.99999999999999289 ) ;
#14812=DIRECTION ( 'NONE',  ( -1.000000000000000000, 0.000000000000000000, 0.000000000000000000 ) ) ;
#14819=EDGE_CURVE ( 'NONE', #14564, #33636, #40950, .T. ) ;
#14822=EDGE_CURVE ( 'NONE', #28052, #30791, #26082, .T. ) ;
#14825=EDGE_CURVE ( 'NONE', #43468, #2823, #300, .T. ) ;
#14827=ORIENTED_EDGE ( 'NONE', *, *, #10784, .T. ) ;
#14829=CARTESIAN_POINT ( 'NONE',  ( 0.000000000000000000, 0.000000000000000000, 0.000000000000000000 ) ) ;
#14831=AXIS2_PLACEMENT_3D ( 'NONE', #4308, #45175, #11638 ) ;
#14836=ORIENTED_EDGE ( 'NONE', *, *, #47902, .F. ) ;
#14839=ORIENTED_EDGE ( 'NONE', *, *, #1036, .F. ) ;
#14841=CYLINDRICAL_SURFACE ( 'NONE', #28813, 32.00000000000000000 ) ;
#14842=LINE ( 'NONE', #27070, #6378 ) ;
#14846=VECTOR ( 'NONE', #5693, 1000.000000000000000 ) ;
#14854=CARTESIAN_POINT ( 'NONE',  ( 10.00000000000000000, 41.76106447765489094, 62.50884508063442269 ) ) ;
#14856=DIRECTION ( 'NONE',  ( 0.000000000000000000, 0.000000000000000000, 1.000000000000000000 ) ) ;
#14869=DIRECTION ( 'NONE',  ( 0.000000000000000000, 0.8090169943749487835, -0.5877852522924712497 ) ) ;
#14870=AXIS2_PLACEMENT_3D ( 'NONE', #11642, #7954, #22890 ) ;
#14872=DIRECTION ( 'NONE',  ( 0.000000000000000000, 0.4539904997395413644, 0.8910065241883706744 ) ) ;
#14876=DIRECTION ( 'NONE',  ( -1.000000000000000000, -0.000000000000000000, -0.000000000000000000 ) ) ;
#14883=ORIENTED_EDGE ( 'NONE', *, *, #48335, .F. ) ;
#14884=CARTESIAN_POINT ( 'NONE',  ( 10.00000000000000000, 76.66974797899837313, 11.30684508768368524 ) ) ;
#14885=CARTESIAN_POINT ( 'NONE',  ( 10.00000000000000000, -72.35160999960801576, -20.41045688087902121 ) ) ;
#14894=VERTEX_POINT ( 'NONE', #1700 ) ;
#14897=CYLINDRICAL_SURFACE ( 'NONE', #33761, 77.49899999999999523 ) ;
#14905=AXIS2_PLACEMENT_3D ( 'NONE', #36748, #21095, #10325 ) ;
#14906=DIRECTION ( 'NONE',  ( 0.000000000000000000, 0.000000000000000000, 1.000000000000000000 ) ) ;
#14910=CIRCLE ( 'NONE', #10225, 31.99999999999999289 ) ;
#14912=CARTESIAN_POINT ( 'NONE',  ( -10.00000000000000000, 0.000000000000000000, 0.000000000000000000 ) ) ;
#14922=DIRECTION ( 'NONE',  ( 0.000000000000000000, 0.7071067811865439090, 0.7071067811865512365 ) ) ;
#14923=DIRECTION ( 'NONE',  ( 1.000000000000000000, 0.000000000000000000, -0.000000000000000000 ) ) ;
#14927=CARTESIAN_POINT ( 'NONE',  ( -10.00000000000000000, 0.000000000000000000, 0.000000000000000000 ) ) ;
#14930=ADVANCED_FACE ( 'NONE', ( #23981 ), #35463, .T. ) ;
#14933=VECTOR ( 'NONE', #25834, 1000.000000000000000 ) ;
#14934=ADVANCED_FACE ( 'NONE', ( #39869 ), #21503, .T. ) ;
#14946=CARTESIAN_POINT ( 'NONE',  ( 0.000000000000000000, 0.000000000000000000, 0.000000000000000000 ) ) ;
#14948=ORIENTED_EDGE ( 'NONE', *, *, #5365, .T. ) ;
#14952=FACE_OUTER_BOUND ( 'NONE', #11299, .T. ) ;
#14953=DIRECTION ( 'NONE',  ( 0.000000000000000000, 0.000000000000000000, 1.000000000000000000 ) ) ;
#14956=CARTESIAN_POINT ( 'NONE',  ( 10.00000000000000000, 0.000000000000000000, 0.000000000000000000 ) ) ;
#14960=ORIENTED_EDGE ( 'NONE', *, *, #48094, .T. ) ;
#14972=ORIENTED_EDGE ( 'NONE', *, *, #16809, .F. ) ;
#14977=CIRCLE ( 'NONE', #33718, 32.00000000000000000 ) ;
#14981=DIRECTION ( 'NONE',  ( -1.000000000000000000, -0.000000000000000000, -0.000000000000000000 ) ) ;
#14989=DIRECTION ( 'NONE',  ( 0.000000000000000000, -0.8526401643540971742, 0.5224985647159409163 ) ) ;
#15000=ADVANCED_FACE ( 'NONE', ( #44012 ), #10968, .T. ) ;
#15008=CIRCLE ( 'NONE', #16541, 77.49899999999999523 ) ;
#15009=EDGE_CURVE ( 'NONE', #45983, #28806, #2401, .T. ) ;
#15011=CIRCLE ( 'NONE', #23594, 82.00000000000000000 ) ;
#15014=AXIS2_PLACEMENT_3D ( 'NONE', #7456, #22388, #34339 ) ;
#15020=AXIS2_PLACEMENT_3D ( 'NONE', #35959, #48186, #14665 ) ;
#15024=DIRECTION ( 'NONE',  ( -1.000000000000000000, 0.000000000000000000, -0.000000000000000000 ) ) ;
#15028=CYLINDRICAL_SURFACE ( 'NONE', #47455, 31.99999999999999289 ) ;
#15030=VERTEX_POINT ( 'NONE', #28614 ) ;
#15036=ORIENTED_EDGE ( 'NONE', *, *, #44474, .T. ) ;
#15037=CARTESIAN_POINT ( 'NONE',  ( 10.00000000000000000, 23.16143007188532366, -73.95703589263949596 ) ) ;
#15040=DIRECTION ( 'NONE',  ( 1.000000000000000000, 0.000000000000000000, 0.000000000000000000 ) ) ;
#15046=EDGE_CURVE ( 'NONE', #46234, #16188, #32990, .T. ) ;
#15048=CIRCLE ( 'NONE', #30654, 82.00000000000000000 ) ;
#15049=CARTESIAN_POINT ( 'NONE',  ( 0.000000000000000000, 3.894527615417891830, 81.90746397400390322 ) ) ;
#15052=CARTESIAN_POINT ( 'NONE',  ( 10.00000000000000000, -49.70050353004933896, 59.46389618801946852 ) ) ;
#15054=CARTESIAN_POINT ( 'NONE',  ( 10.00000000000000000, -21.60688246758529019, -79.10210256391388839 ) ) ;
#15062=LINE ( 'NONE', #44926, #44525 ) ;
#15063=CIRCLE ( 'NONE', #29914, 31.99999999999998579 ) ;
#15065=AXIS2_PLACEMENT_3D ( 'NONE', #19657, #35087, #39011 ) ;
#15069=LINE ( 'NONE', #15792, #6241 ) ;
#15071=CARTESIAN_POINT ( 'NONE',  ( 0.000000000000000000, 0.000000000000000000, 0.000000000000000000 ) ) ;
#15079=CARTESIAN_POINT ( 'NONE',  ( 0.000000000000000000, 0.000000000000000000, 0.000000000000000000 ) ) ;
#15094=EDGE_CURVE ( 'NONE', #25837, #17873, #41318, .T. ) ;
#15097=DIRECTION ( 'NONE',  ( 0.000000000000000000, 0.000000000000000000, 1.000000000000000000 ) ) ;
#15099=VERTEX_POINT ( 'NONE', #44732 ) ;
#15102=DIRECTION ( 'NONE',  ( 0.000000000000000000, 0.000000000000000000, 1.000000000000000000 ) ) ;
#15107=DIRECTION ( 'NONE',  ( -1.000000000000000000, -0.000000000000000000, -0.000000000000000000 ) ) ;
#15108=AXIS2_PLACEMENT_3D ( 'NONE', #23785, #8600, #45837 ) ;
#15112=VECTOR ( 'NONE', #7406, 1000.000000000000000 ) ;
#15117=VECTOR ( 'NONE', #29641, 1000.000000000000000 ) ;
#15124=ORIENTED_EDGE ( 'NONE', *, *, #33262, .T. ) ;
#15128=VERTEX_POINT ( 'NONE', #16509 ) ;
#15134=CYLINDRICAL_SURFACE ( 'NONE', #4627, 32.00000000000000000 ) ;
#15139=VECTOR ( 'NONE', #31820, 1000.000000000000000 ) ;
#15142=ORIENTED_EDGE ( 'NONE', *, *, #1332, .T. ) ;
#15143=FACE_OUTER_BOUND ( 'NONE', #18923, .T. ) ;
#15145=DIRECTION ( 'NONE',  ( 0.000000000000000000, 0.9969173337331276308, 0.07845909572784873220 ) ) ;
#15148=DIRECTION ( 'NONE',  ( -1.000000000000000000, -0.000000000000000000, 0.000000000000000000 ) ) ;
#15149=AXIS2_PLACEMENT_3D ( 'NONE', #9330, #31878, #47020 ) ;
#15158=LINE ( 'NONE', #21993, #13374 ) ;
#15159=AXIS2_PLACEMENT_3D ( 'NONE', #33053, #36958, #3433 ) ;
#15168=DIRECTION ( 'NONE',  ( 0.000000000000000000, 0.9238795325112851842, 0.3826834323650938341 ) ) ;
#15173=CIRCLE ( 'NONE', #34672, 77.49899999999999523 ) ;
#15184=CARTESIAN_POINT ( 'NONE',  ( 0.000000000000000000, 0.000000000000000000, 0.000000000000000000 ) ) ;
#15193=CIRCLE ( 'NONE', #40172, 31.99999999999998579 ) ;
#15196=VERTEX_POINT ( 'NONE', #37882 ) ;
#15203=VECTOR ( 'NONE', #16383, 1000.000000000000000 ) ;
#15215=CARTESIAN_POINT ( 'NONE',  ( 0.000000000000000000, 0.000000000000000000, 0.000000000000000000 ) ) ;
#15216=EDGE_CURVE ( 'NONE', #33075, #40440, #27713, .T. ) ;
#15217=ORIENTED_EDGE ( 'NONE', *, *, #33526, .F. ) ;
#15219=EDGE_LOOP ( 'NONE', ( #34605, #25723, #9451, #33899, #9635, #20141 ) ) ;
#15223=FACE_OUTER_BOUND ( 'NONE', #1174, .T. ) ;
#15227=CARTESIAN_POINT ( 'NONE',  ( 10.00000000000000000, -75.11725578898470701, 2.956366410620372864 ) ) ;
#15228=AXIS2_PLACEMENT_3D ( 'NONE', #32159, #12834, #47077 ) ;
#15230=DIRECTION ( 'NONE',  ( -1.000000000000000000, 0.000000000000000000, -0.000000000000000000 ) ) ;
#15234=ADVANCED_FACE ( 'NONE', ( #7771 ), #48403, .T. ) ;
#15237=CARTESIAN_POINT ( 'NONE',  ( 0.000000000000000000, -28.89263327155796901, 71.91182617369176455 ) ) ;
#15243=CIRCLE ( 'NONE', #44153, 77.49900000000000944 ) ;
#15244=LINE ( 'NONE', #41191, #23658 ) ;
#15249=VERTEX_POINT ( 'NONE', #27781 ) ;
#15257=CIRCLE ( 'NONE', #20694, 31.99999999999999289 ) ;
#15258=AXIS2_PLACEMENT_3D ( 'NONE', #5701, #24546, #39234 ) ;
#15260=EDGE_CURVE ( 'NONE', #38600, #14299, #19893, .T. ) ;
#15270=ORIENTED_EDGE ( 'NONE', *, *, #7017, .T. ) ;
#15275=CYLINDRICAL_SURFACE ( 'NONE', #29610, 77.49899999999999523 ) ;
#15276=EDGE_CURVE ( 'NONE', #39764, #14287, #12900, .T. ) ;
#15280=LINE ( 'NONE', #30210, #46714 ) ;
#15287=CARTESIAN_POINT ( 'NONE',  ( 10.00000000000000000, 0.000000000000000000, 0.000000000000000000 ) ) ;
#15288=CARTESIAN_POINT ( 'NONE',  ( 10.00000000000000000, 0.000000000000000000, 0.000000000000000000 ) ) ;
#15299=CARTESIAN_POINT ( 'NONE',  ( 5.000000000000000000, 33.71516098798740302, 74.74816331893443078 ) ) ;
#15301=CYLINDRICAL_SURFACE ( 'NONE', #47192, 77.49899999999999523 ) ;
#15305=CARTESIAN_POINT ( 'NONE',  ( 10.00000000000000000, 55.19960302592141232, -51.03279382321027668 ) ) ;
#15306=CARTESIAN_POINT ( 'NONE',  ( 10.00000000000000000, -34.94270380257586339, -74.18225833017926618 ) ) ;
#15307=DIRECTION ( 'NONE',  ( 0.000000000000000000, 0.000000000000000000, 1.000000000000000000 ) ) ;
#15314=ORIENTED_EDGE ( 'NONE', *, *, #24919, .T. ) ;
#15317=ORIENTED_EDGE ( 'NONE', *, *, #37290, .F. ) ;
#15321=ADVANCED_FACE ( 'NONE', ( #24329 ), #36066, .T. ) ;
#15340=DIRECTION ( 'NONE',  ( 0.000000000000000000, 0.000000000000000000, 1.000000000000000000 ) ) ;
#15343=VECTOR ( 'NONE', #9864, 1000.000000000000000 ) ;
#15350=CARTESIAN_POINT ( 'NONE',  ( 10.00000000000000000, 73.44644590900061587, 24.73286445877730699 ) ) ;
#15351=CARTESIAN_POINT ( 'NONE',  ( 5.000000000000002665, 39.47590169984944453, -71.87247863392373404 ) ) ;
#15354=DIRECTION ( 'NONE',  ( 0.000000000000000000, -0.8090169943749531134, 0.5877852522924653655 ) ) ;
#15355=EDGE_CURVE ( 'NONE', #18078, #8218, #13083, .T. ) ;
#15358=CARTESIAN_POINT ( 'NONE',  ( 10.00000000000000000, -59.03342792756297541, 46.54456581323783126 ) ) ;
#15361=DIRECTION ( 'NONE',  ( -1.000000000000000000, -0.000000000000000000, 0.000000000000000000 ) ) ;
#15367=AXIS2_PLACEMENT_3D ( 'NONE', #36699, #18093, #43580 ) ;
#15374=AXIS2_PLACEMENT_3D ( 'NONE', #24888, #39606, #2365 ) ;
#15379=EDGE_CURVE ( 'NONE', #21856, #38600, #25265, .T. ) ;
#15384=LINE ( 'NONE', #8010, #41361 ) ;
#15385=ORIENTED_EDGE ( 'NONE', *, *, #6209, .F. ) ;
#15391=VECTOR ( 'NONE', #42815, 1000.000000000000000 ) ;
#15394=CARTESIAN_POINT ( 'NONE',  ( 10.00000000000000000, 72.35432306680455383, 20.40083707023012494 ) ) ;
#15399=ORIENTED_EDGE ( 'NONE', *, *, #48335, .T. ) ;
#15400=EDGE_LOOP ( 'NONE', ( #6987, #21239, #14245, #18727 ) ) ;
#15408=DIRECTION ( 'NONE',  ( 0.000000000000000000, 0.000000000000000000, -1.000000000000000000 ) ) ;
#15414=CARTESIAN_POINT ( 'NONE',  ( 0.000000000000000000, -20.41045688087772092, -72.35160999960838524 ) ) ;
#15416=CARTESIAN_POINT ( 'NONE',  ( 0.000000000000000000, 0.000000000000000000, 0.000000000000000000 ) ) ;
#15427=CARTESIAN_POINT ( 'NONE',  ( 0.000000000000000000, -78.73519480814938731, -22.90783923731713756 ) ) ;
#15432=EDGE_CURVE ( 'NONE', #32581, #6408, #42472, .T. ) ;
#15433=CIRCLE ( 'NONE', #30290, 31.99999999999999289 ) ;
#15434=EDGE_CURVE ( 'NONE', #6719, #37275, #23822, .T. ) ;
#15443=VERTEX_POINT ( 'NONE', #44383 ) ;
#15444=ORIENTED_EDGE ( 'NONE', *, *, #8079, .F. ) ;
#15445=CYLINDRICAL_SURFACE ( 'NONE', #45446, 77.49899999999999523 ) ;
#15450=CARTESIAN_POINT ( 'NONE',  ( 0.000000000000000000, 0.000000000000000000, 0.000000000000000000 ) ) ;
#15451=ORIENTED_EDGE ( 'NONE', *, *, #15756, .T. ) ;
#15452=AXIS2_PLACEMENT_3D ( 'NONE', #15895, #41852, #8310 ) ;
#15455=VERTEX_POINT ( 'NONE', #3011 ) ;
#15457=ORIENTED_EDGE ( 'NONE', *, *, #16486, .T. ) ;
#15461=VERTEX_POINT ( 'NONE', #25527 ) ;
#15462=LINE ( 'NONE', #15942, #22305 ) ;
#15466=CYLINDRICAL_SURFACE ( 'NONE', #26674, 77.49899999999999523 ) ;
#15472=FACE_OUTER_BOUND ( 'NONE', #2348, .T. ) ;
#15481=DIRECTION ( 'NONE',  ( 0.000000000000000000, 0.3090169943749482839, -0.9510565162951533091 ) ) ;
#15482=ORIENTED_EDGE ( 'NONE', *, *, #19613, .F. ) ;
#15484=STYLED_ITEM ( 'NONE', ( #30297 ), #31571 ) ;
#15485=CARTESIAN_POINT ( 'NONE',  ( 0.000000000000000000, 55.16347631943131802, -60.67117009219075641 ) ) ;
#15487=EDGE_CURVE ( 'NONE', #3669, #39957, #33974, .T. ) ;
#15489=AXIS2_PLACEMENT_3D ( 'NONE', #22186, #47638, #3089 ) ;
#15490=ORIENTED_EDGE ( 'NONE', *, *, #8723, .F. ) ;
#15497=DIRECTION ( 'NONE',  ( 0.000000000000000000, 0.000000000000000000, 1.000000000000000000 ) ) ;
#15499=ORIENTED_EDGE ( 'NONE', *, *, #10643, .F. ) ;
#15508=LINE ( 'NONE', #41949, #20887 ) ;
#15509=VERTEX_POINT ( 'NONE', #15725 ) ;
#15510=VERTEX_POINT ( 'NONE', #4241 ) ;
#15519=AXIS2_PLACEMENT_3D ( 'NONE', #2999, #18156, #18653 ) ;
#15533=DIRECTION ( 'NONE',  ( 0.000000000000000000, -6.982962677686266711E-15, 1.000000000000000000 ) ) ;
#15536=CIRCLE ( 'NONE', #26480, 82.00000000000000000 ) ;
#15538=ORIENTED_EDGE ( 'NONE', *, *, #29933, .F. ) ;
#15540=EDGE_CURVE ( 'NONE', #42650, #23818, #4949, .T. ) ;
#15543=ORIENTED_EDGE ( 'NONE', *, *, #25453, .T. ) ;
#15546=ADVANCED_FACE ( 'NONE', ( #30918 ), #1290, .T. ) ;
#15555=CYLINDRICAL_SURFACE ( 'NONE', #14702, 82.00000000000000000 ) ;
#15557=ORIENTED_EDGE ( 'NONE', *, *, #19931, .F. ) ;
#15560=AXIS2_PLACEMENT_3D ( 'NONE', #37159, #29335, #47672 ) ;
#15561=CYLINDRICAL_SURFACE ( 'NONE', #31813, 82.00000000000000000 ) ;
#15567=CARTESIAN_POINT ( 'NONE',  ( 10.00000000000000000, -65.58780272294048075, -36.73666225445966660 ) ) ;
#15575=CARTESIAN_POINT ( 'NONE',  ( 0.000000000000000000, 58.39081064771751528, 50.95692526931350841 ) ) ;
#15579=CARTESIAN_POINT ( 'NONE',  ( 0.000000000000000000, -74.65491531819111515, 23.16904090965678975 ) ) ;
#15582=DIRECTION ( 'NONE',  ( 0.000000000000000000, 0.000000000000000000, 1.000000000000000000 ) ) ;
#15594=CARTESIAN_POINT ( 'NONE',  ( 10.00000000000000000, 30.41916302227216562, -71.27951684757994144 ) ) ;
#15599=EDGE_CURVE ( 'NONE', #10420, #29421, #22830, .T. ) ;
#15604=EDGE_LOOP ( 'NONE', ( #5227, #14839, #30598, #969 ) ) ;
#15606=CARTESIAN_POINT ( 'NONE',  ( 10.00000000000000000, 0.000000000000000000, 0.000000000000000000 ) ) ;
#15608=ORIENTED_EDGE ( 'NONE', *, *, #3924, .F. ) ;
#15610=DIRECTION ( 'NONE',  ( -1.000000000000000000, 0.000000000000000000, 0.000000000000000000 ) ) ;
#15611=ORIENTED_EDGE ( 'NONE', *, *, #44008, .T. ) ;
#15612=EDGE_CURVE ( 'NONE', #11145, #690, #28188, .T. ) ;
#15617=ORIENTED_EDGE ( 'NONE', *, *, #1187, .T. ) ;
#15618=VERTEX_POINT ( 'NONE', #46311 ) ;
#15619=DIRECTION ( 'NONE',  ( -1.000000000000000000, -0.000000000000000000, -0.000000000000000000 ) ) ;
#15622=ORIENTED_EDGE ( 'NONE', *, *, #41506, .T. ) ;
#15626=CIRCLE ( 'NONE', #3106, 31.99999999999999289 ) ;
#15630=EDGE_CURVE ( 'NONE', #25422, #36021, #23734, .T. ) ;
#15634=AXIS2_PLACEMENT_3D ( 'NONE', #13972, #28896, #43832 ) ;
#15643=DIRECTION ( 'NONE',  ( 1.000000000000000000, 0.000000000000000000, -0.000000000000000000 ) ) ;
#15648=ORIENTED_EDGE ( 'NONE', *, *, #33535, .T. ) ;
#15650=FACE_OUTER_BOUND ( 'NONE', #14527, .T. ) ;
#15662=CIRCLE ( 'NONE', #43036, 32.00000000000000000 ) ;
#15670=AXIS2_PLACEMENT_3D ( 'NONE', #28148, #43083, #47235 ) ;
#15681=CARTESIAN_POINT ( 'NONE',  ( 10.00000000000000000, 51.03279382321166224, -55.19960302592011914 ) ) ;
#15682=EDGE_CURVE ( 'NONE', #22252, #270, #8081, .T. ) ;
#15685=CARTESIAN_POINT ( 'NONE',  ( 10.00000000000000000, 3.894527615419054456, -81.90746397400386059 ) ) ;
#15696=DIRECTION ( 'NONE',  ( 0.000000000000000000, 0.000000000000000000, 1.000000000000000000 ) ) ;
#15702=DIRECTION ( 'NONE',  ( 1.000000000000000000, -0.000000000000000000, 0.000000000000000000 ) ) ;
#15703=DIRECTION ( 'NONE',  ( 0.000000000000000000, 0.000000000000000000, 1.000000000000000000 ) ) ;
#15712=CARTESIAN_POINT ( 'NONE',  ( 10.00000000000000000, -72.35432306680498016, 20.40083707022857951 ) ) ;
#15723=VERTEX_POINT ( 'NONE', #20121 ) ;
#15725=CARTESIAN_POINT ( 'NONE',  ( 10.00000000000000000, -39.47590169984793818, -71.87247863392455827 ) ) ;
#15726=ORIENTED_EDGE ( 'NONE', *, *, #2477, .F. ) ;
#15733=AXIS2_PLACEMENT_3D ( 'NONE', #16649, #1244, #31600 ) ;
#15736=ORIENTED_EDGE ( 'NONE', *, *, #45775, .T. ) ;
#15739=LINE ( 'NONE', #39223, #7391 ) ;
#15742=DIRECTION ( 'NONE',  ( -1.000000000000000000, 0.000000000000000000, 0.000000000000000000 ) ) ;
#15743=DIRECTION ( 'NONE',  ( 0.000000000000000000, 0.000000000000000000, -1.000000000000000000 ) ) ;
#15749=ORIENTED_EDGE ( 'NONE', *, *, #46757, .F. ) ;
#15750=AXIS2_PLACEMENT_3D ( 'NONE', #23497, #7845, #41388 ) ;
#15751=LINE ( 'NONE', #4733, #7424 ) ;
#15752=DIRECTION ( 'NONE',  ( 0.000000000000000000, 0.000000000000000000, -1.000000000000000000 ) ) ;
#15753=FACE_OUTER_BOUND ( 'NONE', #5032, .T. ) ;
#15756=EDGE_CURVE ( 'NONE', #42173, #33476, #5756, .T. ) ;
#15759=EDGE_CURVE ( 'NONE', #9826, #5621, #36244, .T. ) ;
#15766=CARTESIAN_POINT ( 'NONE',  ( 10.00000000000000000, 0.000000000000000000, 0.000000000000000000 ) ) ;
#15767=DIRECTION ( 'NONE',  ( 0.000000000000000000, -6.938893903907229955E-15, 1.000000000000000000 ) ) ;
#15772=AXIS2_PLACEMENT_3D ( 'NONE', #14138, #21720, #36643 ) ;
#15775=CYLINDRICAL_SURFACE ( 'NONE', #5054, 77.49899999999999523 ) ;
#15776=VECTOR ( 'NONE', #4009, 1000.000000000000000 ) ;
#15780=VECTOR ( 'NONE', #38279, 1000.000000000000000 ) ;
#15791=CARTESIAN_POINT ( 'NONE',  ( 0.000000000000000000, -34.44570377933648331, 69.42325613327426481 ) ) ;
#15792=CARTESIAN_POINT ( 'NONE',  ( 5.000000000000000000, -63.97538442413390669, -51.29473840253292849 ) ) ;
#15794=EDGE_CURVE ( 'NONE', #18404, #22636, #25699, .T. ) ;
#15799=VERTEX_POINT ( 'NONE', #11029 ) ;
#15806=ORIENTED_EDGE ( 'NONE', *, *, #35590, .F. ) ;
#15810=CARTESIAN_POINT ( 'NONE',  ( 10.00000000000000000, 0.000000000000000000, 0.000000000000000000 ) ) ;
#15817=EDGE_CURVE ( 'NONE', #21525, #14416, #13973, .T. ) ;
#15819=DIRECTION ( 'NONE',  ( -1.000000000000000000, -0.000000000000000000, -0.000000000000000000 ) ) ;
#15820=DIRECTION ( 'NONE',  ( 1.000000000000000000, 0.000000000000000000, 0.000000000000000000 ) ) ;
#15823=ORIENTED_EDGE ( 'NONE', *, *, #18070, .F. ) ;
#15824=CARTESIAN_POINT ( 'NONE',  ( 10.00000000000000000, 0.000000000000000000, 0.000000000000000000 ) ) ;
#15832=EDGE_CURVE ( 'NONE', #23222, #3743, #16733, .T. ) ;
#15849=CARTESIAN_POINT ( 'NONE',  ( 10.00000000000000000, 8.966570791700695153, 81.50828551894228724 ) ) ;
#15854=VERTEX_POINT ( 'NONE', #40420 ) ;
#15856=CARTESIAN_POINT ( 'NONE',  ( 0.000000000000000000, -75.11764819372145041, 29.05362095685286761 ) ) ;
#15863=VERTEX_POINT ( 'NONE', #28828 ) ;
#15869=AXIS2_PLACEMENT_3D ( 'NONE', #28485, #25040, #47786 ) ;
#15874=DIRECTION ( 'NONE',  ( 0.000000000000000000, 0.000000000000000000, 1.000000000000000000 ) ) ;
#15875=DIRECTION ( 'NONE',  ( 0.000000000000000000, 0.000000000000000000, 1.000000000000000000 ) ) ;
#15884=DIRECTION ( 'NONE',  ( 0.000000000000000000, 0.000000000000000000, 1.000000000000000000 ) ) ;
#15889=EDGE_CURVE ( 'NONE', #17705, #7024, #16692, .T. ) ;
#15890=CIRCLE ( 'NONE', #22134, 31.99999999999998934 ) ;
#15891=CARTESIAN_POINT ( 'NONE',  ( 10.00000000000000000, 49.70050353004889132, 59.46389618801982380 ) ) ;
#15895=CARTESIAN_POINT ( 'NONE',  ( 0.000000000000000000, 0.000000000000000000, 0.000000000000000000 ) ) ;
#15908=VECTOR ( 'NONE', #35907, 1000.000000000000000 ) ;
#15909=CIRCLE ( 'NONE', #47930, 77.49899999999999523 ) ;
#15919=VERTEX_POINT ( 'NONE', #24917 ) ;
#15920=AXIS2_PLACEMENT_3D ( 'NONE', #23842, #34350, #11619 ) ;
#15926=VECTOR ( 'NONE', #2707, 1000.000000000000000 ) ;
#15927=EDGE_LOOP ( 'NONE', ( #5098, #16337, #25878, #1646 ) ) ;
#15928=CARTESIAN_POINT ( 'NONE',  ( 10.00000000000000000, 0.000000000000000000, 0.000000000000000000 ) ) ;
#15929=DIRECTION ( 'NONE',  ( 0.000000000000000000, 0.000000000000000000, 1.000000000000000000 ) ) ;
#15930=CIRCLE ( 'NONE', #34637, 77.49899999999998101 ) ;
#15935=FACE_OUTER_BOUND ( 'NONE', #48315, .T. ) ;
#15936=VERTEX_POINT ( 'NONE', #47437 ) ;
#15939=ORIENTED_EDGE ( 'NONE', *, *, #32982, .F. ) ;
#15940=CARTESIAN_POINT ( 'NONE',  ( 0.000000000000000000, 16.00000000000000000, -2.500000000000000000 ) ) ;
#15942=CARTESIAN_POINT ( 'NONE',  ( 10.00000000000000000, -62.20884554314051940, 46.21855187248608132 ) ) ;
#15947=CARTESIAN_POINT ( 'NONE',  ( 0.000000000000000000, -58.39081064771713869, -50.95692526931392052 ) ) ;
#15958=DIRECTION ( 'NONE',  ( -1.000000000000000000, -0.000000000000000000, 0.000000000000000000 ) ) ;
#15967=VECTOR ( 'NONE', #46228, 1000.000000000000000 ) ;
#15979=EDGE_CURVE ( 'NONE', #26518, #34988, #46484, .T. ) ;
#15982=CARTESIAN_POINT ( 'NONE',  ( 0.000000000000000000, 0.000000000000000000, 0.000000000000000000 ) ) ;
#15984=ORIENTED_EDGE ( 'NONE', *, *, #8499, .T. ) ;
#15992=AXIS2_PLACEMENT_3D ( 'NONE', #4779, #30727, #7952 ) ;
#15994=VERTEX_POINT ( 'NONE', #24436 ) ;
#16001=DIRECTION ( 'NONE',  ( -1.000000000000000000, 0.000000000000000000, 0.000000000000000000 ) ) ;
#16004=ORIENTED_EDGE ( 'NONE', *, *, #27039, .T. ) ;
#16008=EDGE_CURVE ( 'NONE', #3237, #45718, #36418, .T. ) ;
#16012=DIRECTION ( 'NONE',  ( -1.000000000000000000, 0.000000000000000000, 0.000000000000000000 ) ) ;
#16013=FACE_OUTER_BOUND ( 'NONE', #39038, .T. ) ;
#16019=AXIS2_PLACEMENT_3D ( 'NONE', #41116, #29835, #15168 ) ;
#16021=CARTESIAN_POINT ( 'NONE',  ( 10.00000000000000000, 41.76106447765489094, 62.50884508063442269 ) ) ;
#16024=ORIENTED_EDGE ( 'NONE', *, *, #45581, .F. ) ;
#16029=VERTEX_POINT ( 'NONE', #48158 ) ;
#16031=AXIS2_PLACEMENT_3D ( 'NONE', #3292, #11141, #14326 ) ;
#16033=ORIENTED_EDGE ( 'NONE', *, *, #39121, .T. ) ;
#16042=CARTESIAN_POINT ( 'NONE',  ( 10.00000000000000000, 26.02418014898310261, 70.52718814184268581 ) ) ;
#16043=ORIENTED_EDGE ( 'NONE', *, *, #2208, .T. ) ;
#16050=FACE_OUTER_BOUND ( 'NONE', #13223, .T. ) ;
#16051=CARTESIAN_POINT ( 'NONE',  ( 10.00000000000000000, 0.000000000000000000, 0.000000000000000000 ) ) ;
#16055=ORIENTED_EDGE ( 'NONE', *, *, #18477, .F. ) ;
#16056=DIRECTION ( 'NONE',  ( -1.000000000000000000, -0.000000000000000000, -0.000000000000000000 ) ) ;
#16057=VERTEX_POINT ( 'NONE', #2883 ) ;
#16059=CARTESIAN_POINT ( 'NONE',  ( 10.00000000000000000, 31.47745569255140552, 68.26794271651274926 ) ) ;
#16067=DIRECTION ( 'NONE',  ( 0.000000000000000000, 0.000000000000000000, 1.000000000000000000 ) ) ;
#16068=DIRECTION ( 'NONE',  ( -1.000000000000000000, 0.000000000000000000, -0.000000000000000000 ) ) ;
#16082=EDGE_CURVE ( 'NONE', #18399, #15510, #34705, .T. ) ;
#16089=LINE ( 'NONE', #41789, #32629 ) ;
#16092=CIRCLE ( 'NONE', #32503, 77.49900000000000944 ) ;
#16095=EDGE_CURVE ( 'NONE', #37458, #32278, #47976, .T. ) ;
#16097=VERTEX_POINT ( 'NONE', #47656 ) ;
#16098=AXIS2_PLACEMENT_3D ( 'NONE', #33343, #22070, #26976 ) ;
#16112=AXIS2_PLACEMENT_3D ( 'NONE', #10642, #4017, #37536 ) ;
#16113=CARTESIAN_POINT ( 'NONE',  ( 10.00000000000000000, 73.72996012237440766, 14.67089635893739619 ) ) ;
#16115=CARTESIAN_POINT ( 'NONE',  ( 10.00000000000000000, -63.18004540532994184, -44.88180994100446952 ) ) ;
#16121=EDGE_LOOP ( 'NONE', ( #42410, #33420, #3077, #32947 ) ) ;
#16134=DIRECTION ( 'NONE',  ( 0.000000000000000000, -0.9723699203976741146, -0.2334453638559159938 ) ) ;
#16136=CYLINDRICAL_SURFACE ( 'NONE', #33768, 31.99999999999998579 ) ;
#16138=CARTESIAN_POINT ( 'NONE',  ( 10.00000000000000000, 44.88180994100376608, 63.18004540533043922 ) ) ;
#16139=DIRECTION ( 'NONE',  ( -1.000000000000000000, -0.000000000000000000, 0.000000000000000000 ) ) ;
#16145=CARTESIAN_POINT ( 'NONE',  ( 0.000000000000000000, 0.000000000000000000, 0.000000000000000000 ) ) ;
#16148=CIRCLE ( 'NONE', #13034, 31.99999999999999645 ) ;
#16149=CARTESIAN_POINT ( 'NONE',  ( 10.00000000000000000, -71.27951684758005513, -30.41916302227188851 ) ) ;
#16151=ORIENTED_EDGE ( 'NONE', *, *, #21841, .F. ) ;
#16152=EDGE_LOOP ( 'NONE', ( #17641, #14948, #9535, #28608, #28788, #42030 ) ) ;
#16153=AXIS2_PLACEMENT_3D ( 'NONE', #38896, #35198, #45488 ) ;
#16164=DIRECTION ( 'NONE',  ( -1.000000000000000000, 0.000000000000000000, -0.000000000000000000 ) ) ;
#16166=ORIENTED_EDGE ( 'NONE', *, *, #8554, .T. ) ;
#16169=ADVANCED_FACE ( 'NONE', ( #38862 ), #34931, .F. ) ;
#16170=VECTOR ( 'NONE', #37595, 1000.000000000000000 ) ;
#16173=DIRECTION ( 'NONE',  ( 0.000000000000000000, 0.000000000000000000, 1.000000000000000000 ) ) ;
#16178=CARTESIAN_POINT ( 'NONE',  ( 10.00000000000000000, 0.000000000000000000, 0.000000000000000000 ) ) ;
#16182=CYLINDRICAL_SURFACE ( 'NONE', #41434, 31.99999999999999289 ) ;
#16186=CYLINDRICAL_SURFACE ( 'NONE', #23290, 31.99999999999999289 ) ;
#16188=VERTEX_POINT ( 'NONE', #18615 ) ;
#16190=FACE_OUTER_BOUND ( 'NONE', #18618, .T. ) ;
#16191=ORIENTED_EDGE ( 'NONE', *, *, #10842, .F. ) ;
#16192=CARTESIAN_POINT ( 'NONE',  ( 10.00000000000000000, 0.000000000000000000, 0.000000000000000000 ) ) ;
#16193=DIRECTION ( 'NONE',  ( 0.000000000000000000, 0.2334453638558990629, 0.9723699203976782224 ) ) ;
#16194=CYLINDRICAL_SURFACE ( 'NONE', #32349, 77.49899999999999523 ) ;
#16195=LINE ( 'NONE', #11788, #10114 ) ;
#16198=DIRECTION ( 'NONE',  ( 0.000000000000000000, 0.5877852522924743583, -0.8090169943749466741 ) ) ;
#16203=ADVANCED_FACE ( 'NONE', ( #20240 ), #31042, .T. ) ;
#16213=CARTESIAN_POINT ( 'NONE',  ( 0.000000000000000000, 16.65972982744934683, 80.28980883073764119 ) ) ;
#16215=ORIENTED_EDGE ( 'NONE', *, *, #47311, .F. ) ;
#16216=ADVANCED_FACE ( 'NONE', ( #14952 ), #42278, .T. ) ;
#16220=LINE ( 'NONE', #31149, #44809 ) ;
#16226=AXIS2_PLACEMENT_3D ( 'NONE', #39692, #17379, #45626 ) ;
#16228=DIRECTION ( 'NONE',  ( -1.000000000000000000, -0.000000000000000000, 0.000000000000000000 ) ) ;
#16233=ORIENTED_EDGE ( 'NONE', *, *, #47249, .F. ) ;
#16248=CARTESIAN_POINT ( 'NONE',  ( 0.000000000000000000, -26.02418014898260878, -70.52718814184285634 ) ) ;
#16251=ORIENTED_EDGE ( 'NONE', *, *, #20509, .F. ) ;
#16257=CARTESIAN_POINT ( 'NONE',  ( 0.000000000000000000, 12.24744871391589207, -2.500000000000000000 ) ) ;
#16263=CARTESIAN_POINT ( 'NONE',  ( 10.00000000000000000, 33.71516098798738881, 74.74816331893441657 ) ) ;
#16270=EDGE_LOOP ( 'NONE', ( #45415, #28292, #7339, #47446 ) ) ;
#16274=CARTESIAN_POINT ( 'NONE',  ( 10.00000000000000000, 0.000000000000000000, 0.000000000000000000 ) ) ;
#16277=ORIENTED_EDGE ( 'NONE', *, *, #27478, .T. ) ;
#16284=CARTESIAN_POINT ( 'NONE',  ( 0.000000000000000000, 0.000000000000000000, 0.000000000000000000 ) ) ;
#16288=DIRECTION ( 'NONE',  ( -1.000000000000000000, 0.000000000000000000, 0.000000000000000000 ) ) ;
#16292=ORIENTED_EDGE ( 'NONE', *, *, #10459, .F. ) ;
#16294=CARTESIAN_POINT ( 'NONE',  ( 5.000000000000000000, 59.75363087400076267, 56.15606465354979804 ) ) ;
#16304=CARTESIAN_POINT ( 'NONE',  ( 0.000000000000000000, 31.47745569255237896, -68.26794271651228030 ) ) ;
#16306=CARTESIAN_POINT ( 'NONE',  ( 0.000000000000000000, -46.54456581323847786, 59.03342792756247093 ) ) ;
#16308=ORIENTED_EDGE ( 'NONE', *, *, #14363, .T. ) ;
#16310=DIRECTION ( 'NONE',  ( 0.000000000000000000, 0.000000000000000000, 1.000000000000000000 ) ) ;
#16311=DIRECTION ( 'NONE',  ( -1.000000000000000000, 0.000000000000000000, -0.000000000000000000 ) ) ;
#16318=DIRECTION ( 'NONE',  ( 0.000000000000000000, -1.000000000000000000, -1.047444401652940007E-14 ) ) ;
#16319=DIRECTION ( 'NONE',  ( -1.000000000000000000, 0.000000000000000000, 0.000000000000000000 ) ) ;
#16321=EDGE_CURVE ( 'NONE', #37827, #4186, #39591, .T. ) ;
#16326=VERTEX_POINT ( 'NONE', #25109 ) ;
#16330=VERTEX_POINT ( 'NONE', #39821 ) ;
#16331=ORIENTED_EDGE ( 'NONE', *, *, #45098, .F. ) ;
#16333=LINE ( 'NONE', #23671, #34343 ) ;
#16336=VERTEX_POINT ( 'NONE', #21446 ) ;
#16337=ORIENTED_EDGE ( 'NONE', *, *, #21370, .T. ) ;
#16340=DIRECTION ( 'NONE',  ( 0.000000000000000000, 0.9238795325112877377, -0.3826834323650873948 ) ) ;
#16342=ORIENTED_EDGE ( 'NONE', *, *, #39396, .F. ) ;
#16345=EDGE_LOOP ( 'NONE', ( #39958, #11783, #3118, #42820 ) ) ;
#16351=CYLINDRICAL_SURFACE ( 'NONE', #9244, 31.99999999999999289 ) ;
#16354=CARTESIAN_POINT ( 'NONE',  ( 10.00000000000000000, -36.72794159290197769, -65.59268652807249111 ) ) ;
#16358=VERTEX_POINT ( 'NONE', #43494 ) ;
#16365=DIRECTION ( 'NONE',  ( -1.000000000000000000, -0.000000000000000000, -0.000000000000000000 ) ) ;
#16370=ADVANCED_FACE ( 'NONE', ( #32473 ), #20969, .T. ) ;
#16381=EDGE_LOOP ( 'NONE', ( #37018, #9155, #5261, #38103 ) ) ;
#16383=DIRECTION ( 'NONE',  ( -1.000000000000000000, 0.000000000000000000, -0.000000000000000000 ) ) ;
#16387=ORIENTED_EDGE ( 'NONE', *, *, #24090, .F. ) ;
#16388=DIRECTION ( 'NONE',  ( -1.000000000000000000, 0.000000000000000000, -0.000000000000000000 ) ) ;
#16390=ORIENTED_EDGE ( 'NONE', *, *, #30873, .F. ) ;
#16394=AXIS2_PLACEMENT_3D ( 'NONE', #36221, #14441, #32559 ) ;
#16395=DIRECTION ( 'NONE',  ( 1.000000000000000000, -0.000000000000000000, -0.000000000000000000 ) ) ;
#16400=ORIENTED_EDGE ( 'NONE', *, *, #4810, .T. ) ;
#16406=EDGE_CURVE ( 'NONE', #24069, #25536, #23814, .T. ) ;
#16410=ORIENTED_EDGE ( 'NONE', *, *, #3692, .F. ) ;
#16412=DIRECTION ( 'NONE',  ( 0.000000000000000000, 0.000000000000000000, 1.000000000000000000 ) ) ;
#16415=ORIENTED_EDGE ( 'NONE', *, *, #19618, .F. ) ;
#16420=CARTESIAN_POINT ( 'NONE',  ( 10.00000000000000000, 80.55351364060589958, 15.33399622253511829 ) ) ;
#16423=EDGE_CURVE ( 'NONE', #46298, #39398, #4298, .T. ) ;
#16428=CARTESIAN_POINT ( 'NONE',  ( 10.00000000000000000, 0.000000000000000000, 0.000000000000000000 ) ) ;
#16430=CARTESIAN_POINT ( 'NONE',  ( 5.000000000000000000, 50.23322058963348979, 64.81221759200361987 ) ) ;
#16435=ORIENTED_EDGE ( 'NONE', *, *, #17228, .T. ) ;
#16437=AXIS2_PLACEMENT_3D ( 'NONE', #16284, #20920, #35351 ) ;
#16441=AXIS2_PLACEMENT_3D ( 'NONE', #21159, #9916, #24841 ) ;
#16447=CIRCLE ( 'NONE', #43794, 82.00000000000000000 ) ;
#16448=AXIS2_PLACEMENT_3D ( 'NONE', #21757, #32546, #47469 ) ;
#16454=FACE_OUTER_BOUND ( 'NONE', #16954, .T. ) ;
#16459=VERTEX_POINT ( 'NONE', #22419 ) ;
#16464=DIRECTION ( 'NONE',  ( 0.000000000000000000, 0.4539904997395478592, -0.8910065241883673437 ) ) ;
#16466=DIRECTION ( 'NONE',  ( 0.000000000000000000, 0.000000000000000000, -1.000000000000000000 ) ) ;
#16467=ADVANCED_FACE ( 'NONE', ( #11158 ), #21688, .T. ) ;
#16472=ORIENTED_EDGE ( 'NONE', *, *, #33810, .F. ) ;
#16481=ORIENTED_EDGE ( 'NONE', *, *, #28773, .F. ) ;
#16486=EDGE_CURVE ( 'NONE', #6719, #25698, #3808, .T. ) ;
#16487=CIRCLE ( 'NONE', #25060, 77.49899999999999523 ) ;
#16492=EDGE_CURVE ( 'NONE', #42004, #39534, #44679, .T. ) ;
#16495=LINE ( 'NONE', #46606, #18957 ) ;
#16496=CARTESIAN_POINT ( 'NONE',  ( 0.000000000000000000, 46.53671651293948486, 59.03961581697416250 ) ) ;
#16497=ORIENTED_EDGE ( 'NONE', *, *, #37932, .F. ) ;
#16500=VERTEX_POINT ( 'NONE', #6766 ) ;
#16503=ORIENTED_EDGE ( 'NONE', *, *, #17245, .F. ) ;
#16506=CIRCLE ( 'NONE', #43854, 31.99999999999999645 ) ;
#16508=CIRCLE ( 'NONE', #7099, 31.99999999999999289 ) ;
#16509=CARTESIAN_POINT ( 'NONE',  ( 0.000000000000000000, -80.28980883073747066, -16.65972982745018172 ) ) ;
#16510=VERTEX_POINT ( 'NONE', #17768 ) ;
#16514=EDGE_CURVE ( 'NONE', #10059, #21026, #35524, .T. ) ;
#16515=FACE_OUTER_BOUND ( 'NONE', #42522, .T. ) ;
#16518=EDGE_CURVE ( 'NONE', #38732, #28147, #12892, .T. ) ;
#16520=VERTEX_POINT ( 'NONE', #44208 ) ;
#16522=CARTESIAN_POINT ( 'NONE',  ( 5.000000000000002665, 76.69515212746057387, -29.01471420065480089 ) ) ;
#16524=DIRECTION ( 'NONE',  ( 0.000000000000000000, -0.3826834323650969427, 0.9238795325112838519 ) ) ;
#16528=VERTEX_POINT ( 'NONE', #18247 ) ;
#16534=CARTESIAN_POINT ( 'NONE',  ( 10.00000000000000000, -34.44570377933549565, -69.42325613327476219 ) ) ;
#16536=CYLINDRICAL_SURFACE ( 'NONE', #14202, 77.49899999999999523 ) ;
#16541=AXIS2_PLACEMENT_3D ( 'NONE', #42862, #3344, #16665 ) ;
#16545=ORIENTED_EDGE ( 'NONE', *, *, #44613, .F. ) ;
#16546=AXIS2_PLACEMENT_3D ( 'NONE', #20677, #35613, #23617 ) ;
#16552=DIRECTION ( 'NONE',  ( 0.000000000000000000, 0.000000000000000000, 1.000000000000000000 ) ) ;
#16556=ORIENTED_EDGE ( 'NONE', *, *, #42094, .T. ) ;
#16558=ORIENTED_EDGE ( 'NONE', *, *, #10123, .F. ) ;
#16563=ORIENTED_EDGE ( 'NONE', *, *, #11221, .F. ) ;
#16564=DIRECTION ( 'NONE',  ( -1.000000000000000000, -0.000000000000000000, -0.000000000000000000 ) ) ;
#16578=CARTESIAN_POINT ( 'NONE',  ( 10.00000000000000000, 70.52718814184260054, 26.02418014898334420 ) ) ;
#16589=CARTESIAN_POINT ( 'NONE',  ( 10.00000000000000000, -66.50666863322028632, 39.78640506895582973 ) ) ;
#16590=CARTESIAN_POINT ( 'NONE',  ( 5.000000000000002665, -29.01471420065507090, -76.69515212746047439 ) ) ;
#16593=EDGE_LOOP ( 'NONE', ( #31231, #16472, #20682, #31901 ) ) ;
#16594=DIRECTION ( 'NONE',  ( 0.000000000000000000, 0.000000000000000000, 1.000000000000000000 ) ) ;
#16597=DIRECTION ( 'NONE',  ( -1.000000000000000000, -0.000000000000000000, 0.000000000000000000 ) ) ;
#16608=VECTOR ( 'NONE', #3956, 1000.000000000000000 ) ;
#16613=VECTOR ( 'NONE', #18072, 1000.000000000000000 ) ;
#16614=FACE_OUTER_BOUND ( 'NONE', #26415, .T. ) ;
#16621=CIRCLE ( 'NONE', #2521, 31.99999999999999289 ) ;
#16627=ORIENTED_EDGE ( 'NONE', *, *, #4831, .F. ) ;
#16631=EDGE_LOOP ( 'NONE', ( #4339, #13387, #23556, #39750 ) ) ;
#16633=VECTOR ( 'NONE', #41926, 1000.000000000000000 ) ;
#16635=EDGE_CURVE ( 'NONE', #18426, #20915, #45692, .T. ) ;
#16638=FACE_OUTER_BOUND ( 'NONE', #1988, .T. ) ;
#16640=LINE ( 'NONE', #27922, #21572 ) ;
#16646=DIRECTION ( 'NONE',  ( -1.000000000000000000, -0.000000000000000000, -0.000000000000000000 ) ) ;
#16647=CIRCLE ( 'NONE', #45571, 31.99999999999999289 ) ;
#16649=CARTESIAN_POINT ( 'NONE',  ( 10.00000000000000000, 0.000000000000000000, 0.000000000000000000 ) ) ;
#16662=CARTESIAN_POINT ( 'NONE',  ( 10.00000000000000000, -49.70050353004933896, 59.46389618801946852 ) ) ;
#16665=DIRECTION ( 'NONE',  ( 0.000000000000000000, 0.8090169943749445647, 0.5877852522924770229 ) ) ;
#16666=DIRECTION ( 'NONE',  ( 0.000000000000000000, 0.000000000000000000, -1.000000000000000000 ) ) ;
#16670=CARTESIAN_POINT ( 'NONE',  ( 10.00000000000000000, 22.90783923731629912, 78.73519480814962890 ) ) ;
#16679=EDGE_LOOP ( 'NONE', ( #14615, #46737, #29326, #26819 ) ) ;
#16689=EDGE_CURVE ( 'NONE', #12049, #42351, #19155, .T. ) ;
#16692=CIRCLE ( 'NONE', #9651, 32.00000000000000000 ) ;
#16695=AXIS2_PLACEMENT_3D ( 'NONE', #45570, #19614, #34797 ) ;
#16702=DIRECTION ( 'NONE',  ( -1.000000000000000000, 0.000000000000000000, 0.000000000000000000 ) ) ;
#16710=CARTESIAN_POINT ( 'NONE',  ( 0.000000000000000000, 0.000000000000000000, 0.000000000000000000 ) ) ;
#16714=DIRECTION ( 'NONE',  ( 0.000000000000000000, -0.9876883405951394357, 0.1564344650402205716 ) ) ;
#16725=DIRECTION ( 'NONE',  ( 0.000000000000000000, 0.000000000000000000, -1.000000000000000000 ) ) ;
#16727=DIRECTION ( 'NONE',  ( 1.000000000000000000, -0.000000000000000000, 0.000000000000000000 ) ) ;
#16733=CIRCLE ( 'NONE', #42515, 31.99999999999998934 ) ;
#16747=EDGE_CURVE ( 'NONE', #19851, #37098, #44183, .T. ) ;
#16751=EDGE_CURVE ( 'NONE', #13135, #8929, #13566, .T. ) ;
#16752=VECTOR ( 'NONE', #22401, 1000.000000000000000 ) ;
#16753=DIRECTION ( 'NONE',  ( -1.000000000000000000, -0.000000000000000000, -0.000000000000000000 ) ) ;
#16754=ORIENTED_EDGE ( 'NONE', *, *, #37639, .T. ) ;
#16755=AXIS2_PLACEMENT_3D ( 'NONE', #22368, #41685, #4489 ) ;
#16760=AXIS2_PLACEMENT_3D ( 'NONE', #45321, #4930, #26492 ) ;
#16768=ORIENTED_EDGE ( 'NONE', *, *, #35202, .T. ) ;
#16772=FACE_OUTER_BOUND ( 'NONE', #46505, .T. ) ;
#16773=CYLINDRICAL_SURFACE ( 'NONE', #18054, 77.49899999999999523 ) ;
#16778=DIRECTION ( 'NONE',  ( -1.000000000000000000, 0.000000000000000000, 0.000000000000000000 ) ) ;
#16789=LINE ( 'NONE', #5293, #39453 ) ;
#16791=CARTESIAN_POINT ( 'NONE',  ( 10.00000000000000000, -22.90783923731686045, 78.73519480814947258 ) ) ;
#16805=ORIENTED_EDGE ( 'NONE', *, *, #10306, .T. ) ;
#16809=EDGE_CURVE ( 'NONE', #42385, #17337, #29333, .T. ) ;
#16811=VERTEX_POINT ( 'NONE', #5270 ) ;
#16824=ORIENTED_EDGE ( 'NONE', *, *, #45776, .T. ) ;
#16826=CARTESIAN_POINT ( 'NONE',  ( 0.000000000000000000, 0.000000000000000000, 0.000000000000000000 ) ) ;
#16831=AXIS2_PLACEMENT_3D ( 'NONE', #16042, #45903, #12372 ) ;
#16832=VECTOR ( 'NONE', #40488, 1000.000000000000000 ) ;
#16834=ORIENTED_EDGE ( 'NONE', *, *, #14657, .T. ) ;
#16837=VERTEX_POINT ( 'NONE', #6002 ) ;
#16845=AXIS2_PLACEMENT_3D ( 'NONE', #6723, #9912, #32192 ) ;
#16847=AXIS2_PLACEMENT_3D ( 'NONE', #42842, #9526, #24226 ) ;
#16848=ORIENTED_EDGE ( 'NONE', *, *, #36407, .T. ) ;
#16849=CARTESIAN_POINT ( 'NONE',  ( 10.00000000000000000, 14.66109333815564852, -73.73191006444555740 ) ) ;
#16852=ORIENTED_EDGE ( 'NONE', *, *, #36974, .F. ) ;
#16855=CARTESIAN_POINT ( 'NONE',  ( 10.00000000000000000, 16.00000000000000000, 2.500000000000000000 ) ) ;
#16856=CARTESIAN_POINT ( 'NONE',  ( 10.00000000000000000, 26.01480285779837232, 70.53064760720326376 ) ) ;
#16868=FACE_OUTER_BOUND ( 'NONE', #178, .T. ) ;
#16884=CARTESIAN_POINT ( 'NONE',  ( 10.00000000000000000, 59.46389618801964616, 49.70050353004912580 ) ) ;
#16888=CARTESIAN_POINT ( 'NONE',  ( 5.000000000000002665, -15.33399622253540961, 80.55351364060584274 ) ) ;
#16893=DIRECTION ( 'NONE',  ( -1.000000000000000000, -0.000000000000000000, 0.000000000000000000 ) ) ;
#16895=DIRECTION ( 'NONE',  ( 0.000000000000000000, 0.8526401643540897357, 0.5224985647159527957 ) ) ;
#16899=EDGE_LOOP ( 'NONE', ( #27921, #7087, #29702, #3125 ) ) ;
#16901=CARTESIAN_POINT ( 'NONE',  ( 10.00000000000000000, 20.41045688087824317, 72.35160999960824313 ) ) ;
#16914=CARTESIAN_POINT ( 'NONE',  ( 0.000000000000000000, 0.000000000000000000, 0.000000000000000000 ) ) ;
#16915=DIRECTION ( 'NONE',  ( 0.000000000000000000, 0.000000000000000000, 1.000000000000000000 ) ) ;
#16932=ORIENTED_EDGE ( 'NONE', *, *, #2858, .F. ) ;
#16938=CARTESIAN_POINT ( 'NONE',  ( 0.000000000000000000, 72.35432306680485226, -20.40083707022909110 ) ) ;
#16943=ORIENTED_EDGE ( 'NONE', *, *, #35910, .T. ) ;
#16945=EDGE_LOOP ( 'NONE', ( #35652, #28531, #24276, #41690 ) ) ;
#16946=FACE_OUTER_BOUND ( 'NONE', #5, .T. ) ;
#16951=EDGE_CURVE ( 'NONE', #42453, #25698, #5092, .T. ) ;
#16953=FACE_OUTER_BOUND ( 'NONE', #16899, .T. ) ;
#16954=EDGE_LOOP ( 'NONE', ( #31269, #18842, #10686, #47162 ) ) ;
#16961=ORIENTED_EDGE ( 'NONE', *, *, #13271, .T. ) ;
#16964=FACE_OUTER_BOUND ( 'NONE', #10638, .T. ) ;
#16978=CIRCLE ( 'NONE', #25562, 31.99999999999999289 ) ;
#16984=CIRCLE ( 'NONE', #39647, 31.99999999999999289 ) ;
#16985=DIRECTION ( 'NONE',  ( 0.000000000000000000, 0.000000000000000000, 1.000000000000000000 ) ) ;
#16987=ORIENTED_EDGE ( 'NONE', *, *, #32284, .T. ) ;
#16989=AXIS2_PLACEMENT_3D ( 'NONE', #46584, #31174, #27984 ) ;
#16993=VERTEX_POINT ( 'NONE', #23079 ) ;
#16994=EDGE_LOOP ( 'NONE', ( #22606, #17002, #45762, #17637 ) ) ;
#16996=DIRECTION ( 'NONE',  ( 0.000000000000000000, 0.000000000000000000, 1.000000000000000000 ) ) ;
#17000=LINE ( 'NONE', #27307, #46240 ) ;
#17002=ORIENTED_EDGE ( 'NONE', *, *, #28792, .T. ) ;
#17003=VECTOR ( 'NONE', #15702, 1000.000000000000000 ) ;
#17005=DIRECTION ( 'NONE',  ( 0.000000000000000000, 0.7604059656000322631, -0.6494480483301821039 ) ) ;
#17006=EDGE_LOOP ( 'NONE', ( #23419, #31960, #37973, #1005 ) ) ;
#17015=DIRECTION ( 'NONE',  ( -1.000000000000000000, 0.000000000000000000, 0.000000000000000000 ) ) ;
#17016=DIRECTION ( 'NONE',  ( -1.000000000000000000, 0.000000000000000000, 0.000000000000000000 ) ) ;
#17020=ORIENTED_EDGE ( 'NONE', *, *, #32797, .T. ) ;
#17022=DIRECTION ( 'NONE',  ( -1.000000000000000000, 0.000000000000000000, 0.000000000000000000 ) ) ;
#17025=EDGE_CURVE ( 'NONE', #9834, #45908, #11392, .T. ) ;
#17028=DIRECTION ( 'NONE',  ( 0.000000000000000000, -0.4539904997395542430, 0.8910065241883641241 ) ) ;
#17033=VECTOR ( 'NONE', #44604, 1000.000000000000000 ) ;
#17040=EDGE_CURVE ( 'NONE', #41560, #21364, #32481, .T. ) ;
#17044=PRODUCT_DEFINITION_FORMATION_WITH_SPECIFIED_SOURCE ( 'ANY', '', #10492, .NOT_KNOWN. ) ;
#17046=CIRCLE ( 'NONE', #21734, 82.00000000000000000 ) ;
#17048=CYLINDRICAL_SURFACE ( 'NONE', #23417, 77.49899999999999523 ) ;
#17050=ORIENTED_EDGE ( 'NONE', *, *, #13967, .T. ) ;
#17064=EDGE_CURVE ( 'NONE', #35099, #2146, #5132, .T. ) ;
#17070=EDGE_LOOP ( 'NONE', ( #21467, #603, #21588, #8911 ) ) ;
#17072=DIRECTION ( 'NONE',  ( 0.000000000000000000, 0.000000000000000000, 1.000000000000000000 ) ) ;
#17078=ORIENTED_EDGE ( 'NONE', *, *, #14320, .F. ) ;
#17080=CARTESIAN_POINT ( 'NONE',  ( -10.00000000000000000, 0.000000000000000000, 0.000000000000000000 ) ) ;
#17091=CARTESIAN_POINT ( 'NONE',  ( 10.00000000000000000, 50.95692526931414790, -58.39081064771693974 ) ) ;
#17103=CARTESIAN_POINT ( 'NONE',  ( 10.00000000000000000, 73.72996012237460661, -14.67089635893632504 ) ) ;
#17107=CARTESIAN_POINT ( 'NONE',  ( 0.000000000000000000, 0.000000000000000000, 0.000000000000000000 ) ) ;
#17113=DIRECTION ( 'NONE',  ( 0.000000000000000000, 1.000000000000000000, 3.469446951953614978E-15 ) ) ;
#17117=ADVANCED_FACE ( 'NONE', ( #20860 ), #9580, .T. ) ;
#17121=VERTEX_POINT ( 'NONE', #17167 ) ;
#17127=DIRECTION ( 'NONE',  ( 0.000000000000000000, 0.000000000000000000, 1.000000000000000000 ) ) ;
#17132=CARTESIAN_POINT ( 'NONE',  ( 0.000000000000000000, 0.000000000000000000, 0.000000000000000000 ) ) ;
#17133=CARTESIAN_POINT ( 'NONE',  ( 10.00000000000000000, -76.41127070299262414, -12.93880638057396304 ) ) ;
#17152=CARTESIAN_POINT ( 'NONE',  ( 10.00000000000000000, -44.88180994100329713, -63.18004540533077318 ) ) ;
#17160=VECTOR ( 'NONE', #26559, 1000.000000000000000 ) ;
#17162=DIRECTION ( 'NONE',  ( -1.000000000000000000, -0.000000000000000000, 0.000000000000000000 ) ) ;
#17164=CARTESIAN_POINT ( 'NONE',  ( 10.00000000000000000, 80.55351364060609853, -15.33399622253395478 ) ) ;
#17167=CARTESIAN_POINT ( 'NONE',  ( 0.000000000000000000, 15.33399622253481986, 80.55351364060595643 ) ) ;
#17171=DIRECTION ( 'NONE',  ( 0.000000000000000000, -0.8910065241883626808, -0.4539904997395568520 ) ) ;
#17174=DIRECTION ( 'NONE',  ( 0.000000000000000000, 0.000000000000000000, 1.000000000000000000 ) ) ;
#17178=ORIENTED_EDGE ( 'NONE', *, *, #9821, .F. ) ;
#17182=ADVANCED_FACE ( 'NONE', ( #46807 ), #42658, .T. ) ;
#17186=CARTESIAN_POINT ( 'NONE',  ( 5.000000000000000000, 74.74816331893477184, -33.71516098798660011 ) ) ;
#17189=CARTESIAN_POINT ( 'NONE',  ( 0.000000000000000000, -46.53671651293907274, -59.03961581697448935 ) ) ;
#17190=LINE ( 'NONE', #13533, #14575 ) ;
#17192=ORIENTED_EDGE ( 'NONE', *, *, #31810, .T. ) ;
#17194=LINE ( 'NONE', #24559, #29356 ) ;
#17201=AXIS2_PLACEMENT_3D ( 'NONE', #17486, #39783, #14562 ) ;
#17204=ORIENTED_EDGE ( 'NONE', *, *, #25075, .F. ) ;
#17205=DIRECTION ( 'NONE',  ( 0.000000000000000000, 0.000000000000000000, -1.000000000000000000 ) ) ;
#17216=ORIENTED_EDGE ( 'NONE', *, *, #10539, .T. ) ;
#17228=EDGE_CURVE ( 'NONE', #23138, #21614, #9800, .T. ) ;
#17231=AXIS2_PLACEMENT_3D ( 'NONE', #36035, #5961, #24547 ) ;
#17234=CIRCLE ( 'NONE', #15670, 82.00000000000000000 ) ;
#17236=ORIENTED_EDGE ( 'NONE', *, *, #7008, .T. ) ;
#17237=CARTESIAN_POINT ( 'NONE',  ( 10.00000000000000000, 0.000000000000000000, 0.000000000000000000 ) ) ;
#17239=CARTESIAN_POINT ( 'NONE',  ( 0.000000000000000000, -71.27951684758005513, -30.41916302227188851 ) ) ;
#17241=DIRECTION ( 'NONE',  ( -1.000000000000000000, -0.000000000000000000, 0.000000000000000000 ) ) ;
#17245=EDGE_CURVE ( 'NONE', #43246, #31534, #12793, .T. ) ;
#17251=CARTESIAN_POINT ( 'NONE',  ( 10.00000000000000000, -68.26794271651286294, 31.47745569255117104 ) ) ;
#17260=CARTESIAN_POINT ( 'NONE',  ( 50.00005079999999680, 1.530808498934191521E-15, -12.50000000000000000 ) ) ;
#17262=AXIS2_PLACEMENT_3D ( 'NONE', #40371, #21024, #9772 ) ;
#17266=ORIENTED_EDGE ( 'NONE', *, *, #1665, .T. ) ;
#17278=ORIENTED_EDGE ( 'NONE', *, *, #22459, .F. ) ;
#17282=EDGE_CURVE ( 'NONE', #11314, #15196, #34807, .T. ) ;
#17289=VERTEX_POINT ( 'NONE', #2958 ) ;
#17295=CIRCLE ( 'NONE', #12640, 31.99999999999998934 ) ;
#17302=ADVANCED_FACE ( 'NONE', ( #47990 ), #36971, .T. ) ;
#17304=ORIENTED_EDGE ( 'NONE', *, *, #11208, .T. ) ;
#17307=VERTEX_POINT ( 'NONE', #6406 ) ;
#17324=CIRCLE ( 'NONE', #34507, 82.00000000000000000 ) ;
#17335=CARTESIAN_POINT ( 'NONE',  ( 10.00000000000000000, 11.30684508768452545, -76.66974797899825944 ) ) ;
#17336=VECTOR ( 'NONE', #33002, 1000.000000000000000 ) ;
#17337=VERTEX_POINT ( 'NONE', #18380 ) ;
#17338=VERTEX_POINT ( 'NONE', #33062 ) ;
#17349=DIRECTION ( 'NONE',  ( -1.000000000000000000, 0.000000000000000000, 0.000000000000000000 ) ) ;
#17353=VECTOR ( 'NONE', #3541, 1000.000000000000000 ) ;
#17355=ADVANCED_FACE ( 'NONE', ( #28688 ), #33313, .T. ) ;
#17358=ORIENTED_EDGE ( 'NONE', *, *, #47210, .F. ) ;
#17361=ORIENTED_EDGE ( 'NONE', *, *, #772, .T. ) ;
#17371=ORIENTED_EDGE ( 'NONE', *, *, #31569, .T. ) ;
#17372=DIRECTION ( 'NONE',  ( -1.000000000000000000, 0.000000000000000000, 0.000000000000000000 ) ) ;
#17375=DIRECTION ( 'NONE',  ( -1.000000000000000000, 0.000000000000000000, 0.000000000000000000 ) ) ;
#17376=CARTESIAN_POINT ( 'NONE',  ( 10.00000000000000000, 0.000000000000000000, 0.000000000000000000 ) ) ;
#17377=CARTESIAN_POINT ( 'NONE',  ( 10.00000000000000000, 0.000000000000000000, 0.000000000000000000 ) ) ;
#17379=DIRECTION ( 'NONE',  ( -1.000000000000000000, 0.000000000000000000, 0.000000000000000000 ) ) ;
#17380=VERTEX_POINT ( 'NONE', #6650 ) ;
#17386=LINE ( 'NONE', #24268, #12826 ) ;
#17390=VERTEX_POINT ( 'NONE', #30377 ) ;
#17392=CYLINDRICAL_SURFACE ( 'NONE', #27345, 82.00000000000000000 ) ;
#17399=ORIENTED_EDGE ( 'NONE', *, *, #36997, .T. ) ;
#17401=AXIS2_PLACEMENT_3D ( 'NONE', #47114, #9918, #40021 ) ;
#17406=ORIENTED_EDGE ( 'NONE', *, *, #33644, .F. ) ;
#17408=CARTESIAN_POINT ( 'NONE',  ( 10.00000000000000000, 73.95703589263975175, 23.16143007188454206 ) ) ;
#17409=CYLINDRICAL_SURFACE ( 'NONE', #38553, 77.49899999999999523 ) ;
#17411=CARTESIAN_POINT ( 'NONE',  ( 10.00000000000000000, 33.71516098798847594, -74.74816331893393340 ) ) ;
#17415=ORIENTED_EDGE ( 'NONE', *, *, #3021, .F. ) ;
#17417=ORIENTED_EDGE ( 'NONE', *, *, #19584, .F. ) ;
#17418=ORIENTED_EDGE ( 'NONE', *, *, #40350, .F. ) ;
#17419=CARTESIAN_POINT ( 'NONE',  ( 10.00000000000000178, 12.24744871391589207, -2.500000000000000000 ) ) ;
#17427=DIRECTION ( 'NONE',  ( 0.000000000000000000, 0.000000000000000000, 1.000000000000000000 ) ) ;
#17430=DIRECTION ( 'NONE',  ( -1.000000000000000000, -0.000000000000000000, -0.000000000000000000 ) ) ;
#17431=EDGE_CURVE ( 'NONE', #43019, #14493, #36077, .T. ) ;
#17437=AXIS2_PLACEMENT_3D ( 'NONE', #12443, #258, #41163 ) ;
#17440=DIRECTION ( 'NONE',  ( 0.000000000000000000, -0.3090169943749349057, -0.9510565162951577500 ) ) ;
#17441=DIRECTION ( 'NONE',  ( 0.000000000000000000, 0.4539904997395413089, 0.8910065241883705633 ) ) ;
#17442=VECTOR ( 'NONE', #14635, 1000.000000000000000 ) ;
#17444=VERTEX_POINT ( 'NONE', #30606 ) ;
#17446=DIRECTION ( 'NONE',  ( 0.000000000000000000, 0.000000000000000000, 1.000000000000000000 ) ) ;
#17453=DIRECTION ( 'NONE',  ( -1.000000000000000000, 0.000000000000000000, -0.000000000000000000 ) ) ;
#17454=AXIS2_PLACEMENT_3D ( 'NONE', #6941, #28964, #32638 ) ;
#17460=VERTEX_POINT ( 'NONE', #7 ) ;
#17461=VECTOR ( 'NONE', #5364, 1000.000000000000000 ) ;
#17467=VECTOR ( 'NONE', #39696, 1000.000000000000000 ) ;
#17468=ORIENTED_EDGE ( 'NONE', *, *, #37371, .F. ) ;
#17469=CARTESIAN_POINT ( 'NONE',  ( 5.000000000000000000, -27.74655509720725988, 77.16300072079653205 ) ) ;
#17470=VERTEX_POINT ( 'NONE', #4659 ) ;
#17473=DIRECTION ( 'NONE',  ( -1.000000000000000000, -0.000000000000000000, -0.000000000000000000 ) ) ;
#17482=CIRCLE ( 'NONE', #22941, 31.99999999999999289 ) ;
#17486=CARTESIAN_POINT ( 'NONE',  ( 0.000000000000000000, 72.35160999960817207, 20.41045688087850607 ) ) ;
#17495=VERTEX_POINT ( 'NONE', #45290 ) ;
#17499=CARTESIAN_POINT ( 'NONE',  ( 0.000000000000000000, 0.000000000000000000, 0.000000000000000000 ) ) ;
#17501=ADVANCED_FACE ( 'NONE', ( #11533 ), #15445, .T. ) ;
#17504=AXIS2_PLACEMENT_3D ( 'NONE', #32833, #6426, #14248 ) ;
#17513=DIRECTION ( 'NONE',  ( -1.000000000000000000, 0.000000000000000000, -0.000000000000000000 ) ) ;
#17515=EDGE_CURVE ( 'NONE', #19820, #27599, #27925, .T. ) ;
#17516=VERTEX_POINT ( 'NONE', #42348 ) ;
#17517=ORIENTED_EDGE ( 'NONE', *, *, #45336, .T. ) ;
#17521=EDGE_CURVE ( 'NONE', #43442, #27549, #21225, .T. ) ;
#17523=ORIENTED_EDGE ( 'NONE', *, *, #22101, .F. ) ;
#17524=AXIS2_PLACEMENT_3D ( 'NONE', #12472, #1213, #19791 ) ;
#17525=ORIENTED_EDGE ( 'NONE', *, *, #5376, .T. ) ;
#17528=VERTEX_POINT ( 'NONE', #5629 ) ;
#17534=CYLINDRICAL_SURFACE ( 'NONE', #655, 31.99999999999999289 ) ;
#17536=AXIS2_PLACEMENT_3D ( 'NONE', #28394, #9794, #20090 ) ;
#17539=ORIENTED_EDGE ( 'NONE', *, *, #3755, .T. ) ;
#17540=VERTEX_POINT ( 'NONE', #1240 ) ;
#17542=AXIS2_PLACEMENT_3D ( 'NONE', #11879, #22885, #45173 ) ;
#17555=CIRCLE ( 'NONE', #23010, 82.00000000000000000 ) ;
#17556=DIRECTION ( 'NONE',  ( 0.000000000000000000, 0.000000000000000000, 1.000000000000000000 ) ) ;
#17557=ORIENTED_EDGE ( 'NONE', *, *, #29455, .F. ) ;
#17558=ADVANCED_FACE ( 'NONE', ( #1717 ), #23997, .T. ) ;
#17564=CIRCLE ( 'NONE', #32426, 31.99999999999998934 ) ;
#17565=DIRECTION ( 'NONE',  ( -1.000000000000000000, 0.000000000000000000, 0.000000000000000000 ) ) ;
#17567=CARTESIAN_POINT ( 'NONE',  ( 0.000000000000000000, 0.000000000000000000, 0.000000000000000000 ) ) ;
#17569=CARTESIAN_POINT ( 'NONE',  ( 10.00000000000000000, -2.956366410620109519, -75.11725578898472122 ) ) ;
#17577=CIRCLE ( 'NONE', #30104, 77.49900000000000944 ) ;
#17580=DIRECTION ( 'NONE',  ( -1.000000000000000000, 0.000000000000000000, -0.000000000000000000 ) ) ;
#17581=VERTEX_POINT ( 'NONE', #38932 ) ;
#17584=AXIS2_PLACEMENT_3D ( 'NONE', #20712, #2340, #2574 ) ;
#17585=DIRECTION ( 'NONE',  ( -1.000000000000000000, 0.000000000000000000, -0.000000000000000000 ) ) ;
#17587=ORIENTED_EDGE ( 'NONE', *, *, #5885, .F. ) ;
#17592=VERTEX_POINT ( 'NONE', #46758 ) ;
#17593=CARTESIAN_POINT ( 'NONE',  ( 10.00000000000000000, -81.34940948281344220, 10.30890764327356557 ) ) ;
#17594=EDGE_LOOP ( 'NONE', ( #14186, #18180, #44096, #29101 ) ) ;
#17597=CARTESIAN_POINT ( 'NONE',  ( 10.00000000000000000, 0.000000000000000000, 0.000000000000000000 ) ) ;
#17600=LINE ( 'NONE', #32544, #25888 ) ;
#17601=ORIENTED_EDGE ( 'NONE', *, *, #32927, .F. ) ;
#17623=DIRECTION ( 'NONE',  ( -1.000000000000000000, -0.000000000000000000, -0.000000000000000000 ) ) ;
#17625=LINE ( 'NONE', #28879, #11963 ) ;
#17626=CARTESIAN_POINT ( 'NONE',  ( 10.00000000000000000, 74.18225833017889670, 34.94270380257666631 ) ) ;
#17631=ORIENTED_EDGE ( 'NONE', *, *, #32488, .F. ) ;
#17635=EDGE_CURVE ( 'NONE', #23818, #41796, #40803, .T. ) ;
#17637=ORIENTED_EDGE ( 'NONE', *, *, #37577, .T. ) ;
#17641=ORIENTED_EDGE ( 'NONE', *, *, #42083, .F. ) ;
#17646=ORIENTED_EDGE ( 'NONE', *, *, #10643, .T. ) ;
#17650=CIRCLE ( 'NONE', #45025, 77.49900000000000944 ) ;
#17651=CARTESIAN_POINT ( 'NONE',  ( 10.00000000000000000, 0.000000000000000000, 0.000000000000000000 ) ) ;
#17653=ORIENTED_EDGE ( 'NONE', *, *, #34982, .F. ) ;
#17655=ORIENTED_EDGE ( 'NONE', *, *, #28235, .T. ) ;
#17671=CARTESIAN_POINT ( 'NONE',  ( 10.00000000000000000, -36.73666225445845157, -65.58780272294114866 ) ) ;
#17678=ORIENTED_EDGE ( 'NONE', *, *, #27524, .T. ) ;
#17683=EDGE_CURVE ( 'NONE', #34659, #24069, #25418, .T. ) ;
#17685=VECTOR ( 'NONE', #45029, 1000.000000000000000 ) ;
#17693=CYLINDRICAL_SURFACE ( 'NONE', #31886, 77.49899999999999523 ) ;
#17700=ORIENTED_EDGE ( 'NONE', *, *, #24858, .F. ) ;
#17701=EDGE_CURVE ( 'NONE', #2295, #32513, #6833, .T. ) ;
#17702=DIRECTION ( 'NONE',  ( 0.000000000000000000, 0.000000000000000000, 1.000000000000000000 ) ) ;
#17705=VERTEX_POINT ( 'NONE', #3377 ) ;
#17706=EDGE_CURVE ( 'NONE', #44567, #7073, #47682, .T. ) ;
#17708=CARTESIAN_POINT ( 'NONE',  ( 0.000000000000000000, 0.000000000000000000, 0.000000000000000000 ) ) ;
#17711=AXIS2_PLACEMENT_3D ( 'NONE', #17567, #47436, #43758 ) ;
#17725=VERTEX_POINT ( 'NONE', #18321 ) ;
#17732=DIRECTION ( 'NONE',  ( 0.000000000000000000, -0.5877852522924802425, 0.8090169943749422332 ) ) ;
#17734=DIRECTION ( 'NONE',  ( -1.000000000000000000, -0.000000000000000000, -0.000000000000000000 ) ) ;
#17737=DIRECTION ( 'NONE',  ( 0.000000000000000000, 0.000000000000000000, 1.000000000000000000 ) ) ;
#17739=EDGE_CURVE ( 'NONE', #16528, #39957, #21522, .T. ) ;
#17743=DIRECTION ( 'NONE',  ( 0.000000000000000000, -0.6494480483301903195, 0.7604059656000251577 ) ) ;
#17745=AXIS2_PLACEMENT_3D ( 'NONE', #13794, #13536, #3226 ) ;
#17746=EDGE_LOOP ( 'NONE', ( #30413, #43906, #18019, #11588 ) ) ;
#17748=EDGE_CURVE ( 'NONE', #2363, #20770, #7180, .T. ) ;
#17750=DIRECTION ( 'NONE',  ( -1.000000000000000000, 0.000000000000000000, -0.000000000000000000 ) ) ;
#17762=AXIS2_PLACEMENT_3D ( 'NONE', #44246, #37381, #6804 ) ;
#17764=ORIENTED_EDGE ( 'NONE', *, *, #22880, .F. ) ;
#17766=CARTESIAN_POINT ( 'NONE',  ( 5.000000000000000000, 40.65526001592713357, -71.21200624218752750 ) ) ;
#17768=CARTESIAN_POINT ( 'NONE',  ( 10.00000000000000000, 29.01471420065564644, 76.69515212746024702 ) ) ;
#17770=CARTESIAN_POINT ( 'NONE',  ( 10.00000000000000000, 68.67312586194995561, 35.91791733033500122 ) ) ;
#17775=CARTESIAN_POINT ( 'NONE',  ( 0.000000000000000000, 78.73519480814955784, 22.90783923731657268 ) ) ;
#17777=CARTESIAN_POINT ( 'NONE',  ( 0.000000000000000000, 44.88180994100468268, -63.18004540532978552 ) ) ;
#17783=ADVANCED_FACE ( 'NONE', ( #32538 ), #10981, .T. ) ;
#17785=LINE ( 'NONE', #32953, #7657 ) ;
#17786=CARTESIAN_POINT ( 'NONE',  ( 0.000000000000000000, 0.000000000000000000, 0.000000000000000000 ) ) ;
#17789=EDGE_CURVE ( 'NONE', #40588, #17873, #27528, .T. ) ;
#17791=DIRECTION ( 'NONE',  ( -1.000000000000000000, 0.000000000000000000, -0.000000000000000000 ) ) ;
#17812=VERTEX_POINT ( 'NONE', #26640 ) ;
#17819=EDGE_CURVE ( 'NONE', #15509, #8725, #3258, .T. ) ;
#17820=LINE ( 'NONE', #39872, #35092 ) ;
#17821=ADVANCED_FACE ( 'NONE', ( #4383 ), #14897, .T. ) ;
#17823=ORIENTED_EDGE ( 'NONE', *, *, #23938, .T. ) ;
#17824=VERTEX_POINT ( 'NONE', #7788 ) ;
#17827=ADVANCED_FACE ( 'NONE', ( #45473 ), #11957, .T. ) ;
#17832=DIRECTION ( 'NONE',  ( -1.000000000000000000, 0.000000000000000000, 0.000000000000000000 ) ) ;
#17855=EDGE_CURVE ( 'NONE', #43648, #11145, #22837, .T. ) ;
#17857=CARTESIAN_POINT ( 'NONE',  ( 0.000000000000000000, -56.15606465355001120, 59.75363087400055662 ) ) ;
#17861=AXIS2_PLACEMENT_3D ( 'NONE', #7020, #25620, #17556 ) ;
#17865=VERTEX_POINT ( 'NONE', #41103 ) ;
#17873=VERTEX_POINT ( 'NONE', #7560 ) ;
#17891=ORIENTED_EDGE ( 'NONE', *, *, #2976, .T. ) ;
#17893=VERTEX_POINT ( 'NONE', #1658 ) ;
#17908=DIRECTION ( 'NONE',  ( -1.000000000000000000, 0.000000000000000000, 0.000000000000000000 ) ) ;
#17910=ORIENTED_EDGE ( 'NONE', *, *, #3136, .F. ) ;
#17917=LINE ( 'NONE', #28718, #20901 ) ;
#17921=LINE ( 'NONE', #37009, #35481 ) ;
#17923=DIRECTION ( 'NONE',  ( -1.000000000000000000, -0.000000000000000000, -0.000000000000000000 ) ) ;
#17938=ADVANCED_FACE ( 'NONE', ( #9002 ), #20253, .T. ) ;
#17939=EDGE_CURVE ( 'NONE', #35290, #43648, #13445, .T. ) ;
#17945=DIRECTION ( 'NONE',  ( -1.000000000000000000, 0.000000000000000000, 0.000000000000000000 ) ) ;
#17946=ORIENTED_EDGE ( 'NONE', *, *, #34124, .T. ) ;
#17962=DIRECTION ( 'NONE',  ( -1.000000000000000000, 0.000000000000000000, 0.000000000000000000 ) ) ;
#17972=AXIS2_PLACEMENT_3D ( 'NONE', #15681, #45297, #37479 ) ;
#17980=ORIENTED_EDGE ( 'NONE', *, *, #4090, .F. ) ;
#17994=AXIS2_PLACEMENT_3D ( 'NONE', #2100, #17015, #12876 ) ;
#18000=FACE_OUTER_BOUND ( 'NONE', #42819, .T. ) ;
#18010=CARTESIAN_POINT ( 'NONE',  ( 5.000000000000002665, 80.28980883073781172, -16.65972982744850839 ) ) ;
#18013=VERTEX_POINT ( 'NONE', #29470 ) ;
#18014=DIRECTION ( 'NONE',  ( -1.000000000000000000, 0.000000000000000000, 0.000000000000000000 ) ) ;
#18015=ORIENTED_EDGE ( 'NONE', *, *, #19659, .T. ) ;
#18017=CARTESIAN_POINT ( 'NONE',  ( 10.00000000000000000, 54.21277698773752718, -55.38113227695725271 ) ) ;
#18019=ORIENTED_EDGE ( 'NONE', *, *, #4831, .T. ) ;
#18024=AXIS2_PLACEMENT_3D ( 'NONE', #8641, #23575, #4984 ) ;
#18026=EDGE_LOOP ( 'NONE', ( #20723, #16292, #33107, #47275 ) ) ;
#18028=FACE_OUTER_BOUND ( 'NONE', #43256, .T. ) ;
#18043=DIRECTION ( 'NONE',  ( 0.000000000000000000, -0.8526401643540860720, -0.5224985647159590130 ) ) ;
#18050=EDGE_CURVE ( 'NONE', #45066, #30212, #35134, .T. ) ;
#18052=ORIENTED_EDGE ( 'NONE', *, *, #29680, .T. ) ;
#18054=AXIS2_PLACEMENT_3D ( 'NONE', #16051, #31225, #43192 ) ;
#18059=ORIENTED_EDGE ( 'NONE', *, *, #23995, .F. ) ;
#18062=AXIS2_PLACEMENT_3D ( 'NONE', #18802, #44282, #7070 ) ;
#18066=LINE ( 'NONE', #10500, #29403 ) ;
#18070=EDGE_CURVE ( 'NONE', #27291, #47457, #8539, .T. ) ;
#18071=LINE ( 'NONE', #48187, #20755 ) ;
#18072=DIRECTION ( 'NONE',  ( -1.000000000000000000, -0.000000000000000000, 0.000000000000000000 ) ) ;
#18078=VERTEX_POINT ( 'NONE', #6952 ) ;
#18082=ORIENTED_EDGE ( 'NONE', *, *, #14822, .F. ) ;
#18092=CIRCLE ( 'NONE', #3246, 82.00000000000000000 ) ;
#18093=DIRECTION ( 'NONE',  ( 1.000000000000000000, 0.000000000000000000, 0.000000000000000000 ) ) ;
#18095=EDGE_CURVE ( 'NONE', #32527, #30674, #22628, .T. ) ;
#18097=LINE ( 'NONE', #14201, #11324 ) ;
#18101=DIRECTION ( 'NONE',  ( 0.000000000000000000, 0.9238795325112878487, -0.3826834323650874503 ) ) ;
#18105=DIRECTION ( 'NONE',  ( 0.000000000000000000, 0.000000000000000000, 1.000000000000000000 ) ) ;
#18109=ORIENTED_EDGE ( 'NONE', *, *, #31014, .T. ) ;
#18111=EDGE_CURVE ( 'NONE', #46082, #48048, #13399, .T. ) ;
#18114=CARTESIAN_POINT ( 'NONE',  ( 10.00000000000000000, 77.32052557432849937, -5.256550761632002633 ) ) ;
#18116=ADVANCED_FACE ( 'NONE', ( #33611 ), #78, .T. ) ;
#18130=CARTESIAN_POINT ( 'NONE',  ( -10.00000000000000000, 0.000000000000000000, 0.000000000000000000 ) ) ;
#18131=ORIENTED_EDGE ( 'NONE', *, *, #46589, .F. ) ;
#18136=LINE ( 'NONE', #36989, #10546 ) ;
#18143=CARTESIAN_POINT ( 'NONE',  ( 0.000000000000000000, 36.72794159290241822, 65.59268652807223532 ) ) ;
#18150=CYLINDRICAL_SURFACE ( 'NONE', #9092, 31.99999999999999289 ) ;
#18152=EDGE_CURVE ( 'NONE', #22698, #30560, #20285, .T. ) ;
#18156=DIRECTION ( 'NONE',  ( -1.000000000000000000, -0.000000000000000000, 0.000000000000000000 ) ) ;
#18161=CARTESIAN_POINT ( 'NONE',  ( 0.000000000000000000, -77.16300072079641836, -27.74655509720751567 ) ) ;
#18172=ORIENTED_EDGE ( 'NONE', *, *, #12961, .T. ) ;
#18173=AXIS2_PLACEMENT_3D ( 'NONE', #39022, #46616, #6219 ) ;
#18175=ORIENTED_EDGE ( 'NONE', *, *, #34532, .T. ) ;
#18180=ORIENTED_EDGE ( 'NONE', *, *, #37578, .F. ) ;
#18185=CIRCLE ( 'NONE', #26022, 31.99999999999999645 ) ;
#18189=CARTESIAN_POINT ( 'NONE',  ( 0.000000000000000000, -68.67312586195022561, 35.91791733033449674 ) ) ;
#18191=CARTESIAN_POINT ( 'NONE',  ( 5.000000000000000000, 77.16300072079700101, -27.74655509720590629 ) ) ;
#18201=CIRCLE ( 'NONE', #28495, 82.00000000000000000 ) ;
#18214=AXIS2_PLACEMENT_3D ( 'NONE', #588, #19185, #23574 ) ;
#18219=DIRECTION ( 'NONE',  ( -1.000000000000000000, 0.000000000000000000, -0.000000000000000000 ) ) ;
#18222=DIRECTION ( 'NONE',  ( -1.000000000000000000, -0.000000000000000000, -0.000000000000000000 ) ) ;
#18223=FACE_OUTER_BOUND ( 'NONE', #26965, .T. ) ;
#18224=ORIENTED_EDGE ( 'NONE', *, *, #9119, .T. ) ;
#18237=ORIENTED_EDGE ( 'NONE', *, *, #30294, .F. ) ;
#18244=CIRCLE ( 'NONE', #4187, 82.00000000000000000 ) ;
#18247=CARTESIAN_POINT ( 'NONE',  ( 10.00000000000000000, -2.543863470247802905, -81.96053171279903893 ) ) ;
#18248=EDGE_LOOP ( 'NONE', ( #28783, #10128, #9237, #5025 ) ) ;
#18252=ORIENTED_EDGE ( 'NONE', *, *, #16486, .F. ) ;
#18259=DIRECTION ( 'NONE',  ( 0.000000000000000000, -0.5224985647159559043, 0.8526401643540879594 ) ) ;
#18261=CARTESIAN_POINT ( 'NONE',  ( 10.00000000000000000, 75.54627589209970040, -17.28742895386005785 ) ) ;
#18262=DIRECTION ( 'NONE',  ( -1.000000000000000000, 0.000000000000000000, 0.000000000000000000 ) ) ;
#18267=CIRCLE ( 'NONE', #45634, 32.00000000000000000 ) ;
#18270=AXIS2_PLACEMENT_3D ( 'NONE', #36033, #31181, #2498 ) ;
#18281=CARTESIAN_POINT ( 'NONE',  ( 10.00000000000000000, 0.000000000000000000, 0.000000000000000000 ) ) ;
#18288=EDGE_CURVE ( 'NONE', #20918, #38585, #27328, .T. ) ;
#18296=CARTESIAN_POINT ( 'NONE',  ( 10.00000000000000000, -20.41045688087772092, -72.35160999960838524 ) ) ;
#18299=ORIENTED_EDGE ( 'NONE', *, *, #25333, .T. ) ;
#18301=DIRECTION ( 'NONE',  ( -1.000000000000000000, 0.000000000000000000, -0.000000000000000000 ) ) ;
#18305=CIRCLE ( 'NONE', #24578, 31.99999999999999289 ) ;
#18315=VECTOR ( 'NONE', #3410, 1000.000000000000000 ) ;
#18317=DIRECTION ( 'NONE',  ( -1.000000000000000000, -0.000000000000000000, -0.000000000000000000 ) ) ;
#18319=EDGE_LOOP ( 'NONE', ( #7192, #33893, #727, #12973 ) ) ;
#18321=CARTESIAN_POINT ( 'NONE',  ( 10.00000000000000000, 77.49459641780886443, -0.8261519478433788644 ) ) ;
#18324=CARTESIAN_POINT ( 'NONE',  ( 50.00005079999999680, 12.24744871391589207, -2.500000000000000000 ) ) ;
#18332=ORIENTED_EDGE ( 'NONE', *, *, #6940, .T. ) ;
#18334=DIRECTION ( 'NONE',  ( -1.000000000000000000, -0.000000000000000000, -0.000000000000000000 ) ) ;
#18335=DIRECTION ( 'NONE',  ( 0.000000000000000000, -0.2334453638559126909, 0.9723699203976748917 ) ) ;
#18341=ADVANCED_FACE ( 'NONE', ( #20869 ), #31419, .T. ) ;
#18343=FACE_OUTER_BOUND ( 'NONE', #17006, .T. ) ;
#18352=LINE ( 'NONE', #29850, #4260 ) ;
#18355=ORIENTED_EDGE ( 'NONE', *, *, #36782, .T. ) ;
#18371=VERTEX_POINT ( 'NONE', #17411 ) ;
#18374=CARTESIAN_POINT ( 'NONE',  ( 10.00000000000000000, -11.30684508768395524, 76.66974797899831628 ) ) ;
#18375=AXIS2_PLACEMENT_3D ( 'NONE', #41473, #16012, #7925 ) ;
#18376=DIRECTION ( 'NONE',  ( 0.000000000000000000, 0.000000000000000000, -1.000000000000000000 ) ) ;
#18377=VERTEX_POINT ( 'NONE', #47051 ) ;
#18378=ORIENTED_EDGE ( 'NONE', *, *, #39852, .F. ) ;
#18380=CARTESIAN_POINT ( 'NONE',  ( 10.00000000000000000, -68.67312586194971402, -35.91791733033549860 ) ) ;
#18381=EDGE_CURVE ( 'NONE', #8188, #14587, #32368, .T. ) ;
#18382=ORIENTED_EDGE ( 'NONE', *, *, #40876, .T. ) ;
#18384=DIRECTION ( 'NONE',  ( -1.000000000000000000, 0.000000000000000000, 0.000000000000000000 ) ) ;
#18398=CARTESIAN_POINT ( 'NONE',  ( 10.00000000000000000, -68.67312586195023982, 35.91791733033450384 ) ) ;
#18399=VERTEX_POINT ( 'NONE', #13281 ) ;
#18401=AXIS2_PLACEMENT_3D ( 'NONE', #13355, #13591, #43211 ) ;
#18404=VERTEX_POINT ( 'NONE', #28444 ) ;
#18406=AXIS2_PLACEMENT_3D ( 'NONE', #23877, #12621, #8941 ) ;
#18413=FACE_OUTER_BOUND ( 'NONE', #42912, .T. ) ;
#18417=EDGE_CURVE ( 'NONE', #40145, #4970, #40648, .T. ) ;
#18419=EDGE_CURVE ( 'NONE', #43648, #28726, #46817, .T. ) ;
#18420=CARTESIAN_POINT ( 'NONE',  ( 5.000000000000000000, 60.67117009219216328, -55.16347631942977614 ) ) ;
#18421=DIRECTION ( 'NONE',  ( 0.000000000000000000, -0.9969173337331287410, 0.07845909572783489605 ) ) ;
#18423=CARTESIAN_POINT ( 'NONE',  ( 5.000000000000000000, 63.97538442413426907, 51.29473840253247374 ) ) ;
#18426=VERTEX_POINT ( 'NONE', #42669 ) ;
#18430=ORIENTED_EDGE ( 'NONE', *, *, #11888, .T. ) ;
#18433=CIRCLE ( 'NONE', #31746, 31.99999999999999289 ) ;
#18434=VERTEX_POINT ( 'NONE', #13769 ) ;
#18438=ORIENTED_EDGE ( 'NONE', *, *, #10539, .F. ) ;
#18442=ORIENTED_EDGE ( 'NONE', *, *, #33929, .T. ) ;
#18448=FACE_OUTER_BOUND ( 'NONE', #16121, .T. ) ;
#18454=ORIENTED_EDGE ( 'NONE', *, *, #27883, .F. ) ;
#18458=DIRECTION ( 'NONE',  ( -1.000000000000000000, -0.000000000000000000, 0.000000000000000000 ) ) ;
#18462=DIRECTION ( 'NONE',  ( -1.000000000000000000, -0.000000000000000000, 0.000000000000000000 ) ) ;
#18463=EDGE_CURVE ( 'NONE', #29434, #21969, #21890, .T. ) ;
#18475=DIRECTION ( 'NONE',  ( 0.000000000000000000, 0.000000000000000000, 1.000000000000000000 ) ) ;
#18477=EDGE_CURVE ( 'NONE', #17581, #38891, #24992, .T. ) ;
#18478=ORIENTED_EDGE ( 'NONE', *, *, #21819, .T. ) ;
#18479=DIRECTION ( 'NONE',  ( 0.000000000000000000, 0.000000000000000000, -1.000000000000000000 ) ) ;
#18482=CARTESIAN_POINT ( 'NONE',  ( 10.00000000000000000, 0.000000000000000000, 0.000000000000000000 ) ) ;
#18490=VERTEX_POINT ( 'NONE', #6658 ) ;
#18502=DIRECTION ( 'NONE',  ( -1.000000000000000000, -0.000000000000000000, -0.000000000000000000 ) ) ;
#18503=VERTEX_POINT ( 'NONE', #44574 ) ;
#18508=DIRECTION ( 'NONE',  ( -1.000000000000000000, -0.000000000000000000, 0.000000000000000000 ) ) ;
#18509=DIRECTION ( 'NONE',  ( -1.000000000000000000, 0.000000000000000000, 0.000000000000000000 ) ) ;
#18520=AXIS2_PLACEMENT_3D ( 'NONE', #42751, #27569, #16552 ) ;
#18524=LINE ( 'NONE', #11666, #42193 ) ;
#18526=ORIENTED_EDGE ( 'NONE', *, *, #27905, .T. ) ;
#18530=LINE ( 'NONE', #37126, #42900 ) ;
#18534=DIRECTION ( 'NONE',  ( -1.000000000000000000, 0.000000000000000000, 0.000000000000000000 ) ) ;
#18537=EDGE_CURVE ( 'NONE', #37110, #30509, #39867, .T. ) ;
#18539=DIRECTION ( 'NONE',  ( 0.000000000000000000, 0.000000000000000000, 1.000000000000000000 ) ) ;
#18540=DIRECTION ( 'NONE',  ( 0.000000000000000000, 0.000000000000000000, 1.000000000000000000 ) ) ;
#18541=AXIS2_PLACEMENT_3D ( 'NONE', #3902, #47704, #40620 ) ;
#18543=( LENGTH_UNIT ( ) NAMED_UNIT ( * ) SI_UNIT ( .MILLI., .METRE. ) );
#18546=VERTEX_POINT ( 'NONE', #7376 ) ;
#18548=EDGE_LOOP ( 'NONE', ( #38194, #30790, #22791, #8917 ) ) ;
#18549=ORIENTED_EDGE ( 'NONE', *, *, #31038, .F. ) ;
#18555=ORIENTED_EDGE ( 'NONE', *, *, #43543, .T. ) ;
#18557=ORIENTED_EDGE ( 'NONE', *, *, #31488, .F. ) ;
#18560=EDGE_CURVE ( 'NONE', #29434, #10009, #3203, .T. ) ;
#18563=DIRECTION ( 'NONE',  ( 0.000000000000000000, 0.8090169943749446757, 0.5877852522924769119 ) ) ;
#18571=DIRECTION ( 'NONE',  ( 0.000000000000000000, -0.9510565162951566398, 0.3090169943749381809 ) ) ;
#18588=DIRECTION ( 'NONE',  ( -1.000000000000000000, -0.000000000000000000, 0.000000000000000000 ) ) ;
#18599=CARTESIAN_POINT ( 'NONE',  ( 10.00000000000000000, -2.946379043145784582, -75.11764819372150725 ) ) ;
#18607=ORIENTED_EDGE ( 'NONE', *, *, #45144, .T. ) ;
#18608=EDGE_CURVE ( 'NONE', #43090, #47670, #32811, .T. ) ;
#18610=VERTEX_POINT ( 'NONE', #47998 ) ;
#18612=ORIENTED_EDGE ( 'NONE', *, *, #47959, .F. ) ;
#18615=CARTESIAN_POINT ( 'NONE',  ( 0.000000000000000000, 63.18004540533027580, 44.88180994100400056 ) ) ;
#18616=EDGE_CURVE ( 'NONE', #31274, #10549, #38320, .T. ) ;
#18617=CARTESIAN_POINT ( 'NONE',  ( 10.00000000000000000, -75.11764819372145041, 29.05362095685286761 ) ) ;
#18618=EDGE_LOOP ( 'NONE', ( #12911, #38621, #18252, #14035 ) ) ;
#18619=ADVANCED_FACE ( 'NONE', ( #41887 ), #16182, .T. ) ;
#18626=CYLINDRICAL_SURFACE ( 'NONE', #2076, 31.99999999999999289 ) ;
#18635=DIRECTION ( 'NONE',  ( -1.000000000000000000, 0.000000000000000000, -0.000000000000000000 ) ) ;
#18640=DIRECTION ( 'NONE',  ( -1.000000000000000000, -0.000000000000000000, -0.000000000000000000 ) ) ;
#18641=AXIS2_PLACEMENT_3D ( 'NONE', #38022, #33845, #319 ) ;
#18653=DIRECTION ( 'NONE',  ( 0.000000000000000000, -0.8910065241883627918, -0.4539904997395567965 ) ) ;
#18654=ORIENTED_EDGE ( 'NONE', *, *, #9077, .T. ) ;
#18657=CARTESIAN_POINT ( 'NONE',  ( 0.000000000000000000, 74.65491531819118620, -8.830959090342659579 ) ) ;
#18659=CARTESIAN_POINT ( 'NONE',  ( 5.000000000000000000, 56.15606465355042332, -59.75363087400017292 ) ) ;
#18665=ADVANCED_FACE ( 'NONE', ( #743 ), #984, .T. ) ;
#18666=DIRECTION ( 'NONE',  ( 0.000000000000000000, -0.9510565162951566398, 0.3090169943749381809 ) ) ;
#18670=CIRCLE ( 'NONE', #42936, 82.00000000000000000 ) ;
#18672=ADVANCED_FACE ( 'NONE', ( #4444 ), #34038, .T. ) ;
#18679=DIRECTION ( 'NONE',  ( 0.000000000000000000, 0.000000000000000000, 1.000000000000000000 ) ) ;
#18680=DIRECTION ( 'NONE',  ( 0.000000000000000000, 0.000000000000000000, 1.000000000000000000 ) ) ;
#18683=DIRECTION ( 'NONE',  ( 0.000000000000000000, -0.3090169943749548342, 0.9510565162951510887 ) ) ;
#18694=PLANE ( 'NONE',  #41487 ) ;
#18696=CARTESIAN_POINT ( 'NONE',  ( 0.000000000000000000, 0.000000000000000000, 0.000000000000000000 ) ) ;
#18698=VECTOR ( 'NONE', #42771, 1000.000000000000000 ) ;
#18701=DIRECTION ( 'NONE',  ( 0.000000000000000000, 0.000000000000000000, 1.000000000000000000 ) ) ;
#18707=CARTESIAN_POINT ( 'NONE',  ( 5.000000000000002665, -8.966570791700153364, -81.50828551894237251 ) ) ;
#18713=DIRECTION ( 'NONE',  ( -1.000000000000000000, 0.000000000000000000, -0.000000000000000000 ) ) ;
#18714=ORIENTED_EDGE ( 'NONE', *, *, #29918, .T. ) ;
#18717=CARTESIAN_POINT ( 'NONE',  ( 10.00000000000000000, 75.11764819372142199, 2.946379043147685728 ) ) ;
#18721=EDGE_CURVE ( 'NONE', #47783, #27549, #19108, .T. ) ;
#18725=DIRECTION ( 'NONE',  ( -1.000000000000000000, -0.000000000000000000, 0.000000000000000000 ) ) ;
#18727=ORIENTED_EDGE ( 'NONE', *, *, #11828, .T. ) ;
#18729=ORIENTED_EDGE ( 'NONE', *, *, #12520, .F. ) ;
#18732=DIRECTION ( 'NONE',  ( -1.000000000000000000, -0.000000000000000000, 0.000000000000000000 ) ) ;
#18737=AXIS2_PLACEMENT_3D ( 'NONE', #23275, #4668, #30384 ) ;
#18739=EDGE_LOOP ( 'NONE', ( #31101, #16556, #38208, #17980 ) ) ;
#18741=LINE ( 'NONE', #6783, #19384 ) ;
#18744=DIRECTION ( 'NONE',  ( -1.000000000000000000, -0.000000000000000000, 0.000000000000000000 ) ) ;
#18748=CARTESIAN_POINT ( 'NONE',  ( 5.000000000000000000, 74.74816331893430288, 33.71516098798768013 ) ) ;
#18752=ORIENTED_EDGE ( 'NONE', *, *, #8716, .T. ) ;
#18763=AXIS2_PLACEMENT_3D ( 'NONE', #45902, #31460, #20413 ) ;
#18770=ORIENTED_EDGE ( 'NONE', *, *, #8252, .F. ) ;
#18772=CIRCLE ( 'NONE', #3935, 31.99999999999999289 ) ;
#18780=DIRECTION ( 'NONE',  ( -1.000000000000000000, 0.000000000000000000, 0.000000000000000000 ) ) ;
#18782=ORIENTED_EDGE ( 'NONE', *, *, #39121, .F. ) ;
#18790=LINE ( 'NONE', #30074, #48126 ) ;
#18802=CARTESIAN_POINT ( 'NONE',  ( 10.00000000000000000, -68.27212725128298132, 31.46837873494953541 ) ) ;
#18803=ORIENTED_EDGE ( 'NONE', *, *, #35205, .T. ) ;
#18810=DIRECTION ( 'NONE',  ( 0.000000000000000000, 0.000000000000000000, 1.000000000000000000 ) ) ;
#18813=DIRECTION ( 'NONE',  ( -1.000000000000000000, 0.000000000000000000, 0.000000000000000000 ) ) ;
#18816=DIRECTION ( 'NONE',  ( 0.000000000000000000, -0.9238795325112906243, 0.3826834323650804559 ) ) ;
#18817=EDGE_CURVE ( 'NONE', #43544, #46765, #17234, .T. ) ;
#18842=ORIENTED_EDGE ( 'NONE', *, *, #11556, .F. ) ;
#18846=ORIENTED_EDGE ( 'NONE', *, *, #36061, .F. ) ;
#18849=ORIENTED_EDGE ( 'NONE', *, *, #41198, .T. ) ;
#18850=CARTESIAN_POINT ( 'NONE',  ( 0.000000000000000000, 31.46837873494978055, 68.27212725128286763 ) ) ;
#18855=ORIENTED_EDGE ( 'NONE', *, *, #17939, .F. ) ;
#18864=FACE_OUTER_BOUND ( 'NONE', #5283, .T. ) ;
#18866=AXIS2_PLACEMENT_3D ( 'NONE', #45723, #30799, #6532 ) ;
#18879=AXIS2_PLACEMENT_3D ( 'NONE', #10567, #32585, #21801 ) ;
#18883=CARTESIAN_POINT ( 'NONE',  ( 10.00000000000000000, 71.27951684758069462, -30.41916302227035729 ) ) ;
#18886=ORIENTED_EDGE ( 'NONE', *, *, #21130, .T. ) ;
#18887=EDGE_CURVE ( 'NONE', #16528, #24990, #35210, .T. ) ;
#18893=DIRECTION ( 'NONE',  ( 1.000000000000000000, -0.000000000000000000, -0.000000000000000000 ) ) ;
#18895=CIRCLE ( 'NONE', #38481, 31.99999999999999645 ) ;
#18898=CARTESIAN_POINT ( 'NONE',  ( 0.000000000000000000, -31.46837873494930093, -68.27212725128309501 ) ) ;
#18900=AXIS2_PLACEMENT_3D ( 'NONE', #27087, #30281, #1379 ) ;
#18901=EDGE_CURVE ( 'NONE', #30560, #10624, #12993, .T. ) ;
#18904=DIRECTION ( 'NONE',  ( -1.000000000000000000, -0.000000000000000000, -0.000000000000000000 ) ) ;
#18906=AXIS2_PLACEMENT_3D ( 'NONE', #39662, #13699, #19289 ) ;
#18908=EDGE_CURVE ( 'NONE', #34659, #37280, #9414, .T. ) ;
#18909=ORIENTED_EDGE ( 'NONE', *, *, #19388, .T. ) ;
#18912=CARTESIAN_POINT ( 'NONE',  ( 10.00000000000000000, -12.93880638057369659, 76.41127070299266677 ) ) ;
#18916=DIRECTION ( 'NONE',  ( -1.000000000000000000, -0.000000000000000000, 0.000000000000000000 ) ) ;
#18918=ORIENTED_EDGE ( 'NONE', *, *, #38332, .F. ) ;
#18919=CARTESIAN_POINT ( 'NONE',  ( 0.000000000000000000, 59.75363087400153006, -56.15606465354897381 ) ) ;
#18921=CARTESIAN_POINT ( 'NONE',  ( 10.00000000000000000, -5.256550761632340141, -77.32052557432847095 ) ) ;
#18923=EDGE_LOOP ( 'NONE', ( #34825, #29503, #28277, #34018 ) ) ;
#18928=DIRECTION ( 'NONE',  ( -1.000000000000000000, -0.000000000000000000, -0.000000000000000000 ) ) ;
#18932=DIRECTION ( 'NONE',  ( -1.000000000000000000, -0.000000000000000000, -0.000000000000000000 ) ) ;
#18934=VECTOR ( 'NONE', #47463, 1000.000000000000000 ) ;
#18937=EDGE_CURVE ( 'NONE', #7367, #6719, #32858, .T. ) ;
#18938=AXIS2_PLACEMENT_3D ( 'NONE', #40616, #19063, #45024 ) ;
#18944=EDGE_CURVE ( 'NONE', #6258, #15099, #18772, .T. ) ;
#18945=CARTESIAN_POINT ( 'NONE',  ( 10.00000000000000000, -55.16347631942997509, -60.67117009219195722 ) ) ;
#18950=ORIENTED_EDGE ( 'NONE', *, *, #27463, .T. ) ;
#18953=CYLINDRICAL_SURFACE ( 'NONE', #13265, 32.00000000000000000 ) ;
#18954=AXIS2_PLACEMENT_3D ( 'NONE', #3497, #34072, #41428 ) ;
#18957=VECTOR ( 'NONE', #12113, 1000.000000000000000 ) ;
#18959=DIRECTION ( 'NONE',  ( 0.000000000000000000, 0.000000000000000000, 1.000000000000000000 ) ) ;
#18960=AXIS2_PLACEMENT_3D ( 'NONE', #37172, #3641, #48419 ) ;
#18962=ORIENTED_EDGE ( 'NONE', *, *, #44754, .T. ) ;
#18968=EDGE_LOOP ( 'NONE', ( #30125, #43011, #21645, #42179 ) ) ;
#18973=CIRCLE ( 'NONE', #28386, 31.99999999999998934 ) ;
#18976=DIRECTION ( 'NONE',  ( 0.000000000000000000, 0.000000000000000000, 1.000000000000000000 ) ) ;
#18980=EDGE_CURVE ( 'NONE', #17592, #11314, #5512, .T. ) ;
#18983=CARTESIAN_POINT ( 'NONE',  ( 0.000000000000000000, 73.72996012237460661, -14.67089635893632504 ) ) ;
#18986=EDGE_CURVE ( 'NONE', #17380, #17289, #11763, .T. ) ;
#18992=VERTEX_POINT ( 'NONE', #2668 ) ;
#18996=DIRECTION ( 'NONE',  ( -1.000000000000000000, -0.000000000000000000, -0.000000000000000000 ) ) ;
#19003=CIRCLE ( 'NONE', #47144, 77.49899999999999523 ) ;
#19013=FILL_AREA_STYLE_COLOUR ( '', #28005 ) ;
#19018=AXIS2_PLACEMENT_3D ( 'NONE', #41002, #25320, #48328 ) ;
#19023=DIRECTION ( 'NONE',  ( -1.000000000000000000, 0.000000000000000000, -0.000000000000000000 ) ) ;
#19024=ORIENTED_EDGE ( 'NONE', *, *, #26845, .F. ) ;
#19025=VECTOR ( 'NONE', #9634, 1000.000000000000000 ) ;
#19029=EDGE_CURVE ( 'NONE', #31653, #13885, #37551, .T. ) ;
#19039=AXIS2_PLACEMENT_3D ( 'NONE', #20688, #35854, #35624 ) ;
#19041=AXIS2_PLACEMENT_3D ( 'NONE', #3613, #14876, #7537 ) ;
#19043=DIRECTION ( 'NONE',  ( -1.000000000000000000, -0.000000000000000000, 0.000000000000000000 ) ) ;
#19048=DIRECTION ( 'NONE',  ( 1.000000000000000000, -0.000000000000000000, 0.000000000000000000 ) ) ;
#19052=ORIENTED_EDGE ( 'NONE', *, *, #44340, .F. ) ;
#19054=AXIS2_PLACEMENT_3D ( 'NONE', #24015, #34521, #20318 ) ;
#19057=VECTOR ( 'NONE', #28889, 1000.000000000000000 ) ;
#19058=CARTESIAN_POINT ( 'NONE',  ( 10.00000000000000000, -65.64334221924939072, 41.19522573413710376 ) ) ;
#19060=LINE ( 'NONE', #29365, #32924 ) ;
#19062=ORIENTED_EDGE ( 'NONE', *, *, #13995, .T. ) ;
#19063=DIRECTION ( 'NONE',  ( 1.000000000000000000, 0.000000000000000000, 0.000000000000000000 ) ) ;
#19067=EDGE_CURVE ( 'NONE', #38490, #16837, #28978, .T. ) ;
#19075=ADVANCED_FACE ( 'NONE', ( #462 ), #4614, .T. ) ;
#19076=ORIENTED_EDGE ( 'NONE', *, *, #48196, .F. ) ;
#19078=CARTESIAN_POINT ( 'NONE',  ( 0.000000000000000000, 0.000000000000000000, 0.000000000000000000 ) ) ;
#19081=DIRECTION ( 'NONE',  ( 0.000000000000000000, 0.000000000000000000, 1.000000000000000000 ) ) ;
#19085=AXIS2_PLACEMENT_3D ( 'NONE', #22215, #3608, #18540 ) ;
#19087=DIRECTION ( 'NONE',  ( -1.000000000000000000, 0.000000000000000000, 0.000000000000000000 ) ) ;
#19095=EDGE_CURVE ( 'NONE', #27309, #17444, #37659, .T. ) ;
#19104=EDGE_LOOP ( 'NONE', ( #14058, #25948, #24150, #41979 ) ) ;
#19108=LINE ( 'NONE', #521, #1601 ) ;
#19111=ORIENTED_EDGE ( 'NONE', *, *, #41387, .F. ) ;
#19117=DIRECTION ( 'NONE',  ( 0.000000000000000000, 0.3090169943749482839, -0.9510565162951533091 ) ) ;
#19118=ORIENTED_EDGE ( 'NONE', *, *, #34856, .F. ) ;
#19121=CARTESIAN_POINT ( 'NONE',  ( 10.00000000000000000, 0.000000000000000000, 0.000000000000000000 ) ) ;
#19123=CARTESIAN_POINT ( 'NONE',  ( 10.00000000000000000, -62.50884508063453637, 41.76106447765467777 ) ) ;
#19125=DIRECTION ( 'NONE',  ( -1.000000000000000000, 0.000000000000000000, -0.000000000000000000 ) ) ;
#19127=FACE_OUTER_BOUND ( 'NONE', #44221, .T. ) ;
#19129=VECTOR ( 'NONE', #13133, 1000.000000000000000 ) ;
#19131=ADVANCED_FACE ( 'NONE', ( #26168 ), #8288, .T. ) ;
#19137=DIRECTION ( 'NONE',  ( 0.000000000000000000, 0.000000000000000000, 1.000000000000000000 ) ) ;
#19143=ORIENTED_EDGE ( 'NONE', *, *, #8142, .T. ) ;
#19152=CARTESIAN_POINT ( 'NONE',  ( -10.00000000000000000, 0.000000000000000000, 0.000000000000000000 ) ) ;
#19155=CIRCLE ( 'NONE', #16831, 32.00000000000000000 ) ;
#19159=EDGE_LOOP ( 'NONE', ( #3061, #43318, #28494, #29398 ) ) ;
#19162=CIRCLE ( 'NONE', #28545, 32.00000000000000711 ) ;
#19164=CIRCLE ( 'NONE', #46548, 32.00000000000000000 ) ;
#19167=CARTESIAN_POINT ( 'NONE',  ( 10.00000000000000000, 0.000000000000000000, 0.000000000000000000 ) ) ;
#19169=ADVANCED_FACE ( 'NONE', ( #26650 ), #32025, .T. ) ;
#19170=DIRECTION ( 'NONE',  ( 1.000000000000000000, 0.000000000000000000, 0.000000000000000000 ) ) ;
#19175=ORIENTED_EDGE ( 'NONE', *, *, #35931, .F. ) ;
#19178=DIRECTION ( 'NONE',  ( 1.000000000000000000, -0.000000000000000000, 0.000000000000000000 ) ) ;
#19182=CARTESIAN_POINT ( 'NONE',  ( 0.000000000000000000, -28.89263327155693517, -71.91182617369219088 ) ) ;
#19185=DIRECTION ( 'NONE',  ( -1.000000000000000000, -0.000000000000000000, -0.000000000000000000 ) ) ;
#19194=CARTESIAN_POINT ( 'NONE',  ( 0.000000000000000000, -81.50828551894234408, 8.966570791700407383 ) ) ;
#19198=ORIENTED_EDGE ( 'NONE', *, *, #25526, .T. ) ;
#19203=CARTESIAN_POINT ( 'NONE',  ( 10.00000000000000000, 75.11764819372149304, -2.946379043146603482 ) ) ;
#19204=ORIENTED_EDGE ( 'NONE', *, *, #23210, .F. ) ;
#19209=VERTEX_POINT ( 'NONE', #43029 ) ;
#19214=ADVANCED_FACE ( 'NONE', ( #5838 ), #9251, .T. ) ;
#19215=CIRCLE ( 'NONE', #5153, 31.99999999999999289 ) ;
#19218=CARTESIAN_POINT ( 'NONE',  ( 10.00000000000000000, -64.81221759200380461, 50.23322058963325532 ) ) ;
#19223=EDGE_LOOP ( 'NONE', ( #23189, #13207, #14330, #12191 ) ) ;
#19224=VERTEX_POINT ( 'NONE', #39355 ) ;
#19229=EDGE_LOOP ( 'NONE', ( #20557, #28818, #25432, #19744 ) ) ;
#19232=ORIENTED_EDGE ( 'NONE', *, *, #46248, .F. ) ;
#19233=DIRECTION ( 'NONE',  ( 0.000000000000000000, -0.8526401643540861830, -0.5224985647159590130 ) ) ;
#19235=EDGE_CURVE ( 'NONE', #46809, #37478, #29793, .T. ) ;
#19238=CARTESIAN_POINT ( 'NONE',  ( 10.00000000000000000, 0.000000000000000000, 0.000000000000000000 ) ) ;
#19245=DIRECTION ( 'NONE',  ( 0.000000000000000000, 0.000000000000000000, 1.000000000000000000 ) ) ;
#19246=ORIENTED_EDGE ( 'NONE', *, *, #12362, .F. ) ;
#19250=DIRECTION ( 'NONE',  ( -1.000000000000000000, 0.000000000000000000, -0.000000000000000000 ) ) ;
#19256=DIRECTION ( 'NONE',  ( 0.000000000000000000, 0.000000000000000000, 1.000000000000000000 ) ) ;
#19258=CARTESIAN_POINT ( 'NONE',  ( 10.00000000000000000, -55.19960302592104284, 51.03279382321070301 ) ) ;
#19260=CARTESIAN_POINT ( 'NONE',  ( 10.00000000000000000, -77.32052557432837148, -5.256550761633697277 ) ) ;
#19263=ORIENTED_EDGE ( 'NONE', *, *, #12488, .F. ) ;
#19269=EDGE_CURVE ( 'NONE', #36021, #43246, #14910, .T. ) ;
#19271=ADVANCED_FACE ( 'NONE', ( #1186 ), #9726, .T. ) ;
#19272=DIRECTION ( 'NONE',  ( -1.000000000000000000, -0.000000000000000000, 0.000000000000000000 ) ) ;
#19275=ORIENTED_EDGE ( 'NONE', *, *, #25170, .F. ) ;
#19278=CARTESIAN_POINT ( 'NONE',  ( 10.00000000000000000, 0.000000000000000000, 0.000000000000000000 ) ) ;
#19280=DIRECTION ( 'NONE',  ( 0.000000000000000000, 0.000000000000000000, 1.000000000000000000 ) ) ;
#19281=ORIENTED_EDGE ( 'NONE', *, *, #21673, .T. ) ;
#19288=EDGE_CURVE ( 'NONE', #38732, #14493, #38647, .T. ) ;
#19289=DIRECTION ( 'NONE',  ( 0.000000000000000000, 0.000000000000000000, 1.000000000000000000 ) ) ;
#19290=EDGE_CURVE ( 'NONE', #38922, #21614, #33656, .T. ) ;
#19297=ORIENTED_EDGE ( 'NONE', *, *, #6303, .F. ) ;
#19300=CARTESIAN_POINT ( 'NONE',  ( 0.000000000000000000, 20.40083707022987625, -72.35432306680462489 ) ) ;
#19302=CIRCLE ( 'NONE', #24803, 82.00000000000000000 ) ;
#19324=ORIENTED_EDGE ( 'NONE', *, *, #33982, .F. ) ;
#19334=EDGE_CURVE ( 'NONE', #43536, #48063, #10708, .T. ) ;
#19336=CIRCLE ( 'NONE', #29515, 82.00000000000000000 ) ;
#19338=CARTESIAN_POINT ( 'NONE',  ( 0.000000000000000000, 44.88180994100376608, 63.18004540533043922 ) ) ;
#19349=DIRECTION ( 'NONE',  ( 0.000000000000000000, 0.000000000000000000, 1.000000000000000000 ) ) ;
#19350=ORIENTED_EDGE ( 'NONE', *, *, #26845, .T. ) ;
#19366=DIRECTION ( 'NONE',  ( 0.000000000000000000, 0.8910065241883655673, 0.4539904997395510233 ) ) ;
#19372=CARTESIAN_POINT ( 'NONE',  ( 10.00000000000000000, 0.000000000000000000, 0.000000000000000000 ) ) ;
#19377=ORIENTED_EDGE ( 'NONE', *, *, #22969, .T. ) ;
#19383=ORIENTED_EDGE ( 'NONE', *, *, #27883, .T. ) ;
#19384=VECTOR ( 'NONE', #48132, 1000.000000000000000 ) ;
#19388=EDGE_CURVE ( 'NONE', #32236, #28820, #39863, .T. ) ;
#19395=CIRCLE ( 'NONE', #9277, 77.49899999999999523 ) ;
#19396=FACE_OUTER_BOUND ( 'NONE', #28012, .T. ) ;
#19402=DIRECTION ( 'NONE',  ( -1.000000000000000000, 0.000000000000000000, -0.000000000000000000 ) ) ;
#19407=CARTESIAN_POINT ( 'NONE',  ( -10.00000000000000000, 0.000000000000000000, 0.000000000000000000 ) ) ;
#19409=DIRECTION ( 'NONE',  ( -1.000000000000000000, 0.000000000000000000, 0.000000000000000000 ) ) ;
#19414=FACE_OUTER_BOUND ( 'NONE', #41865, .T. ) ;
#19418=DIRECTION ( 'NONE',  ( 0.000000000000000000, 0.000000000000000000, -1.000000000000000000 ) ) ;
#19433=ADVANCED_FACE ( 'NONE', ( #869 ), #7258, .T. ) ;
#19435=ORIENTED_EDGE ( 'NONE', *, *, #40821, .T. ) ;
#19436=FACE_OUTER_BOUND ( 'NONE', #43052, .T. ) ;
#19443=DIRECTION ( 'NONE',  ( 1.000000000000000000, 0.000000000000000000, -0.000000000000000000 ) ) ;
#19447=ORIENTED_EDGE ( 'NONE', *, *, #9998, .F. ) ;
#19448=DIRECTION ( 'NONE',  ( 0.000000000000000000, -0.5224985647159560154, 0.8526401643540879594 ) ) ;
#19450=EDGE_CURVE ( 'NONE', #4251, #2189, #18524, .T. ) ;
#19454=CARTESIAN_POINT ( 'NONE',  ( 10.00000000000000000, -3.894527615417343824, -81.90746397400393164 ) ) ;
#19459=DIRECTION ( 'NONE',  ( 0.000000000000000000, -1.000000000000000000, -1.040834085586084730E-14 ) ) ;
#19463=VECTOR ( 'NONE', #37294, 1000.000000000000000 ) ;
#19464=FACE_OUTER_BOUND ( 'NONE', #224, .T. ) ;
#19466=VERTEX_POINT ( 'NONE', #26595 ) ;
#19467=EDGE_CURVE ( 'NONE', #270, #41584, #26106, .T. ) ;
#19472=DIRECTION ( 'NONE',  ( -1.000000000000000000, 0.000000000000000000, 0.000000000000000000 ) ) ;
#19475=FACE_OUTER_BOUND ( 'NONE', #45796, .T. ) ;
#19484=ORIENTED_EDGE ( 'NONE', *, *, #13965, .F. ) ;
#19485=EDGE_CURVE ( 'NONE', #43495, #41616, #150, .T. ) ;
#19486=ORIENTED_EDGE ( 'NONE', *, *, #43709, .F. ) ;
#19493=EDGE_LOOP ( 'NONE', ( #13799, #38708, #35174, #1098 ) ) ;
#19497=EDGE_LOOP ( 'NONE', ( #43426, #1354, #32217, #43666 ) ) ;
#19511=CARTESIAN_POINT ( 'NONE',  ( 0.000000000000000000, -23.16143007188480496, 73.95703589263965227 ) ) ;
#19514=CARTESIAN_POINT ( 'NONE',  ( 10.00000000000000000, 20.41045688087930898, -72.35160999960793049 ) ) ;
#19515=CIRCLE ( 'NONE', #35952, 31.99999999999999645 ) ;
#19522=DIRECTION ( 'NONE',  ( -1.000000000000000000, 0.000000000000000000, 0.000000000000000000 ) ) ;
#19523=CARTESIAN_POINT ( 'NONE',  ( 10.00000000000000000, -55.38113227695743745, -54.21277698773734244 ) ) ;
#19524=FACE_OUTER_BOUND ( 'NONE', #38001, .T. ) ;
#19529=CARTESIAN_POINT ( 'NONE',  ( 10.00000000000000000, 72.35160999960817207, 20.41045688087850607 ) ) ;
#19540=ORIENTED_EDGE ( 'NONE', *, *, #19572, .T. ) ;
#19541=DIRECTION ( 'NONE',  ( -1.000000000000000000, 0.000000000000000000, -0.000000000000000000 ) ) ;
#19549=CIRCLE ( 'NONE', #43033, 77.49900000000000944 ) ;
#19569=DIRECTION ( 'NONE',  ( -1.000000000000000000, 0.000000000000000000, 0.000000000000000000 ) ) ;
#19572=EDGE_CURVE ( 'NONE', #39870, #12844, #9380, .T. ) ;
#19574=ORIENTED_EDGE ( 'NONE', *, *, #7017, .F. ) ;
#19581=DIRECTION ( 'NONE',  ( 0.000000000000000000, 0.000000000000000000, 1.000000000000000000 ) ) ;
#19583=CARTESIAN_POINT ( 'NONE',  ( -10.00000000000000000, 0.000000000000000000, 0.000000000000000000 ) ) ;
#19584=EDGE_CURVE ( 'NONE', #23235, #6704, #42307, .T. ) ;
#19586=DIRECTION ( 'NONE',  ( 0.000000000000000000, 0.000000000000000000, 1.000000000000000000 ) ) ;
#19592=CYLINDRICAL_SURFACE ( 'NONE', #45854, 31.99999999999999289 ) ;
#19595=AXIS2_PLACEMENT_3D ( 'NONE', #6113, #39878, #46983 ) ;
#19597=CARTESIAN_POINT ( 'NONE',  ( 0.000000000000000000, 41.19522573413731692, 65.64334221924924861 ) ) ;
#19602=AXIS2_PLACEMENT_3D ( 'NONE', #10026, #35970, #13462 ) ;
#19605=ADVANCED_FACE ( 'NONE', ( #42741 ), #34641, .T. ) ;
#19607=EDGE_LOOP ( 'NONE', ( #10919, #46698, #11420, #16987 ) ) ;
#19613=EDGE_CURVE ( 'NONE', #33332, #8066, #21117, .T. ) ;
#19614=DIRECTION ( 'NONE',  ( -1.000000000000000000, -0.000000000000000000, -0.000000000000000000 ) ) ;
#19618=EDGE_CURVE ( 'NONE', #39890, #12529, #48452, .T. ) ;
#19625=EDGE_LOOP ( 'NONE', ( #43119, #40839, #35332, #10371 ) ) ;
#19627=AXIS2_PLACEMENT_3D ( 'NONE', #4377, #31531, #9236 ) ;
#19628=ORIENTED_EDGE ( 'NONE', *, *, #146, .F. ) ;
#19629=AXIS2_PLACEMENT_3D ( 'NONE', #23448, #8290, #15875 ) ;
#19631=DIRECTION ( 'NONE',  ( -1.000000000000000000, -0.000000000000000000, -0.000000000000000000 ) ) ;
#19632=CARTESIAN_POINT ( 'NONE',  ( 10.00000000000000000, -62.20884554313985149, -46.21855187248698371 ) ) ;
#19639=EDGE_LOOP ( 'NONE', ( #16166, #39261, #27858, #10319 ) ) ;
#19641=DIRECTION ( 'NONE',  ( 0.000000000000000000, -0.9723699203976741146, -0.2334453638559159938 ) ) ;
#19644=DIRECTION ( 'NONE',  ( 1.000000000000000000, -0.000000000000000000, -0.000000000000000000 ) ) ;
#19646=CARTESIAN_POINT ( 'NONE',  ( 0.000000000000000000, 0.000000000000000000, -2.500000000000000000 ) ) ;
#19651=CARTESIAN_POINT ( 'NONE',  ( 0.000000000000000000, -46.53671651293991118, 59.03961581697383565 ) ) ;
#19655=CYLINDRICAL_SURFACE ( 'NONE', #12670, 31.99999999999999289 ) ;
#19657=CARTESIAN_POINT ( 'NONE',  ( 0.000000000000000000, 36.73666225445894185, 65.58780272294090707 ) ) ;
#19658=CARTESIAN_POINT ( 'NONE',  ( 10.00000000000000000, 0.000000000000000000, 0.000000000000000000 ) ) ;
#19659=EDGE_CURVE ( 'NONE', #14587, #37445, #36768, .T. ) ;
#19670=DIRECTION ( 'NONE',  ( -1.000000000000000000, -0.000000000000000000, 0.000000000000000000 ) ) ;
#19675=AXIS2_PLACEMENT_3D ( 'NONE', #37902, #15148, #41337 ) ;
#19676=ORIENTED_EDGE ( 'NONE', *, *, #16514, .F. ) ;
#19684=ORIENTED_EDGE ( 'NONE', *, *, #17855, .F. ) ;
#19689=CIRCLE ( 'NONE', #5638, 32.00000000000000000 ) ;
#19693=ORIENTED_EDGE ( 'NONE', *, *, #13450, .F. ) ;
#19694=AXIS2_PLACEMENT_3D ( 'NONE', #31354, #27432, #46267 ) ;
#19698=CARTESIAN_POINT ( 'NONE',  ( 10.00000000000000000, -73.72996012237449293, 14.67089635893687571 ) ) ;
#19704=CARTESIAN_POINT ( 'NONE',  ( 0.000000000000000000, 29.01471420065674423, -76.69515212745984911 ) ) ;
#19706=CARTESIAN_POINT ( 'NONE',  ( 5.000000000000000000, 46.11716303203284184, -67.80270845531839541 ) ) ;
#19708=DIRECTION ( 'NONE',  ( 1.000000000000000000, 0.000000000000000000, -0.000000000000000000 ) ) ;
#19710=CARTESIAN_POINT ( 'NONE',  ( 10.00000000000000000, -51.02545421589363883, 55.20638768913742922 ) ) ;
#19718=CARTESIAN_POINT ( 'NONE',  ( 0.000000000000000000, 0.000000000000000000, 0.000000000000000000 ) ) ;
#19719=DIRECTION ( 'NONE',  ( 0.000000000000000000, -0.2334453638558922628, -0.9723699203976798877 ) ) ;
#19722=ORIENTED_EDGE ( 'NONE', *, *, #45098, .T. ) ;
#19730=CIRCLE ( 'NONE', #6481, 31.99999999999999289 ) ;
#19734=MANIFOLD_SOLID_BREP ( 'Cut-Extrude-Thin1', #25490 ) ;
#19736=AXIS2_PLACEMENT_3D ( 'NONE', #37545, #10650, #11380 ) ;
#19744=ORIENTED_EDGE ( 'NONE', *, *, #38689, .T. ) ;
#19746=ORIENTED_EDGE ( 'NONE', *, *, #19288, .T. ) ;
#19769=EDGE_CURVE ( 'NONE', #3739, #17824, #12540, .T. ) ;
#19770=DIRECTION ( 'NONE',  ( -1.000000000000000000, 0.000000000000000000, 0.000000000000000000 ) ) ;
#19774=CARTESIAN_POINT ( 'NONE',  ( 0.000000000000000000, 46.21855187248628738, 62.20884554314034887 ) ) ;
#19775=DIRECTION ( 'NONE',  ( -1.000000000000000000, -0.000000000000000000, -0.000000000000000000 ) ) ;
#19778=DIRECTION ( 'NONE',  ( -1.000000000000000000, -0.000000000000000000, 0.000000000000000000 ) ) ;
#19780=LINE ( 'NONE', #48270, #2679 ) ;
#19783=CARTESIAN_POINT ( 'NONE',  ( 0.000000000000000000, 46.11716303203284184, -67.80270845531839541 ) ) ;
#19786=DIRECTION ( 'NONE',  ( -1.000000000000000000, 0.000000000000000000, 0.000000000000000000 ) ) ;
#19789=EDGE_LOOP ( 'NONE', ( #37543, #32625, #3926, #3519 ) ) ;
#19790=EDGE_CURVE ( 'NONE', #828, #24345, #47035, .T. ) ;
#19791=DIRECTION ( 'NONE',  ( 0.000000000000000000, 0.000000000000000000, -1.000000000000000000 ) ) ;
#19794=EDGE_CURVE ( 'NONE', #7344, #39808, #27723, .T. ) ;
#19797=ADVANCED_FACE ( 'NONE', ( #24047 ), #1293, .T. ) ;
#19800=CIRCLE ( 'NONE', #33890, 82.00000000000000000 ) ;
#19802=ORIENTED_EDGE ( 'NONE', *, *, #27039, .F. ) ;
#19803=ORIENTED_EDGE ( 'NONE', *, *, #32807, .T. ) ;
#19806=DIRECTION ( 'NONE',  ( 0.000000000000000000, 0.000000000000000000, -1.000000000000000000 ) ) ;
#19808=AXIS2_PLACEMENT_3D ( 'NONE', #12351, #45884, #34122 ) ;
#19820=VERTEX_POINT ( 'NONE', #3439 ) ;
#19824=CARTESIAN_POINT ( 'NONE',  ( 0.000000000000000000, 0.000000000000000000, 0.000000000000000000 ) ) ;
#19827=ORIENTED_EDGE ( 'NONE', *, *, #48180, .F. ) ;
#19830=DIRECTION ( 'NONE',  ( -1.000000000000000000, -0.000000000000000000, -0.000000000000000000 ) ) ;
#19834=DIRECTION ( 'NONE',  ( -1.000000000000000000, 0.000000000000000000, -0.000000000000000000 ) ) ;
#19840=CIRCLE ( 'NONE', #36267, 77.49899999999999523 ) ;
#19841=CARTESIAN_POINT ( 'NONE',  ( 10.00000000000000000, 81.90746397400388901, 3.894527615418187150 ) ) ;
#19846=AXIS2_PLACEMENT_3D ( 'NONE', #11624, #11395, #1076 ) ;
#19851=VERTEX_POINT ( 'NONE', #18374 ) ;
#19855=CIRCLE ( 'NONE', #11277, 31.99999999999999645 ) ;
#19857=CIRCLE ( 'NONE', #47226, 82.00000000000000000 ) ;
#19858=CARTESIAN_POINT ( 'NONE',  ( 5.000000000000000000, 56.15606465354959198, 59.75363087400094741 ) ) ;
#19861=ORIENTED_EDGE ( 'NONE', *, *, #25526, .F. ) ;
#19862=ADVANCED_FACE ( 'NONE', ( #14714 ), #33306, .T. ) ;
#19867=DIRECTION ( 'NONE',  ( -1.000000000000000000, 0.000000000000000000, 0.000000000000000000 ) ) ;
#19868=CARTESIAN_POINT ( 'NONE',  ( 0.000000000000000000, 59.46389618801963195, 49.70050353004911159 ) ) ;
#19874=AXIS2_PLACEMENT_3D ( 'NONE', #44633, #11105, #40974 ) ;
#19878=CARTESIAN_POINT ( 'NONE',  ( 0.000000000000000000, -5.256550761633411284, 77.32052557432838569 ) ) ;
#19880=CARTESIAN_POINT ( 'NONE',  ( 0.000000000000000000, -2.543863470248944214, 81.96053171279901051 ) ) ;
#19881=ADVANCED_FACE ( 'NONE', ( #21074 ), #10068, .T. ) ;
#19886=VERTEX_POINT ( 'NONE', #9827 ) ;
#19888=ORIENTED_EDGE ( 'NONE', *, *, #45625, .T. ) ;
#19893=CIRCLE ( 'NONE', #8854, 82.00000000000000000 ) ;
#19906=DIRECTION ( 'NONE',  ( -1.000000000000000000, 0.000000000000000000, -0.000000000000000000 ) ) ;
#19907=CARTESIAN_POINT ( 'NONE',  ( 10.00000000000000000, -59.46389618801928378, -49.70050353004953791 ) ) ;
#19911=PLANE ( 'NONE',  #36245 ) ;
#19914=ORIENTED_EDGE ( 'NONE', *, *, #30609, .T. ) ;
#19917=ORIENTED_EDGE ( 'NONE', *, *, #35324, .F. ) ;
#19918=ORIENTED_EDGE ( 'NONE', *, *, #11780, .F. ) ;
#19922=ORIENTED_EDGE ( 'NONE', *, *, #23832, .F. ) ;
#19931=EDGE_CURVE ( 'NONE', #29124, #16097, #10220, .T. ) ;
#19935=DIRECTION ( 'NONE',  ( -1.000000000000000000, -0.000000000000000000, -0.000000000000000000 ) ) ;
#19944=PLANE ( 'NONE',  #13960 ) ;
#19945=FACE_OUTER_BOUND ( 'NONE', #4321, .T. ) ;
#19950=ORIENTED_EDGE ( 'NONE', *, *, #30781, .T. ) ;
#19952=ORIENTED_EDGE ( 'NONE', *, *, #7290, .F. ) ;
#19955=DIRECTION ( 'NONE',  ( -1.000000000000000000, 0.000000000000000000, 0.000000000000000000 ) ) ;
#19958=DIRECTION ( 'NONE',  ( -1.000000000000000000, -0.000000000000000000, -0.000000000000000000 ) ) ;
#19965=CARTESIAN_POINT ( 'NONE',  ( 0.000000000000000000, -8.830959090342926032, 74.65491531819115778 ) ) ;
#19977=DIRECTION ( 'NONE',  ( -1.000000000000000000, 0.000000000000000000, 0.000000000000000000 ) ) ;
#19978=DIRECTION ( 'NONE',  ( -1.000000000000000000, -0.000000000000000000, 0.000000000000000000 ) ) ;
#19979=CIRCLE ( 'NONE', #23090, 77.49899999999998101 ) ;
#19985=LINE ( 'NONE', #15594, #3379 ) ;
#19992=ORIENTED_EDGE ( 'NONE', *, *, #8115, .F. ) ;
#20007=EDGE_LOOP ( 'NONE', ( #27679, #672, #38243, #13758 ) ) ;
#20009=AXIS2_PLACEMENT_3D ( 'NONE', #38057, #29978, #15533 ) ;
#20014=CARTESIAN_POINT ( 'NONE',  ( 10.00000000000000000, 0.000000000000000000, 0.000000000000000000 ) ) ;
#20021=ORIENTED_EDGE ( 'NONE', *, *, #29941, .T. ) ;
#20022=ORIENTED_EDGE ( 'NONE', *, *, #4210, .F. ) ;
#20023=DIRECTION ( 'NONE',  ( -1.000000000000000000, -0.000000000000000000, -0.000000000000000000 ) ) ;
#20025=CIRCLE ( 'NONE', #47394, 77.49899999999999523 ) ;
#20034=DIRECTION ( 'NONE',  ( 0.000000000000000000, 0.000000000000000000, 1.000000000000000000 ) ) ;
#20035=DIRECTION ( 'NONE',  ( -1.000000000000000000, -0.000000000000000000, 0.000000000000000000 ) ) ;
#20036=LINE ( 'NONE', #34965, #41994 ) ;
#20039=DIRECTION ( 'NONE',  ( -1.000000000000000000, 0.000000000000000000, -0.000000000000000000 ) ) ;
#20047=ORIENTED_EDGE ( 'NONE', *, *, #14626, .T. ) ;
#20057=ADVANCED_FACE ( 'NONE', ( #15935 ), #27676, .T. ) ;
#20058=CARTESIAN_POINT ( 'NONE',  ( 10.00000000000000000, 2.956366410621684260, -75.11725578898465017 ) ) ;
#20061=VERTEX_POINT ( 'NONE', #23749 ) ;
#20063=VERTEX_POINT ( 'NONE', #41888 ) ;
#20067=ORIENTED_EDGE ( 'NONE', *, *, #29455, .T. ) ;
#20069=FACE_OUTER_BOUND ( 'NONE', #8677, .T. ) ;
#20070=ADVANCED_FACE ( 'NONE', ( #42850 ), #12994, .T. ) ;
#20071=VERTEX_POINT ( 'NONE', #985 ) ;
#20074=VECTOR ( 'NONE', #39129, 1000.000000000000000 ) ;
#20076=CYLINDRICAL_SURFACE ( 'NONE', #45496, 82.00000000000000000 ) ;
#20085=VERTEX_POINT ( 'NONE', #12271 ) ;
#20090=DIRECTION ( 'NONE',  ( 0.000000000000000000, 0.000000000000000000, 1.000000000000000000 ) ) ;
#20091=CARTESIAN_POINT ( 'NONE',  ( 10.00000000000000000, 24.73286445877808148, -73.44644590900034586 ) ) ;
#20096=AXIS2_PLACEMENT_3D ( 'NONE', #1875, #31753, #46898 ) ;
#20097=DIRECTION ( 'NONE',  ( -1.000000000000000000, 0.000000000000000000, -0.000000000000000000 ) ) ;
#20105=DIRECTION ( 'NONE',  ( -1.000000000000000000, 0.000000000000000000, 0.000000000000000000 ) ) ;
#20108=VERTEX_POINT ( 'NONE', #24005 ) ;
#20111=ADVANCED_FACE ( 'NONE', ( #39167 ), #23276, .T. ) ;
#20115=EDGE_CURVE ( 'NONE', #42670, #32991, #28183, .T. ) ;
#20117=ORIENTED_EDGE ( 'NONE', *, *, #44499, .T. ) ;
#20121=CARTESIAN_POINT ( 'NONE',  ( 10.00000000000000000, 75.16055320797059380, -18.89407956138177269 ) ) ;
#20123=DIRECTION ( 'NONE',  ( -1.000000000000000000, -0.000000000000000000, -0.000000000000000000 ) ) ;
#20126=CARTESIAN_POINT ( 'NONE',  ( 0.000000000000000000, 22.90783923731741112, -78.73519480814930205 ) ) ;
#20127=EDGE_LOOP ( 'NONE', ( #37470, #4132, #11360, #31543 ) ) ;
#20128=DIRECTION ( 'NONE',  ( 0.000000000000000000, 0.000000000000000000, -1.000000000000000000 ) ) ;
#20129=EDGE_LOOP ( 'NONE', ( #3875, #21556, #2718, #37041 ) ) ;
#20130=ORIENTED_EDGE ( 'NONE', *, *, #10330, .T. ) ;
#20134=DIRECTION ( 'NONE',  ( -1.000000000000000000, 0.000000000000000000, -0.000000000000000000 ) ) ;
#20141=ORIENTED_EDGE ( 'NONE', *, *, #35820, .T. ) ;
#20151=DIRECTION ( 'NONE',  ( -1.000000000000000000, 0.000000000000000000, 0.000000000000000000 ) ) ;
#20160=EDGE_LOOP ( 'NONE', ( #43747, #30939, #23215, #18382 ) ) ;
#20164=DIRECTION ( 'NONE',  ( 0.000000000000000000, 0.8526401643540897357, 0.5224985647159531288 ) ) ;
#20168=ORIENTED_EDGE ( 'NONE', *, *, #31869, .F. ) ;
#20169=EDGE_CURVE ( 'NONE', #17121, #13194, #32108, .T. ) ;
#20176=ORIENTED_EDGE ( 'NONE', *, *, #18986, .F. ) ;
#20179=CIRCLE ( 'NONE', #31919, 82.00000000000000000 ) ;
#20190=CARTESIAN_POINT ( 'NONE',  ( 10.00000000000000000, 0.000000000000000000, 0.000000000000000000 ) ) ;
#20197=ORIENTED_EDGE ( 'NONE', *, *, #39740, .F. ) ;
#20202=LINE ( 'NONE', #35125, #45462 ) ;
#20204=DIRECTION ( 'NONE',  ( -1.000000000000000000, -0.000000000000000000, 0.000000000000000000 ) ) ;
#20206=DIRECTION ( 'NONE',  ( -1.000000000000000000, 0.000000000000000000, -0.000000000000000000 ) ) ;
#20207=FACE_OUTER_BOUND ( 'NONE', #44034, .T. ) ;
#20209=CARTESIAN_POINT ( 'NONE',  ( 10.00000000000000000, 74.65491531819118620, -8.830959090342659579 ) ) ;
#20214=VECTOR ( 'NONE', #16597, 1000.000000000000000 ) ;
#20218=ADVANCED_FACE ( 'NONE', ( #47470 ), #25180, .T. ) ;
#20222=DIRECTION ( 'NONE',  ( 0.000000000000000000, 0.6494480483301849905, -0.7604059656000299317 ) ) ;
#20224=ORIENTED_EDGE ( 'NONE', *, *, #16635, .T. ) ;
#20225=EDGE_CURVE ( 'NONE', #29124, #10023, #3029, .T. ) ;
#20230=ADVANCED_FACE ( 'NONE', ( #25426 ), #47692, .T. ) ;
#20238=AXIS2_PLACEMENT_3D ( 'NONE', #6823, #17585, #14162 ) ;
#20239=DIRECTION ( 'NONE',  ( 1.000000000000000000, 0.000000000000000000, 0.000000000000000000 ) ) ;
#20240=FACE_OUTER_BOUND ( 'NONE', #12461, .T. ) ;
#20242=AXIS2_PLACEMENT_3D ( 'NONE', #35883, #43717, #32228 ) ;
#20248=EDGE_LOOP ( 'NONE', ( #40894, #26149, #7855, #42592 ) ) ;
#20249=DIRECTION ( 'NONE',  ( 0.000000000000000000, 0.000000000000000000, 1.000000000000000000 ) ) ;
#20253=CYLINDRICAL_SURFACE ( 'NONE', #26728, 31.99999999999999289 ) ;
#20257=DIRECTION ( 'NONE',  ( 0.000000000000000000, 0.07845909572784530439, -0.9969173337331279638 ) ) ;
#20265=ORIENTED_EDGE ( 'NONE', *, *, #17431, .T. ) ;
#20282=ADVANCED_FACE ( 'NONE', ( #40381 ), #28385, .T. ) ;
#20285=CIRCLE ( 'NONE', #14036, 32.00000000000000000 ) ;
#20291=ORIENTED_EDGE ( 'NONE', *, *, #31701, .F. ) ;
#20293=ORIENTED_EDGE ( 'NONE', *, *, #23938, .F. ) ;
#20295=CARTESIAN_POINT ( 'NONE',  ( 0.000000000000000000, 0.000000000000000000, 0.000000000000000000 ) ) ;
#20296=ORIENTED_EDGE ( 'NONE', *, *, #40882, .F. ) ;
#20297=CARTESIAN_POINT ( 'NONE',  ( 10.00000000000000000, 41.76106447765580043, -62.50884508063379741 ) ) ;
#20304=CARTESIAN_POINT ( 'NONE',  ( 10.00000000000000000, -70.52718814184277107, 26.02418014898285037 ) ) ;
#20306=DIRECTION ( 'NONE',  ( -1.000000000000000000, -0.000000000000000000, -0.000000000000000000 ) ) ;
#20308=FACE_OUTER_BOUND ( 'NONE', #48164, .T. ) ;
#20310=AXIS2_PLACEMENT_3D ( 'NONE', #10574, #21812, #33070 ) ;
#20312=DIRECTION ( 'NONE',  ( 0.000000000000000000, 0.7604059656000323741, -0.6494480483301819929 ) ) ;
#20318=DIRECTION ( 'NONE',  ( 0.000000000000000000, 0.000000000000000000, 1.000000000000000000 ) ) ;
#20322=CARTESIAN_POINT ( 'NONE',  ( 0.000000000000000000, -64.81221759200306565, -50.23322058963418613 ) ) ;
#20338=ADVANCED_FACE ( 'NONE', ( #30330 ), #41110, .T. ) ;
#20340=CIRCLE ( 'NONE', #5499, 31.99999999999998934 ) ;
#20350=DIRECTION ( 'NONE',  ( 1.000000000000000000, 0.000000000000000000, 0.000000000000000000 ) ) ;
#20352=PRESENTATION_STYLE_ASSIGNMENT (( #23545 ) ) ;
#20353=EDGE_CURVE ( 'NONE', #42231, #44962, #28249, .T. ) ;
#20355=DIRECTION ( 'NONE',  ( 0.000000000000000000, 0.000000000000000000, 1.000000000000000000 ) ) ;
#20361=DIRECTION ( 'NONE',  ( 0.000000000000000000, 0.000000000000000000, -1.000000000000000000 ) ) ;
#20364=VECTOR ( 'NONE', #1060, 1000.000000000000000 ) ;
#20368=CARTESIAN_POINT ( 'NONE',  ( 5.000000000000000000, 71.21200624218795383, 40.65526001592638039 ) ) ;
#20369=EDGE_LOOP ( 'NONE', ( #7131, #31883, #4083, #19722 ) ) ;
#20371=ADVANCED_FACE ( 'NONE', ( #44516 ), #10993, .T. ) ;
#20374=EDGE_CURVE ( 'NONE', #28683, #16330, #15158, .T. ) ;
#20393=ORIENTED_EDGE ( 'NONE', *, *, #33417, .F. ) ;
#20398=CARTESIAN_POINT ( 'NONE',  ( 5.000000000000002665, -44.99326035066006568, -68.55367621811190304 ) ) ;
#20403=AXIS2_PLACEMENT_3D ( 'NONE', #47407, #6294, #6775 ) ;
#20404=VERTEX_POINT ( 'NONE', #33266 ) ;
#20410=AXIS2_PLACEMENT_3D ( 'NONE', #32308, #24950, #46769 ) ;
#20413=DIRECTION ( 'NONE',  ( 0.000000000000000000, 0.000000000000000000, 1.000000000000000000 ) ) ;
#20418=ORIENTED_EDGE ( 'NONE', *, *, #18477, .T. ) ;
#20426=CARTESIAN_POINT ( 'NONE',  ( 0.000000000000000000, 0.000000000000000000, 0.000000000000000000 ) ) ;
#20429=DIRECTION ( 'NONE',  ( 0.000000000000000000, 0.000000000000000000, 1.000000000000000000 ) ) ;
#20431=CARTESIAN_POINT ( 'NONE',  ( 10.00000000000000000, -73.95703589263958122, -23.16143007188506431 ) ) ;
#20435=CARTESIAN_POINT ( 'NONE',  ( 0.000000000000000000, -16.65972982744991882, 80.28980883073752750 ) ) ;
#20437=ORIENTED_EDGE ( 'NONE', *, *, #1513, .F. ) ;
#20443=ORIENTED_EDGE ( 'NONE', *, *, #22330, .F. ) ;
#20444=VERTEX_POINT ( 'NONE', #5349 ) ;
#20445=DIRECTION ( 'NONE',  ( 0.000000000000000000, 0.000000000000000000, -1.000000000000000000 ) ) ;
#20450=CARTESIAN_POINT ( 'NONE',  ( 10.00000000000000000, 12.93880638057314059, 76.41127070299278046 ) ) ;
#20454=DIRECTION ( 'NONE',  ( 0.000000000000000000, 0.000000000000000000, -1.000000000000000000 ) ) ;
#20461=EDGE_LOOP ( 'NONE', ( #31726, #37849, #38446, #47881 ) ) ;
#20463=DIRECTION ( 'NONE',  ( 0.000000000000000000, 0.07845909572783793529, 0.9969173337331285190 ) ) ;
#20476=EDGE_CURVE ( 'NONE', #39544, #28423, #7102, .T. ) ;
#20480=CARTESIAN_POINT ( 'NONE',  ( 0.000000000000000000, 0.000000000000000000, 0.000000000000000000 ) ) ;
#20485=ORIENTED_EDGE ( 'NONE', *, *, #22923, .F. ) ;
#20492=DIRECTION ( 'NONE',  ( -1.000000000000000000, 0.000000000000000000, 0.000000000000000000 ) ) ;
#20509=EDGE_CURVE ( 'NONE', #2989, #38555, #41582, .T. ) ;
#20516=ORIENTED_EDGE ( 'NONE', *, *, #28293, .T. ) ;
#20519=DIRECTION ( 'NONE',  ( 0.000000000000000000, 0.000000000000000000, -1.000000000000000000 ) ) ;
#20523=ORIENTED_EDGE ( 'NONE', *, *, #18608, .T. ) ;
#20524=ORIENTED_EDGE ( 'NONE', *, *, #39805, .T. ) ;
#20527=DIRECTION ( 'NONE',  ( 0.000000000000000000, 0.000000000000000000, 1.000000000000000000 ) ) ;
#20529=EDGE_LOOP ( 'NONE', ( #38885, #27303, #20022, #38419 ) ) ;
#20532=EDGE_CURVE ( 'NONE', #45521, #16029, #25098, .T. ) ;
#20538=AXIS2_PLACEMENT_3D ( 'NONE', #27201, #19830, #8102 ) ;
#20541=DIRECTION ( 'NONE',  ( -1.000000000000000000, 0.000000000000000000, -0.000000000000000000 ) ) ;
#20543=DIRECTION ( 'NONE',  ( 0.000000000000000000, 0.000000000000000000, 1.000000000000000000 ) ) ;
#20546=CIRCLE ( 'NONE', #12738, 31.99999999999999289 ) ;
#20550=ADVANCED_FACE ( 'NONE', ( #11965 ), #34953, .T. ) ;
#20555=CARTESIAN_POINT ( 'NONE',  ( 10.00000000000000000, 0.000000000000000000, 0.000000000000000000 ) ) ;
#20557=ORIENTED_EDGE ( 'NONE', *, *, #1437, .T. ) ;
#20569=EDGE_LOOP ( 'NONE', ( #7826, #20197, #25957, #25662 ) ) ;
#20570=CARTESIAN_POINT ( 'NONE',  ( 10.00000000000000000, 65.64334221924909230, 41.19522573413756561 ) ) ;
#20572=CARTESIAN_POINT ( 'NONE',  ( 0.000000000000000000, 0.000000000000000000, 0.000000000000000000 ) ) ;
#20573=CYLINDRICAL_SURFACE ( 'NONE', #47140, 31.99999999999999289 ) ;
#20576=AXIS2_PLACEMENT_3D ( 'NONE', #35993, #2229, #36235 ) ;
#20578=DIRECTION ( 'NONE',  ( 0.000000000000000000, 0.9876883405951383255, -0.1564344650402277048 ) ) ;
#20583=DIRECTION ( 'NONE',  ( -1.000000000000000000, 0.000000000000000000, 0.000000000000000000 ) ) ;
#20588=ADVANCED_FACE ( 'NONE', ( #2868 ), #24184, .T. ) ;
#20589=VECTOR ( 'NONE', #30656, 1000.000000000000000 ) ;
#20590=AXIS2_PLACEMENT_3D ( 'NONE', #37320, #37556, #22140 ) ;
#20609=DIRECTION ( 'NONE',  ( -1.000000000000000000, -0.000000000000000000, 0.000000000000000000 ) ) ;
#20610=DIRECTION ( 'NONE',  ( -1.000000000000000000, 0.000000000000000000, 0.000000000000000000 ) ) ;
#20614=VECTOR ( 'NONE', #9363, 1000.000000000000000 ) ;
#20623=VECTOR ( 'NONE', #32216, 1000.000000000000000 ) ;
#20624=CARTESIAN_POINT ( 'NONE',  ( 0.000000000000000000, 24.73286445877808148, -73.44644590900034586 ) ) ;
#20629=PRODUCT_DEFINITION_SHAPE ( 'NONE', 'NONE',  #29525 ) ;
#20633=EDGE_CURVE ( 'NONE', #6477, #33547, #21471, .T. ) ;
#20637=CARTESIAN_POINT ( 'NONE',  ( 0.000000000000000000, 0.000000000000000000, 0.000000000000000000 ) ) ;
#20638=CARTESIAN_POINT ( 'NONE',  ( 10.00000000000000000, 26.01480285779837232, 70.53064760720326376 ) ) ;
#20639=AXIS2_PLACEMENT_3D ( 'NONE', #35199, #1195, #8526 ) ;
#20640=AXIS2_PLACEMENT_3D ( 'NONE', #11747, #30841, #11994 ) ;
#20642=DIRECTION ( 'NONE',  ( 0.000000000000000000, 0.000000000000000000, 1.000000000000000000 ) ) ;
#20649=DIRECTION ( 'NONE',  ( 0.000000000000000000, -0.6494480483301903195, 0.7604059656000251577 ) ) ;
#20652=VECTOR ( 'NONE', #28483, 1000.000000000000000 ) ;
#20653=CARTESIAN_POINT ( 'NONE',  ( -10.00000000000000000, 0.000000000000000000, 0.000000000000000000 ) ) ;
#20668=AXIS2_PLACEMENT_3D ( 'NONE', #29331, #39645, #6105 ) ;
#20669=CARTESIAN_POINT ( 'NONE',  ( 10.00000000000000000, -46.54456581323762521, -59.03342792756313884 ) ) ;
#20670=ORIENTED_EDGE ( 'NONE', *, *, #33105, .T. ) ;
#20673=ORIENTED_EDGE ( 'NONE', *, *, #18887, .F. ) ;
#20675=DIRECTION ( 'NONE',  ( 0.000000000000000000, 0.000000000000000000, -1.000000000000000000 ) ) ;
#20677=CARTESIAN_POINT ( 'NONE',  ( 0.000000000000000000, 0.000000000000000000, 0.000000000000000000 ) ) ;
#20678=ORIENTED_EDGE ( 'NONE', *, *, #22471, .F. ) ;
#20680=ORIENTED_EDGE ( 'NONE', *, *, #9482, .T. ) ;
#20682=ORIENTED_EDGE ( 'NONE', *, *, #2335, .T. ) ;
#20688=CARTESIAN_POINT ( 'NONE',  ( 10.00000000000000000, 0.000000000000000000, 0.000000000000000000 ) ) ;
#20692=DIRECTION ( 'NONE',  ( -1.000000000000000000, 0.000000000000000000, 0.000000000000000000 ) ) ;
#20694=AXIS2_PLACEMENT_3D ( 'NONE', #37917, #1680, #23959 ) ;
#20695=DIRECTION ( 'NONE',  ( 0.000000000000000000, 0.000000000000000000, 1.000000000000000000 ) ) ;
#20700=CYLINDRICAL_SURFACE ( 'NONE', #43895, 77.49899999999999523 ) ;
#20701=CYLINDRICAL_SURFACE ( 'NONE', #43288, 82.00000000000000000 ) ;
#20707=AXIS2_PLACEMENT_3D ( 'NONE', #6747, #28063, #9441 ) ;
#20712=CARTESIAN_POINT ( 'NONE',  ( 10.00000000000000000, 0.000000000000000000, 0.000000000000000000 ) ) ;
#20715=DIRECTION ( 'NONE',  ( -1.000000000000000000, -0.000000000000000000, -0.000000000000000000 ) ) ;
#20718=ORIENTED_EDGE ( 'NONE', *, *, #6963, .T. ) ;
#20723=ORIENTED_EDGE ( 'NONE', *, *, #25075, .T. ) ;
#20726=ORIENTED_EDGE ( 'NONE', *, *, #15540, .F. ) ;
#20731=DIRECTION ( 'NONE',  ( -1.000000000000000000, 0.000000000000000000, 0.000000000000000000 ) ) ;
#20755=VECTOR ( 'NONE', #36910, 1000.000000000000000 ) ;
#20760=LINE ( 'NONE', #5352, #20214 ) ;
#20770=VERTEX_POINT ( 'NONE', #44469 ) ;
#20771=CARTESIAN_POINT ( 'NONE',  ( 0.000000000000000000, -44.88180994100329713, -63.18004540533077318 ) ) ;
#20773=FACE_OUTER_BOUND ( 'NONE', #38764, .T. ) ;
#20774=DIRECTION ( 'NONE',  ( 0.000000000000000000, 0.000000000000000000, 1.000000000000000000 ) ) ;
#20782=AXIS2_PLACEMENT_3D ( 'NONE', #32204, #47118, #20695 ) ;
#20784=EDGE_CURVE ( 'NONE', #2670, #11996, #44959, .T. ) ;
#20786=VECTOR ( 'NONE', #19178, 1000.000000000000000 ) ;
#20794=ORIENTED_EDGE ( 'NONE', *, *, #23798, .F. ) ;
#20795=AXIS2_PLACEMENT_3D ( 'NONE', #16710, #46579, #12087 ) ;
#20806=DIRECTION ( 'NONE',  ( 0.000000000000000000, 0.000000000000000000, 1.000000000000000000 ) ) ;
#20807=ORIENTED_EDGE ( 'NONE', *, *, #14596, .F. ) ;
#20813=ORIENTED_EDGE ( 'NONE', *, *, #25032, .T. ) ;
#20814=DIRECTION ( 'NONE',  ( 0.000000000000000000, 0.3826834323650905589, -0.9238795325112864054 ) ) ;
#20820=CARTESIAN_POINT ( 'NONE',  ( 10.00000000000000000, -46.54456581323847786, 59.03342792756247093 ) ) ;
#20826=CARTESIAN_POINT ( 'NONE',  ( -10.00000000000000000, 0.000000000000000000, 0.000000000000000000 ) ) ;
#20829=DIRECTION ( 'NONE',  ( -1.000000000000000000, 0.000000000000000000, 0.000000000000000000 ) ) ;
#20832=VECTOR ( 'NONE', #13280, 1000.000000000000000 ) ;
#20835=FACE_OUTER_BOUND ( 'NONE', #18739, .T. ) ;
#20848=AXIS2_PLACEMENT_3D ( 'NONE', #24603, #16778, #39779 ) ;
#20860=FACE_OUTER_BOUND ( 'NONE', #38038, .T. ) ;
#20864=CIRCLE ( 'NONE', #32569, 31.99999999999998934 ) ;
#20869=FACE_OUTER_BOUND ( 'NONE', #40634, .T. ) ;
#20871=DIRECTION ( 'NONE',  ( 0.000000000000000000, 0.000000000000000000, 1.000000000000000000 ) ) ;
#20872=ORIENTED_EDGE ( 'NONE', *, *, #28703, .F. ) ;
#20876=CYLINDRICAL_SURFACE ( 'NONE', #6706, 31.99999999999999289 ) ;
#20882=LINE ( 'NONE', #17186, #26115 ) ;
#20887=VECTOR ( 'NONE', #18916, 1000.000000000000000 ) ;
#20895=AXIS2_PLACEMENT_3D ( 'NONE', #37192, #36931, #22267 ) ;
#20901=VECTOR ( 'NONE', #39743, 1000.000000000000000 ) ;
#20903=CARTESIAN_POINT ( 'NONE',  ( 0.000000000000000000, -6.903761155838323837, 77.19088730480521576 ) ) ;
#20910=ORIENTED_EDGE ( 'NONE', *, *, #22697, .F. ) ;
#20911=ORIENTED_EDGE ( 'NONE', *, *, #31569, .F. ) ;
#20912=ADVANCED_FACE ( 'NONE', ( #42242 ), #34173, .T. ) ;
#20915=VERTEX_POINT ( 'NONE', #646 ) ;
#20917=CARTESIAN_POINT ( 'NONE',  ( 10.00000000000000000, 20.40083707022882820, 72.35432306680490910 ) ) ;
#20918=VERTEX_POINT ( 'NONE', #15575 ) ;
#20920=DIRECTION ( 'NONE',  ( -1.000000000000000000, -0.000000000000000000, -0.000000000000000000 ) ) ;
#20922=ORIENTED_EDGE ( 'NONE', *, *, #2913, .T. ) ;
#20924=CARTESIAN_POINT ( 'NONE',  ( 10.00000000000000000, 0.000000000000000000, 0.000000000000000000 ) ) ;
#20945=LINE ( 'NONE', #10658, #17353 ) ;
#20954=DIRECTION ( 'NONE',  ( -1.000000000000000000, -0.000000000000000000, -0.000000000000000000 ) ) ;
#20959=EDGE_LOOP ( 'NONE', ( #32412, #11548, #39599, #17020 ) ) ;
#20963=LINE ( 'NONE', #40527, #34312 ) ;
#20967=EDGE_CURVE ( 'NONE', #46842, #10502, #40035, .T. ) ;
#20969=CYLINDRICAL_SURFACE ( 'NONE', #8158, 31.99999999999999289 ) ;
#20970=ORIENTED_EDGE ( 'NONE', *, *, #4927, .T. ) ;
#20974=EDGE_CURVE ( 'NONE', #14404, #24169, #31448, .T. ) ;
#20981=DIRECTION ( 'NONE',  ( 1.000000000000000000, 0.000000000000000000, -0.000000000000000000 ) ) ;
#20982=CIRCLE ( 'NONE', #27241, 77.49899999999999523 ) ;
#20983=AXIS2_PLACEMENT_3D ( 'NONE', #3597, #22199, #24903 ) ;
#20993=DIRECTION ( 'NONE',  ( 0.000000000000000000, 0.000000000000000000, 1.000000000000000000 ) ) ;
#20994=ADVANCED_FACE ( 'NONE', ( #34897 ), #12165, .T. ) ;
#20995=DIRECTION ( 'NONE',  ( -1.000000000000000000, 0.000000000000000000, 0.000000000000000000 ) ) ;
#20999=EDGE_CURVE ( 'NONE', #39605, #28052, #29853, .T. ) ;
#21002=ORIENTED_EDGE ( 'NONE', *, *, #22914, .F. ) ;
#21004=DIRECTION ( 'NONE',  ( 0.000000000000000000, 0.9510565162951546414, -0.3090169943749446202 ) ) ;
#21007=CARTESIAN_POINT ( 'NONE',  ( 0.000000000000000000, 23.16143007188426850, 73.95703589263983702 ) ) ;
#21008=ORIENTED_EDGE ( 'NONE', *, *, #31417, .F. ) ;
#21014=AXIS2_PLACEMENT_3D ( 'NONE', #11476, #11220, #22481 ) ;
#21020=VERTEX_POINT ( 'NONE', #16791 ) ;
#21024=DIRECTION ( 'NONE',  ( 1.000000000000000000, 0.000000000000000000, 0.000000000000000000 ) ) ;
#21025=ORIENTED_EDGE ( 'NONE', *, *, #31417, .T. ) ;
#21026=VERTEX_POINT ( 'NONE', #9921 ) ;
#21042=DIRECTION ( 'NONE',  ( -1.000000000000000000, 0.000000000000000000, -0.000000000000000000 ) ) ;
#21050=DIRECTION ( 'NONE',  ( -1.000000000000000000, -0.000000000000000000, -0.000000000000000000 ) ) ;
#21053=DIRECTION ( 'NONE',  ( -1.000000000000000000, -0.000000000000000000, 0.000000000000000000 ) ) ;
#21058=DIRECTION ( 'NONE',  ( -1.000000000000000000, -0.000000000000000000, -0.000000000000000000 ) ) ;
#21074=FACE_OUTER_BOUND ( 'NONE', #44135, .T. ) ;
#21081=VERTEX_POINT ( 'NONE', #2559 ) ;
#21083=LINE ( 'NONE', #17408, #42365 ) ;
#21084=EDGE_CURVE ( 'NONE', #13194, #28502, #47375, .T. ) ;
#21088=CYLINDRICAL_SURFACE ( 'NONE', #4338, 82.00000000000000000 ) ;
#21092=FACE_OUTER_BOUND ( 'NONE', #47814, .T. ) ;
#21093=ORIENTED_EDGE ( 'NONE', *, *, #27420, .F. ) ;
#21094=DIRECTION ( 'NONE',  ( -1.000000000000000000, -0.000000000000000000, 0.000000000000000000 ) ) ;
#21095=DIRECTION ( 'NONE',  ( -1.000000000000000000, 0.000000000000000000, -0.000000000000000000 ) ) ;
#21100=FACE_OUTER_BOUND ( 'NONE', #23955, .T. ) ;
#21101=EDGE_CURVE ( 'NONE', #41161, #33614, #1615, .T. ) ;
#21105=AXIS2_PLACEMENT_3D ( 'NONE', #9404, #35607, #16996 ) ;
#21107=CARTESIAN_POINT ( 'NONE',  ( 10.00000000000000000, 20.40083707022987625, -72.35432306680462489 ) ) ;
#21115=CARTESIAN_POINT ( 'NONE',  ( 10.00000000000000000, 0.000000000000000000, 0.000000000000000000 ) ) ;
#21116=DIRECTION ( 'NONE',  ( -1.000000000000000000, 0.000000000000000000, 0.000000000000000000 ) ) ;
#21117=CIRCLE ( 'NONE', #25031, 32.00000000000000000 ) ;
#21120=CYLINDRICAL_SURFACE ( 'NONE', #46495, 31.99999999999999289 ) ;
#21121=VECTOR ( 'NONE', #9299, 1000.000000000000000 ) ;
#21125=CARTESIAN_POINT ( 'NONE',  ( 10.00000000000000000, 81.96053171279901051, -2.543863470248666658 ) ) ;
#21130=EDGE_CURVE ( 'NONE', #37827, #15854, #38458, .T. ) ;
#21144=ORIENTED_EDGE ( 'NONE', *, *, #34467, .F. ) ;
#21146=FACE_OUTER_BOUND ( 'NONE', #28313, .T. ) ;
#21151=VECTOR ( 'NONE', #32961, 1000.000000000000000 ) ;
#21152=CARTESIAN_POINT ( 'NONE',  ( 10.00000000000000000, 0.000000000000000000, 0.000000000000000000 ) ) ;
#21159=CARTESIAN_POINT ( 'NONE',  ( 10.00000000000000000, -2.946379043145784582, -75.11764819372150725 ) ) ;
#21165=DIRECTION ( 'NONE',  ( -1.000000000000000000, 0.000000000000000000, 0.000000000000000000 ) ) ;
#21167=DIRECTION ( 'NONE',  ( -1.000000000000000000, 0.000000000000000000, 0.000000000000000000 ) ) ;
#21171=CYLINDRICAL_SURFACE ( 'NONE', #40132, 32.00000000000000000 ) ;
#21181=CIRCLE ( 'NONE', #17262, 31.99999999999999289 ) ;
#21182=CARTESIAN_POINT ( 'NONE',  ( 10.00000000000000000, -14.66109333815410487, -73.73191006444587003 ) ) ;
#21189=ORIENTED_EDGE ( 'NONE', *, *, #10459, .T. ) ;
#21194=ORIENTED_EDGE ( 'NONE', *, *, #2379, .F. ) ;
#21205=ORIENTED_EDGE ( 'NONE', *, *, #14704, .F. ) ;
#21209=CIRCLE ( 'NONE', #7902, 82.00000000000000000 ) ;
#21225=CIRCLE ( 'NONE', #43115, 82.00000000000000000 ) ;
#21227=DIRECTION ( 'NONE',  ( -1.000000000000000000, 0.000000000000000000, 0.000000000000000000 ) ) ;
#21239=ORIENTED_EDGE ( 'NONE', *, *, #23866, .T. ) ;
#21242=ORIENTED_EDGE ( 'NONE', *, *, #32808, .T. ) ;
#21244=AXIS2_PLACEMENT_3D ( 'NONE', #46113, #30955, #39009 ) ;
#21245=DIRECTION ( 'NONE',  ( 0.000000000000000000, 0.000000000000000000, 1.000000000000000000 ) ) ;
#21249=CARTESIAN_POINT ( 'NONE',  ( 10.00000000000000000, -74.18225833017913828, 34.94270380257611919 ) ) ;
#21253=ORIENTED_EDGE ( 'NONE', *, *, #14704, .T. ) ;
#21262=DIRECTION ( 'NONE',  ( -1.000000000000000000, 0.000000000000000000, -0.000000000000000000 ) ) ;
#21274=EDGE_CURVE ( 'NONE', #18013, #919, #23597, .T. ) ;
#21276=CARTESIAN_POINT ( 'NONE',  ( 5.000000000000000000, -40.65526001592664329, 71.21200624218782593 ) ) ;
#21279=CARTESIAN_POINT ( 'NONE',  ( 10.00000000000000000, -18.89407956138203204, -75.16055320797050854 ) ) ;
#21283=DIRECTION ( 'NONE',  ( 0.000000000000000000, 0.000000000000000000, 1.000000000000000000 ) ) ;
#21285=CARTESIAN_POINT ( 'NONE',  ( 10.00000000000000000, 5.256550761632864166, 77.32052557432842832 ) ) ;
#21291=DIRECTION ( 'NONE',  ( -1.000000000000000000, -0.000000000000000000, 0.000000000000000000 ) ) ;
#21293=ADVANCED_FACE ( 'NONE', ( #34841 ), #45612, .T. ) ;
#21294=CARTESIAN_POINT ( 'NONE',  ( 0.000000000000000000, 0.000000000000000000, 0.000000000000000000 ) ) ;
#21297=ORIENTED_EDGE ( 'NONE', *, *, #35529, .F. ) ;
#21302=LINE ( 'NONE', #36240, #15926 ) ;
#21309=CARTESIAN_POINT ( 'NONE',  ( 10.00000000000000000, 0.000000000000000000, 0.000000000000000000 ) ) ;
#21314=DIRECTION ( 'NONE',  ( 0.000000000000000000, 0.000000000000000000, 1.000000000000000000 ) ) ;
#21315=ADVANCED_FACE ( 'NONE', ( #46107 ), #7923, .T. ) ;
#21322=ORIENTED_EDGE ( 'NONE', *, *, #22221, .F. ) ;
#21328=CARTESIAN_POINT ( 'NONE',  ( 10.00000000000000000, -18.89407956138310496, 75.16055320797023853 ) ) ;
#21333=FACE_OUTER_BOUND ( 'NONE', #39941, .T. ) ;
#21343=CARTESIAN_POINT ( 'NONE',  ( 0.000000000000000000, 20.41045688087930898, -72.35160999960793049 ) ) ;
#21349=CIRCLE ( 'NONE', #44790, 77.49899999999999523 ) ;
#21351=CARTESIAN_POINT ( 'NONE',  ( 0.000000000000000000, 0.000000000000000000, 0.000000000000000000 ) ) ;
#21353=CARTESIAN_POINT ( 'NONE',  ( 0.000000000000000000, 75.11725578898472122, -2.956366410619845730 ) ) ;
#21355=AXIS2_PLACEMENT_3D ( 'NONE', #25847, #7256, #22189 ) ;
#21359=CARTESIAN_POINT ( 'NONE',  ( 0.000000000000000000, 41.76937507738788469, 62.50329211542452157 ) ) ;
#21364=VERTEX_POINT ( 'NONE', #12343 ) ;
#21366=CIRCLE ( 'NONE', #42479, 31.99999999999999645 ) ;
#21370=EDGE_CURVE ( 'NONE', #41616, #24887, #32238, .T. ) ;
#21374=ORIENTED_EDGE ( 'NONE', *, *, #44526, .T. ) ;
#21394=VERTEX_POINT ( 'NONE', #11849 ) ;
#21403=DIRECTION ( 'NONE',  ( -1.000000000000000000, 0.000000000000000000, 0.000000000000000000 ) ) ;
#21405=AXIS2_PLACEMENT_3D ( 'NONE', #21855, #26276, #8385 ) ;
#21407=DIRECTION ( 'NONE',  ( 0.000000000000000000, -0.9723699203976789995, 0.2334453638558956212 ) ) ;
#21411=VERTEX_POINT ( 'NONE', #26774 ) ;
#21412=VERTEX_POINT ( 'NONE', #23341 ) ;
#21413=DIRECTION ( 'NONE',  ( -1.000000000000000000, 0.000000000000000000, -0.000000000000000000 ) ) ;
#21421=DIRECTION ( 'NONE',  ( 0.000000000000000000, 0.000000000000000000, 1.000000000000000000 ) ) ;
#21423=CIRCLE ( 'NONE', #37854, 82.00000000000000000 ) ;
#21426=ADVANCED_FACE ( 'NONE', ( #19414 ), #817, .T. ) ;
#21435=ORIENTED_EDGE ( 'NONE', *, *, #9013, .F. ) ;
#21439=EDGE_LOOP ( 'NONE', ( #8491, #31290, #19297, #21008 ) ) ;
#21443=EDGE_LOOP ( 'NONE', ( #46183, #17631, #3250, #47845 ) ) ;
#21445=CARTESIAN_POINT ( 'NONE',  ( -10.00000000000000000, 0.000000000000000000, 0.000000000000000000 ) ) ;
#21446=CARTESIAN_POINT ( 'NONE',  ( 10.00000000000000000, -78.73519480814938731, -22.90783923731713756 ) ) ;
#21451=VERTEX_POINT ( 'NONE', #5711 ) ;
#21453=DIRECTION ( 'NONE',  ( -1.000000000000000000, -0.000000000000000000, -0.000000000000000000 ) ) ;
#21455=CARTESIAN_POINT ( 'NONE',  ( 10.00000000000000000, 0.000000000000000000, 0.000000000000000000 ) ) ;
#21458=DIRECTION ( 'NONE',  ( 1.000000000000000000, -0.000000000000000000, 0.000000000000000000 ) ) ;
#21462=ORIENTED_EDGE ( 'NONE', *, *, #16951, .F. ) ;
#21467=ORIENTED_EDGE ( 'NONE', *, *, #35655, .F. ) ;
#21471=LINE ( 'NONE', #9972, #38420 ) ;
#21472=AXIS2_PLACEMENT_3D ( 'NONE', #32935, #14348, #29278 ) ;
#21473=CIRCLE ( 'NONE', #30072, 77.49899999999999523 ) ;
#21478=VECTOR ( 'NONE', #11814, 1000.000000000000000 ) ;
#21480=CARTESIAN_POINT ( 'NONE',  ( 10.00000000000000000, 81.96053171279901051, 2.543863470248666658 ) ) ;
#21487=ORIENTED_EDGE ( 'NONE', *, *, #27844, .T. ) ;
#21488=EDGE_CURVE ( 'NONE', #8273, #15618, #38487, .T. ) ;
#21497=ORIENTED_EDGE ( 'NONE', *, *, #48082, .T. ) ;
#21500=AXIS2_PLACEMENT_3D ( 'NONE', #7448, #22380, #3766 ) ;
#21501=VERTEX_POINT ( 'NONE', #28465 ) ;
#21503=CYLINDRICAL_SURFACE ( 'NONE', #4268, 77.49899999999999523 ) ;
#21504=ORIENTED_EDGE ( 'NONE', *, *, #27527, .T. ) ;
#21509=DIRECTION ( 'NONE',  ( -1.000000000000000000, -0.000000000000000000, -0.000000000000000000 ) ) ;
#21513=ORIENTED_EDGE ( 'NONE', *, *, #12767, .F. ) ;
#21516=ADVANCED_FACE ( 'NONE', ( #1560 ), #35574, .T. ) ;
#21522=LINE ( 'NONE', #25171, #8751 ) ;
#21524=CARTESIAN_POINT ( 'NONE',  ( 0.000000000000000000, -5.256550761632340141, -77.32052557432847095 ) ) ;
#21525=VERTEX_POINT ( 'NONE', #38778 ) ;
#21528=DIRECTION ( 'NONE',  ( -1.000000000000000000, -0.000000000000000000, -0.000000000000000000 ) ) ;
#21539=CYLINDRICAL_SURFACE ( 'NONE', #10427, 32.00000000000000000 ) ;
#21542=CARTESIAN_POINT ( 'NONE',  ( 0.000000000000000000, 73.44644590900061587, 24.73286445877730699 ) ) ;
#21543=AXIS2_PLACEMENT_3D ( 'NONE', #35783, #6172, #43379 ) ;
#21554=CYLINDRICAL_SURFACE ( 'NONE', #47483, 31.99999999999999289 ) ;
#21556=ORIENTED_EDGE ( 'NONE', *, *, #10799, .F. ) ;
#21557=ORIENTED_EDGE ( 'NONE', *, *, #45938, .T. ) ;
#21563=ORIENTED_EDGE ( 'NONE', *, *, #25668, .F. ) ;
#21572=VECTOR ( 'NONE', #42838, 1000.000000000000000 ) ;
#21577=ORIENTED_EDGE ( 'NONE', *, *, #46858, .F. ) ;
#21578=VECTOR ( 'NONE', #14507, 1000.000000000000000 ) ;
#21579=DIRECTION ( 'NONE',  ( -1.000000000000000000, -0.000000000000000000, -0.000000000000000000 ) ) ;
#21581=CARTESIAN_POINT ( 'NONE',  ( 10.00000000000000000, -30.41916302227060598, -71.27951684758059514 ) ) ;
#21588=ORIENTED_EDGE ( 'NONE', *, *, #5423, .T. ) ;
#21589=DIRECTION ( 'NONE',  ( -1.000000000000000000, -0.000000000000000000, -0.000000000000000000 ) ) ;
#21598=DIRECTION ( 'NONE',  ( -1.000000000000000000, 0.000000000000000000, 0.000000000000000000 ) ) ;
#21605=VECTOR ( 'NONE', #14923, 1000.000000000000000 ) ;
#21608=CARTESIAN_POINT ( 'NONE',  ( 10.00000000000000000, 59.03961581697465277, -46.53671651293886669 ) ) ;
#21609=DIRECTION ( 'NONE',  ( -1.000000000000000000, 0.000000000000000000, -0.000000000000000000 ) ) ;
#21610=CARTESIAN_POINT ( 'NONE',  ( 10.00000000000000000, -79.10210256391383155, 21.60688246758557796 ) ) ;
#21614=VERTEX_POINT ( 'NONE', #702 ) ;
#21616=DIRECTION ( 'NONE',  ( 0.000000000000000000, 0.9969173337331276308, 0.07845909572784873220 ) ) ;
#21617=CARTESIAN_POINT ( 'NONE',  ( 10.00000000000000000, -75.16055320797043748, 18.89407956138229494 ) ) ;
#21629=ORIENTED_EDGE ( 'NONE', *, *, #27527, .F. ) ;
#21632=EDGE_LOOP ( 'NONE', ( #48383, #2190, #37883, #26513 ) ) ;
#21638=CYLINDRICAL_SURFACE ( 'NONE', #1997, 31.99999999999999289 ) ;
#21641=FACE_OUTER_BOUND ( 'NONE', #10434, .T. ) ;
#21644=CIRCLE ( 'NONE', #31836, 31.99999999999998934 ) ;
#21645=ORIENTED_EDGE ( 'NONE', *, *, #19790, .F. ) ;
#21649=CARTESIAN_POINT ( 'NONE',  ( 10.00000000000000000, -69.42325613327466272, 34.44570377933573724 ) ) ;
#21652=DIRECTION ( 'NONE',  ( -1.000000000000000000, -0.000000000000000000, -0.000000000000000000 ) ) ;
#21655=CARTESIAN_POINT ( 'NONE',  ( -10.00000000000000000, 0.000000000000000000, 0.000000000000000000 ) ) ;
#21657=CARTESIAN_POINT ( 'NONE',  ( 10.00000000000000000, -72.35432306680469594, -20.40083707022958848 ) ) ;
#21659=DIRECTION ( 'NONE',  ( 0.000000000000000000, 0.2334453638558990907, 0.9723699203976781114 ) ) ;
#21661=AXIS2_PLACEMENT_3D ( 'NONE', #22622, #38048, #595 ) ;
#21663=CARTESIAN_POINT ( 'NONE',  ( 10.00000000000000000, 69.42325613327439271, 34.44570377933623462 ) ) ;
#21664=EDGE_CURVE ( 'NONE', #42774, #32530, #40062, .T. ) ;
#21673=EDGE_CURVE ( 'NONE', #14404, #46520, #22004, .T. ) ;
#21674=FACE_OUTER_BOUND ( 'NONE', #48009, .T. ) ;
#21678=CIRCLE ( 'NONE', #24033, 82.00000000000000000 ) ;
#21680=CIRCLE ( 'NONE', #43559, 32.00000000000000000 ) ;
#21688=CYLINDRICAL_SURFACE ( 'NONE', #26932, 77.49899999999999523 ) ;
#21691=ORIENTED_EDGE ( 'NONE', *, *, #25873, .F. ) ;
#21699=ORIENTED_EDGE ( 'NONE', *, *, #6468, .T. ) ;
#21700=ORIENTED_EDGE ( 'NONE', *, *, #7233, .T. ) ;
#21705=DIRECTION ( 'NONE',  ( 0.000000000000000000, 0.5224985647159500202, -0.8526401643540916231 ) ) ;
#21719=VERTEX_POINT ( 'NONE', #38660 ) ;
#21720=DIRECTION ( 'NONE',  ( -1.000000000000000000, 0.000000000000000000, 0.000000000000000000 ) ) ;
#21723=EDGE_CURVE ( 'NONE', #30126, #10449, #27894, .T. ) ;
#21734=AXIS2_PLACEMENT_3D ( 'NONE', #27162, #30833, #33755 ) ;
#21735=EDGE_LOOP ( 'NONE', ( #18052, #13190, #44342, #5882 ) ) ;
#21740=ORIENTED_EDGE ( 'NONE', *, *, #15216, .F. ) ;
#21746=CARTESIAN_POINT ( 'NONE',  ( 10.00000000000000000, -80.28980883073768382, 16.65972982744906972 ) ) ;
#21749=ADVANCED_FACE ( 'NONE', ( #35201 ), #31556, .T. ) ;
#21752=LINE ( 'NONE', #32762, #16613 ) ;
#21757=CARTESIAN_POINT ( 'NONE',  ( 10.00000000000000000, 0.000000000000000000, 0.000000000000000000 ) ) ;
#21758=DIRECTION ( 'NONE',  ( -1.000000000000000000, -0.000000000000000000, 0.000000000000000000 ) ) ;
#21763=EDGE_LOOP ( 'NONE', ( #6164, #26287, #28132, #5932 ) ) ;
#21769=DIRECTION ( 'NONE',  ( -1.000000000000000000, 0.000000000000000000, 0.000000000000000000 ) ) ;
#21770=EDGE_CURVE ( 'NONE', #15509, #7240, #26907, .T. ) ;
#21772=CARTESIAN_POINT ( 'NONE',  ( 10.00000000000000000, -70.52718814184277107, 26.02418014898285037 ) ) ;
#21773=PLANE ( 'NONE',  #3606 ) ;
#21774=CARTESIAN_POINT ( 'NONE',  ( 10.00000000000000000, 0.000000000000000000, 0.000000000000000000 ) ) ;
#21775=VECTOR ( 'NONE', #20981, 1000.000000000000000 ) ;
#21780=DIRECTION ( 'NONE',  ( 0.000000000000000000, 0.1564344650402312020, -0.9876883405951376593 ) ) ;
#21797=CARTESIAN_POINT ( 'NONE',  ( 0.000000000000000000, 5.256550761633969060, -77.32052557432835727 ) ) ;
#21798=CIRCLE ( 'NONE', #29632, 31.99999999999998934 ) ;
#21801=DIRECTION ( 'NONE',  ( 0.000000000000000000, 0.000000000000000000, 1.000000000000000000 ) ) ;
#21803=AXIS2_PLACEMENT_3D ( 'NONE', #31036, #1151, #46186 ) ;
#21804=EDGE_CURVE ( 'NONE', #14555, #34506, #16647, .T. ) ;
#21806=CIRCLE ( 'NONE', #5410, 77.49900000000002365 ) ;
#21810=LINE ( 'NONE', #40911, #27622 ) ;
#21811=LINE ( 'NONE', #31905, #5191 ) ;
#21812=DIRECTION ( 'NONE',  ( -1.000000000000000000, -0.000000000000000000, -0.000000000000000000 ) ) ;
#21819=EDGE_CURVE ( 'NONE', #42231, #45900, #26044, .T. ) ;
#21821=LINE ( 'NONE', #29423, #31673 ) ;
#21823=FACE_OUTER_BOUND ( 'NONE', #36031, .T. ) ;
#21830=LINE ( 'NONE', #36754, #21578 ) ;
#21839=CARTESIAN_POINT ( 'NONE',  ( 10.00000000000000000, 81.50828551894225882, 8.966570791700975818 ) ) ;
#21840=CARTESIAN_POINT ( 'NONE',  ( -10.00000000000000000, 0.000000000000000000, 0.000000000000000000 ) ) ;
#21841=EDGE_CURVE ( 'NONE', #2889, #29380, #20546, .T. ) ;
#21845=VECTOR ( 'NONE', #30724, 1000.000000000000000 ) ;
#21848=AXIS2_PLACEMENT_3D ( 'NONE', #38068, #48108, #25819 ) ;
#21854=ORIENTED_EDGE ( 'NONE', *, *, #47848, .F. ) ;
#21855=CARTESIAN_POINT ( 'NONE',  ( 0.000000000000000000, 14.67089635893819377, -73.72996012237423713 ) ) ;
#21856=VERTEX_POINT ( 'NONE', #4623 ) ;
#21862=FACE_OUTER_BOUND ( 'NONE', #48189, .T. ) ;
#21871=ORIENTED_EDGE ( 'NONE', *, *, #46743, .F. ) ;
#21873=AXIS2_PLACEMENT_3D ( 'NONE', #37582, #4053, #18959 ) ;
#21874=LINE ( 'NONE', #36566, #2901 ) ;
#21876=EDGE_LOOP ( 'NONE', ( #36265, #24889, #2953, #5821 ) ) ;
#21879=AXIS2_PLACEMENT_3D ( 'NONE', #20058, #39392, #34987 ) ;
#21890=CIRCLE ( 'NONE', #7814, 82.00000000000000000 ) ;
#21894=CARTESIAN_POINT ( 'NONE',  ( 0.000000000000000000, -76.41127070299280888, 12.93880638057289012 ) ) ;
#21906=AXIS2_PLACEMENT_3D ( 'NONE', #26878, #38133, #23199 ) ;
#21907=CIRCLE ( 'NONE', #28177, 82.00000000000000000 ) ;
#21908=DIRECTION ( 'NONE',  ( -1.000000000000000000, 0.000000000000000000, 0.000000000000000000 ) ) ;
#21909=ORIENTED_EDGE ( 'NONE', *, *, #3603, .T. ) ;
#21910=VECTOR ( 'NONE', #13502, 1000.000000000000000 ) ;
#21919=ORIENTED_EDGE ( 'NONE', *, *, #28838, .T. ) ;
#21923=ORIENTED_EDGE ( 'NONE', *, *, #14697, .F. ) ;
#21924=ORIENTED_EDGE ( 'NONE', *, *, #9077, .F. ) ;
#21931=ORIENTED_EDGE ( 'NONE', *, *, #27304, .T. ) ;
#21944=CIRCLE ( 'NONE', #39920, 31.99999999999999289 ) ;
#21948=DIRECTION ( 'NONE',  ( -1.000000000000000000, 0.000000000000000000, 0.000000000000000000 ) ) ;
#21951=CARTESIAN_POINT ( 'NONE',  ( 10.00000000000000000, 72.35160999960844208, -20.41045688087747223 ) ) ;
#21953=CARTESIAN_POINT ( 'NONE',  ( 10.00000000000000000, 31.46837873494978055, 68.27212725128286763 ) ) ;
#21960=DIRECTION ( 'NONE',  ( 1.000000000000000000, 0.000000000000000000, 0.000000000000000000 ) ) ;
#21969=VERTEX_POINT ( 'NONE', #39369 ) ;
#21983=EDGE_LOOP ( 'NONE', ( #18442, #381, #5338, #32879 ) ) ;
#21989=CARTESIAN_POINT ( 'NONE',  ( 0.000000000000000000, 71.21200624218795383, 40.65526001592638039 ) ) ;
#21991=ORIENTED_EDGE ( 'NONE', *, *, #40514, .T. ) ;
#21993=CARTESIAN_POINT ( 'NONE',  ( 10.00000000000000000, 30.41916302227113178, 71.27951684758036777 ) ) ;
#21994=ORIENTED_EDGE ( 'NONE', *, *, #23644, .F. ) ;
#22004=LINE ( 'NONE', #37670, #37710 ) ;
#22006=EDGE_CURVE ( 'NONE', #42551, #21081, #44004, .T. ) ;
#22009=CIRCLE ( 'NONE', #40782, 31.99999999999999289 ) ;
#22011=DIRECTION ( 'NONE',  ( 1.000000000000000000, -0.000000000000000000, 0.000000000000000000 ) ) ;
#22014=DIRECTION ( 'NONE',  ( 0.000000000000000000, -0.6494480483301739993, -0.7604059656000390355 ) ) ;
#22015=LINE ( 'NONE', #44301, #23009 ) ;
#22028=DIRECTION ( 'NONE',  ( -1.000000000000000000, 0.000000000000000000, 0.000000000000000000 ) ) ;
#22033=VERTEX_POINT ( 'NONE', #4093 ) ;
#22046=ORIENTED_EDGE ( 'NONE', *, *, #28773, .T. ) ;
#22048=DIRECTION ( 'NONE',  ( 0.000000000000000000, 0.000000000000000000, 1.000000000000000000 ) ) ;
#22053=ORIENTED_EDGE ( 'NONE', *, *, #43226, .F. ) ;
#22055=EDGE_LOOP ( 'NONE', ( #39119, #23194, #22889, #25546 ) ) ;
#22057=FACE_OUTER_BOUND ( 'NONE', #17746, .T. ) ;
#22068=DIRECTION ( 'NONE',  ( 1.000000000000000000, 0.000000000000000000, 0.000000000000000000 ) ) ;
#22070=DIRECTION ( 'NONE',  ( -1.000000000000000000, 0.000000000000000000, 0.000000000000000000 ) ) ;
#22072=DIRECTION ( 'NONE',  ( 1.000000000000000000, 0.000000000000000000, 0.000000000000000000 ) ) ;
#22073=FACE_OUTER_BOUND ( 'NONE', #21983, .T. ) ;
#22074=VECTOR ( 'NONE', #23451, 1000.000000000000000 ) ;
#22084=DIRECTION ( 'NONE',  ( -1.000000000000000000, -0.000000000000000000, -0.000000000000000000 ) ) ;
#22085=ORIENTED_EDGE ( 'NONE', *, *, #19288, .F. ) ;
#22088=ADVANCED_FACE ( 'NONE', ( #32971 ), #22207, .T. ) ;
#22098=CARTESIAN_POINT ( 'NONE',  ( 0.000000000000000000, 26.02418014898407961, -70.52718814184231633 ) ) ;
#22099=VERTEX_POINT ( 'NONE', #7026 ) ;
#22101=EDGE_CURVE ( 'NONE', #34021, #29746, #38559, .T. ) ;
#22102=EDGE_CURVE ( 'NONE', #21614, #22033, #36878, .T. ) ;
#22110=ORIENTED_EDGE ( 'NONE', *, *, #32199, .F. ) ;
#22117=CIRCLE ( 'NONE', #4136, 31.99999999999998934 ) ;
#22124=DIRECTION ( 'NONE',  ( -1.000000000000000000, 0.000000000000000000, 0.000000000000000000 ) ) ;
#22125=DIRECTION ( 'NONE',  ( 0.000000000000000000, 0.000000000000000000, 1.000000000000000000 ) ) ;
#22130=CARTESIAN_POINT ( 'NONE',  ( 0.000000000000000000, 65.59268652807263322, -36.72794159290169347 ) ) ;
#22131=CARTESIAN_POINT ( 'NONE',  ( 0.000000000000000000, -76.69515212746036070, 29.01471420065537643 ) ) ;
#22134=AXIS2_PLACEMENT_3D ( 'NONE', #14067, #28988, #43925 ) ;
#22136=DIRECTION ( 'NONE',  ( -1.000000000000000000, 0.000000000000000000, 0.000000000000000000 ) ) ;
#22140=DIRECTION ( 'NONE',  ( 0.000000000000000000, 0.000000000000000000, 1.000000000000000000 ) ) ;
#22142=LINE ( 'NONE', #14079, #14546 ) ;
#22143=CARTESIAN_POINT ( 'NONE',  ( 0.000000000000000000, -65.58780272294100655, 36.73666225445870737 ) ) ;
#22149=EDGE_CURVE ( 'NONE', #9352, #7024, #23174, .T. ) ;
#22155=ORIENTED_EDGE ( 'NONE', *, *, #29727, .F. ) ;
#22156=AXIS2_PLACEMENT_3D ( 'NONE', #38576, #34892, #43205 ) ;
#22158=CIRCLE ( 'NONE', #26071, 77.49900000000000944 ) ;
#22176=ORIENTED_EDGE ( 'NONE', *, *, #39810, .T. ) ;
#22177=FACE_OUTER_BOUND ( 'NONE', #22238, .T. ) ;
#22180=DIRECTION ( 'NONE',  ( -1.000000000000000000, -0.000000000000000000, -0.000000000000000000 ) ) ;
#22186=CARTESIAN_POINT ( 'NONE',  ( 0.000000000000000000, 59.03342792756263435, 46.54456581323825048 ) ) ;
#22189=DIRECTION ( 'NONE',  ( 0.000000000000000000, 0.5877852522924684742, 0.8090169943749506709 ) ) ;
#22191=AXIS2_PLACEMENT_3D ( 'NONE', #32631, #3006, #17702 ) ;
#22194=ORIENTED_EDGE ( 'NONE', *, *, #11964, .F. ) ;
#22197=AXIS2_PLACEMENT_3D ( 'NONE', #29425, #44349, #19581 ) ;
#22198=ORIENTED_EDGE ( 'NONE', *, *, #31929, .F. ) ;
#22199=DIRECTION ( 'NONE',  ( -1.000000000000000000, -0.000000000000000000, -0.000000000000000000 ) ) ;
#22200=ORIENTED_EDGE ( 'NONE', *, *, #25621, .T. ) ;
#22203=AXIS2_PLACEMENT_3D ( 'NONE', #46416, #28775, #1627 ) ;
#22207=CYLINDRICAL_SURFACE ( 'NONE', #36203, 82.00000000000000000 ) ;
#22215=CARTESIAN_POINT ( 'NONE',  ( 0.000000000000000000, 0.000000000000000000, 0.000000000000000000 ) ) ;
#22221=EDGE_CURVE ( 'NONE', #39014, #23379, #8078, .T. ) ;
#22222=VERTEX_POINT ( 'NONE', #22922 ) ;
#22225=ORIENTED_EDGE ( 'NONE', *, *, #10847, .T. ) ;
#22227=AXIS2_PLACEMENT_3D ( 'NONE', #25988, #33577, #23707 ) ;
#22232=EDGE_LOOP ( 'NONE', ( #16497, #7112, #41702, #35619 ) ) ;
#22233=AXIS2_PLACEMENT_3D ( 'NONE', #34227, #19522, #8295 ) ;
#22238=EDGE_LOOP ( 'NONE', ( #24924, #1976, #24817, #24751 ) ) ;
#22239=CIRCLE ( 'NONE', #19874, 77.49900000000000944 ) ;
#22251=CARTESIAN_POINT ( 'NONE',  ( 0.000000000000000000, -51.02545421589285723, -55.20638768913812555 ) ) ;
#22252=VERTEX_POINT ( 'NONE', #34651 ) ;
#22258=CARTESIAN_POINT ( 'NONE',  ( 10.00000000000000000, 0.000000000000000000, 0.000000000000000000 ) ) ;
#22267=DIRECTION ( 'NONE',  ( 0.000000000000000000, 0.5877852522924743583, -0.8090169943749466741 ) ) ;
#22272=ADVANCED_FACE ( 'NONE', ( #19475 ), #1134, .T. ) ;
#22276=ADVANCED_FACE ( 'NONE', ( #39565 ), #21171, .T. ) ;
#22292=ORIENTED_EDGE ( 'NONE', *, *, #10784, .F. ) ;
#22301=VECTOR ( 'NONE', #12579, 1000.000000000000000 ) ;
#22305=VECTOR ( 'NONE', #30626, 1000.000000000000000 ) ;
#22310=ORIENTED_EDGE ( 'NONE', *, *, #10041, .F. ) ;
#22320=ORIENTED_EDGE ( 'NONE', *, *, #46546, .T. ) ;
#22324=ORIENTED_EDGE ( 'NONE', *, *, #18901, .T. ) ;
#22330=EDGE_CURVE ( 'NONE', #35415, #28305, #38608, .T. ) ;
#22333=CARTESIAN_POINT ( 'NONE',  ( 0.000000000000000000, 67.80270845531956070, -46.11716303203112943 ) ) ;
#22334=FACE_OUTER_BOUND ( 'NONE', #16679, .T. ) ;
#22335=ORIENTED_EDGE ( 'NONE', *, *, #36543, .T. ) ;
#22340=LINE ( 'NONE', #26491, #15112 ) ;
#22341=DIRECTION ( 'NONE',  ( 0.000000000000000000, 0.000000000000000000, 1.000000000000000000 ) ) ;
#22344=DIRECTION ( 'NONE',  ( 0.000000000000000000, 0.000000000000000000, 1.000000000000000000 ) ) ;
#22348=CARTESIAN_POINT ( 'NONE',  ( -10.00000000000000000, 0.000000000000000000, 0.000000000000000000 ) ) ;
#22349=ORIENTED_EDGE ( 'NONE', *, *, #46120, .T. ) ;
#22353=EDGE_LOOP ( 'NONE', ( #8380, #9641, #20523, #39384 ) ) ;
#22364=ORIENTED_EDGE ( 'NONE', *, *, #42206, .F. ) ;
#22367=ORIENTED_EDGE ( 'NONE', *, *, #31969, .F. ) ;
#22368=CARTESIAN_POINT ( 'NONE',  ( 0.000000000000000000, -51.03279382321048985, -55.19960302592120627 ) ) ;
#22371=VECTOR ( 'NONE', #10276, 1000.000000000000000 ) ;
#22379=ADVANCED_FACE ( 'NONE', ( #32673 ), #20701, .T. ) ;
#22380=DIRECTION ( 'NONE',  ( 1.000000000000000000, 0.000000000000000000, 0.000000000000000000 ) ) ;
#22381=DIRECTION ( 'NONE',  ( -1.000000000000000000, -0.000000000000000000, 0.000000000000000000 ) ) ;
#22384=CARTESIAN_POINT ( 'NONE',  ( 10.00000000000000000, 69.42325613327489009, -34.44570377933524696 ) ) ;
#22388=DIRECTION ( 'NONE',  ( -1.000000000000000000, -0.000000000000000000, -0.000000000000000000 ) ) ;
#22400=CARTESIAN_POINT ( 'NONE',  ( 5.000000000000000000, 21.60688246758696707, -79.10210256391346206 ) ) ;
#22401=DIRECTION ( 'NONE',  ( -1.000000000000000000, -0.000000000000000000, 0.000000000000000000 ) ) ;
#22411=ORIENTED_EDGE ( 'NONE', *, *, #41897, .F. ) ;
#22414=ORIENTED_EDGE ( 'NONE', *, *, #7551, .F. ) ;
#22418=DIRECTION ( 'NONE',  ( -1.000000000000000000, -0.000000000000000000, 0.000000000000000000 ) ) ;
#22419=CARTESIAN_POINT ( 'NONE',  ( 0.000000000000000000, 49.70050353004977239, -59.46389618801908483 ) ) ;
#22420=ORIENTED_EDGE ( 'NONE', *, *, #35910, .F. ) ;
#22427=CARTESIAN_POINT ( 'NONE',  ( 0.000000000000000000, 0.000000000000000000, 0.000000000000000000 ) ) ;
#22432=ORIENTED_EDGE ( 'NONE', *, *, #13327, .T. ) ;
#22442=CIRCLE ( 'NONE', #32590, 31.99999999999999289 ) ;
#22443=ADVANCED_FACE ( 'NONE', ( #36821 ), #349, .T. ) ;
#22445=ORIENTED_EDGE ( 'NONE', *, *, #26378, .F. ) ;
#22446=DIRECTION ( 'NONE',  ( -1.000000000000000000, -0.000000000000000000, 0.000000000000000000 ) ) ;
#22447=LINE ( 'NONE', #33682, #47231 ) ;
#22452=ADVANCED_FACE ( 'NONE', ( #33877 ), #15301, .T. ) ;
#22453=LINE ( 'NONE', #22917, #31204 ) ;
#22459=EDGE_CURVE ( 'NONE', #21525, #23147, #26077, .T. ) ;
#22466=AXIS2_PLACEMENT_3D ( 'NONE', #37864, #11680, #26606 ) ;
#22471=EDGE_CURVE ( 'NONE', #11742, #26881, #29492, .T. ) ;
#22473=ORIENTED_EDGE ( 'NONE', *, *, #34184, .F. ) ;
#22477=CIRCLE ( 'NONE', #40478, 77.49899999999998101 ) ;
#22481=DIRECTION ( 'NONE',  ( 0.000000000000000000, 0.000000000000000000, 1.000000000000000000 ) ) ;
#22482=AXIS2_PLACEMENT_3D ( 'NONE', #41635, #45538, #37968 ) ;
#22484=ORIENTED_EDGE ( 'NONE', *, *, #37903, .F. ) ;
#22487=ADVANCED_FACE ( 'NONE', ( #44423 ), #29251, .T. ) ;
#22495=ORIENTED_EDGE ( 'NONE', *, *, #18986, .T. ) ;
#22503=DIRECTION ( 'NONE',  ( -1.000000000000000000, -0.000000000000000000, -0.000000000000000000 ) ) ;
#22509=AXIS2_PLACEMENT_3D ( 'NONE', #19238, #34387, #41518 ) ;
#22526=AXIS2_PLACEMENT_3D ( 'NONE', #10194, #21453, #36386 ) ;
#22527=VERTEX_POINT ( 'NONE', #44904 ) ;
#22529=ORIENTED_EDGE ( 'NONE', *, *, #15432, .T. ) ;
#22536=DIRECTION ( 'NONE',  ( -1.000000000000000000, 0.000000000000000000, 0.000000000000000000 ) ) ;
#22538=ORIENTED_EDGE ( 'NONE', *, *, #45948, .F. ) ;
#22539=EDGE_CURVE ( 'NONE', #41161, #8489, #47939, .T. ) ;
#22540=DIRECTION ( 'NONE',  ( -1.000000000000000000, 0.000000000000000000, 0.000000000000000000 ) ) ;
#22546=CARTESIAN_POINT ( 'NONE',  ( 0.000000000000000000, 66.50666863322055633, -39.78640506895536078 ) ) ;
#22554=VERTEX_POINT ( 'NONE', #44181 ) ;
#22564=AXIS2_PLACEMENT_3D ( 'NONE', #3817, #7243, #3573 ) ;
#22565=CYLINDRICAL_SURFACE ( 'NONE', #46874, 31.99999999999998579 ) ;
#22572=LINE ( 'NONE', #18420, #4106 ) ;
#22584=ADVANCED_FACE ( 'NONE', ( #7929 ), #1071, .F. ) ;
#22588=VERTEX_POINT ( 'NONE', #30958 ) ;
#22595=VERTEX_POINT ( 'NONE', #8422 ) ;
#22599=DIRECTION ( 'NONE',  ( -1.000000000000000000, -0.000000000000000000, 0.000000000000000000 ) ) ;
#22605=DIRECTION ( 'NONE',  ( 0.000000000000000000, 0.000000000000000000, 1.000000000000000000 ) ) ;
#22606=ORIENTED_EDGE ( 'NONE', *, *, #1513, .T. ) ;
#22609=DIRECTION ( 'NONE',  ( 0.000000000000000000, 0.000000000000000000, -1.000000000000000000 ) ) ;
#22610=EDGE_CURVE ( 'NONE', #3259, #37588, #25267, .T. ) ;
#22613=ORIENTED_EDGE ( 'NONE', *, *, #31929, .T. ) ;
#22615=FACE_OUTER_BOUND ( 'NONE', #42795, .T. ) ;
#22620=LINE ( 'NONE', #37552, #44981 ) ;
#22621=CARTESIAN_POINT ( 'NONE',  ( 10.00000000000000000, -28.89263327155693517, -71.91182617369219088 ) ) ;
#22622=CARTESIAN_POINT ( 'NONE',  ( 0.000000000000000000, 0.000000000000000000, 0.000000000000000000 ) ) ;
#22624=DIRECTION ( 'NONE',  ( -1.000000000000000000, 0.000000000000000000, 0.000000000000000000 ) ) ;
#22626=DIRECTION ( 'NONE',  ( 0.000000000000000000, 0.000000000000000000, 1.000000000000000000 ) ) ;
#22628=CIRCLE ( 'NONE', #37484, 82.00000000000000000 ) ;
#22630=DIRECTION ( 'NONE',  ( -1.000000000000000000, 0.000000000000000000, 0.000000000000000000 ) ) ;
#22633=ORIENTED_EDGE ( 'NONE', *, *, #44281, .F. ) ;
#22636=VERTEX_POINT ( 'NONE', #4286 ) ;
#22640=ORIENTED_EDGE ( 'NONE', *, *, #28411, .F. ) ;
#22641=ADVANCED_FACE ( 'NONE', ( #23584, #38530 ), #19911, .F. ) ;
#22644=CYLINDRICAL_SURFACE ( 'NONE', #21873, 77.49899999999999523 ) ;
#22659=ORIENTED_EDGE ( 'NONE', *, *, #41130, .T. ) ;
#22665=CARTESIAN_POINT ( 'NONE',  ( 0.000000000000000000, 64.81221759200343513, 50.23322058963371006 ) ) ;
#22668=DIRECTION ( 'NONE',  ( -1.000000000000000000, 0.000000000000000000, 0.000000000000000000 ) ) ;
#22669=CARTESIAN_POINT ( 'NONE',  ( 0.000000000000000000, 55.38113227695858143, -54.21277698773617715 ) ) ;
#22670=CARTESIAN_POINT ( 'NONE',  ( 10.00000000000000000, 51.03279382321088065, 55.19960302592086521 ) ) ;
#22672=DIRECTION ( 'NONE',  ( 1.000000000000000000, -0.000000000000000000, 0.000000000000000000 ) ) ;
#22673=LINE ( 'NONE', #11907, #339 ) ;
#22678=DIRECTION ( 'NONE',  ( 0.000000000000000000, 0.000000000000000000, -1.000000000000000000 ) ) ;
#22681=DIRECTION ( 'NONE',  ( -1.000000000000000000, 0.000000000000000000, 0.000000000000000000 ) ) ;
#22683=EDGE_LOOP ( 'NONE', ( #25177, #40324, #39414, #5557 ) ) ;
#22684=DIRECTION ( 'NONE',  ( -1.000000000000000000, 0.000000000000000000, 0.000000000000000000 ) ) ;
#22686=AXIS2_PLACEMENT_3D ( 'NONE', #34088, #26278, #15497 ) ;
#22687=CIRCLE ( 'NONE', #1590, 82.00000000000000000 ) ;
#22688=AXIS2_PLACEMENT_3D ( 'NONE', #20295, #31586, #23992 ) ;
#22689=CARTESIAN_POINT ( 'NONE',  ( -10.00000000000000000, 0.000000000000000000, 0.000000000000000000 ) ) ;
#22690=CARTESIAN_POINT ( 'NONE',  ( 0.000000000000000000, 0.000000000000000000, 0.000000000000000000 ) ) ;
#22693=VERTEX_POINT ( 'NONE', #23348 ) ;
#22694=CIRCLE ( 'NONE', #42224, 31.99999999999999289 ) ;
#22695=EDGE_CURVE ( 'NONE', #32278, #10070, #39375, .T. ) ;
#22697=EDGE_CURVE ( 'NONE', #9926, #42385, #39984, .T. ) ;
#22698=VERTEX_POINT ( 'NONE', #13797 ) ;
#22699=DIRECTION ( 'NONE',  ( -1.000000000000000000, 0.000000000000000000, 0.000000000000000000 ) ) ;
#22701=ORIENTED_EDGE ( 'NONE', *, *, #23060, .T. ) ;
#22703=CARTESIAN_POINT ( 'NONE',  ( 0.000000000000000000, 22.90783923731629912, 78.73519480814962890 ) ) ;
#22717=CARTESIAN_POINT ( 'NONE',  ( 10.00000000000000000, 0.000000000000000000, 0.000000000000000000 ) ) ;
#22723=AXIS2_PLACEMENT_3D ( 'NONE', #24989, #40178, #21314 ) ;
#22725=AXIS2_PLACEMENT_3D ( 'NONE', #7144, #34051, #44585 ) ;
#22733=ORIENTED_EDGE ( 'NONE', *, *, #40596, .T. ) ;
#22748=CIRCLE ( 'NONE', #14160, 31.99999999999999289 ) ;
#22753=EDGE_CURVE ( 'NONE', #42000, #9517, #31589, .T. ) ;
#22754=FACE_OUTER_BOUND ( 'NONE', #34830, .T. ) ;
#22763=EDGE_CURVE ( 'NONE', #23501, #46809, #19855, .T. ) ;
#22780=DIRECTION ( 'NONE',  ( -1.000000000000000000, -0.000000000000000000, -0.000000000000000000 ) ) ;
#22781=DIRECTION ( 'NONE',  ( -1.000000000000000000, 0.000000000000000000, -0.000000000000000000 ) ) ;
#22782=ORIENTED_EDGE ( 'NONE', *, *, #31918, .T. ) ;
#22785=ADVANCED_FACE ( 'NONE', ( #28480 ), #9379, .T. ) ;
#22789=DIRECTION ( 'NONE',  ( 0.000000000000000000, -0.3826834323650772363, -0.9238795325112919565 ) ) ;
#22791=ORIENTED_EDGE ( 'NONE', *, *, #32807, .F. ) ;
#22796=DIRECTION ( 'NONE',  ( -1.000000000000000000, -0.000000000000000000, 0.000000000000000000 ) ) ;
#22797=DIRECTION ( 'NONE',  ( 0.000000000000000000, 0.000000000000000000, 1.000000000000000000 ) ) ;
#22798=DIRECTION ( 'NONE',  ( -1.000000000000000000, 0.000000000000000000, 0.000000000000000000 ) ) ;
#22799=CARTESIAN_POINT ( 'NONE',  ( 10.00000000000000000, 26.02418014898310261, 70.52718814184268581 ) ) ;
#22814=DIRECTION ( 'NONE',  ( 0.000000000000000000, 0.000000000000000000, 1.000000000000000000 ) ) ;
#22826=ADVANCED_FACE ( 'NONE', ( #41192 ), #7646, .T. ) ;
#22830=LINE ( 'NONE', #4479, #20589 ) ;
#22834=CARTESIAN_POINT ( 'NONE',  ( 5.000000000000002665, 40.65526001592612459, 71.21200624218811015 ) ) ;
#22837=CIRCLE ( 'NONE', #14246, 31.99999999999998934 ) ;
#22844=DIRECTION ( 'NONE',  ( -1.000000000000000000, -0.000000000000000000, 0.000000000000000000 ) ) ;
#22846=ORIENTED_EDGE ( 'NONE', *, *, #21804, .F. ) ;
#22848=AXIS2_PLACEMENT_3D ( 'NONE', #29360, #11968, #45484 ) ;
#22849=DIRECTION ( 'NONE',  ( 0.000000000000000000, -0.9238795325112821866, -0.3826834323651006065 ) ) ;
#22850=CARTESIAN_POINT ( 'NONE',  ( 0.000000000000000000, 59.75363087400076267, 56.15606465354979804 ) ) ;
#22858=VECTOR ( 'NONE', #9189, 1000.000000000000000 ) ;
#22859=CARTESIAN_POINT ( 'NONE',  ( 10.00000000000000000, -50.23322058963299241, -64.81221759200398935 ) ) ;
#22867=CARTESIAN_POINT ( 'NONE',  ( 10.00000000000000000, 80.28980883073757013, 16.65972982744963460 ) ) ;
#22875=ORIENTED_EDGE ( 'NONE', *, *, #36782, .F. ) ;
#22877=EDGE_CURVE ( 'NONE', #9486, #1645, #7352, .T. ) ;
#22880=EDGE_CURVE ( 'NONE', #45199, #42057, #15193, .T. ) ;
#22882=AXIS2_PLACEMENT_3D ( 'NONE', #41665, #4234, #26000 ) ;
#22885=DIRECTION ( 'NONE',  ( -1.000000000000000000, -0.000000000000000000, -0.000000000000000000 ) ) ;
#22889=ORIENTED_EDGE ( 'NONE', *, *, #35202, .F. ) ;
#22890=DIRECTION ( 'NONE',  ( 0.000000000000000000, 0.000000000000000000, 1.000000000000000000 ) ) ;
#22902=CARTESIAN_POINT ( 'NONE',  ( 10.00000000000000000, -75.11764819372145041, -2.946379043147127064 ) ) ;
#22905=DIRECTION ( 'NONE',  ( 0.000000000000000000, 0.5224985647159440250, 0.8526401643540951758 ) ) ;
#22906=DIRECTION ( 'NONE',  ( 1.000000000000000000, -0.000000000000000000, -0.000000000000000000 ) ) ;
#22907=DIRECTION ( 'NONE',  ( 0.000000000000000000, 0.000000000000000000, -1.000000000000000000 ) ) ;
#22911=FACE_OUTER_BOUND ( 'NONE', #22055, .T. ) ;
#22913=DIRECTION ( 'NONE',  ( 0.000000000000000000, 0.4539904997395413644, 0.8910065241883706744 ) ) ;
#22914=EDGE_CURVE ( 'NONE', #38308, #3813, #28943, .T. ) ;
#22917=CARTESIAN_POINT ( 'NONE',  ( 5.000000000000002665, 22.90783923731741112, -78.73519480814930205 ) ) ;
#22920=DIRECTION ( 'NONE',  ( -1.000000000000000000, 0.000000000000000000, 0.000000000000000000 ) ) ;
#22922=CARTESIAN_POINT ( 'NONE',  ( 10.00000000000000000, 24.73286445877703699, 73.44644590900070114 ) ) ;
#22923=EDGE_CURVE ( 'NONE', #10549, #8725, #17921, .T. ) ;
#22924=DIRECTION ( 'NONE',  ( 0.000000000000000000, 0.000000000000000000, 1.000000000000000000 ) ) ;
#22925=DIRECTION ( 'NONE',  ( -1.000000000000000000, 0.000000000000000000, -0.000000000000000000 ) ) ;
#22927=CARTESIAN_POINT ( 'NONE',  ( 0.000000000000000000, 49.70050353004889132, 59.46389618801982380 ) ) ;
#22928=CARTESIAN_POINT ( 'NONE',  ( 10.00000000000000000, 54.21277698773675979, 55.38113227695801299 ) ) ;
#22932=EDGE_CURVE ( 'NONE', #42951, #19820, #14389, .T. ) ;
#22941=AXIS2_PLACEMENT_3D ( 'NONE', #21343, #36280, #2745 ) ;
#22942=VECTOR ( 'NONE', #18893, 1000.000000000000000 ) ;
#22947=ADVANCED_FACE ( 'NONE', ( #10604 ), #11077, .T. ) ;
#22949=CARTESIAN_POINT ( 'NONE',  ( 10.00000000000000000, -26.02418014898359289, 70.52718814184250107 ) ) ;
#22953=CYLINDRICAL_SURFACE ( 'NONE', #46848, 77.49899999999999523 ) ;
#22958=ORIENTED_EDGE ( 'NONE', *, *, #27583, .T. ) ;
#22961=AXIS2_PLACEMENT_3D ( 'NONE', #32438, #2802, #17737 ) ;
#22965=CARTESIAN_POINT ( 'NONE',  ( 0.000000000000000000, 0.000000000000000000, 0.000000000000000000 ) ) ;
#22968=DIRECTION ( 'NONE',  ( 0.000000000000000000, 0.000000000000000000, 1.000000000000000000 ) ) ;
#22969=EDGE_CURVE ( 'NONE', #6182, #40126, #26897, .T. ) ;
#22973=EDGE_LOOP ( 'NONE', ( #5109, #24348, #34028, #13201 ) ) ;
#22977=AXIS2_PLACEMENT_3D ( 'NONE', #48221, #14701, #10058 ) ;
#22978=DIRECTION ( 'NONE',  ( -1.000000000000000000, 0.000000000000000000, 0.000000000000000000 ) ) ;
#22987=DIRECTION ( 'NONE',  ( 0.000000000000000000, 0.000000000000000000, 1.000000000000000000 ) ) ;
#23003=CARTESIAN_POINT ( 'NONE',  ( 0.000000000000000000, -2.543863470247813119, -81.96053171279905314 ) ) ;
#23009=VECTOR ( 'NONE', #36940, 1000.000000000000000 ) ;
#23010=AXIS2_PLACEMENT_3D ( 'NONE', #11449, #7754, #26365 ) ;
#23012=VECTOR ( 'NONE', #17580, 1000.000000000000000 ) ;
#23015=ORIENTED_EDGE ( 'NONE', *, *, #20353, .T. ) ;
#23020=VERTEX_POINT ( 'NONE', #27458 ) ;
#23024=CARTESIAN_POINT ( 'NONE',  ( 10.00000000000000000, -29.01471420065617224, 76.69515212746006227 ) ) ;
#23025=ORIENTED_EDGE ( 'NONE', *, *, #10172, .T. ) ;
#23029=ORIENTED_EDGE ( 'NONE', *, *, #8493, .T. ) ;
#23041=DIRECTION ( 'NONE',  ( -1.000000000000000000, 0.000000000000000000, 0.000000000000000000 ) ) ;
#23043=CARTESIAN_POINT ( 'NONE',  ( 5.000000000000002665, -2.543863470248944214, 81.96053171279901051 ) ) ;
#23046=CYLINDRICAL_SURFACE ( 'NONE', #38049, 31.99999999999999289 ) ;
#23050=ADVANCED_FACE ( 'NONE', ( #27220 ), #11568, .T. ) ;
#23059=CIRCLE ( 'NONE', #12139, 82.00000000000000000 ) ;
#23060=EDGE_CURVE ( 'NONE', #23124, #10502, #41019, .T. ) ;
#23063=EDGE_CURVE ( 'NONE', #36193, #22222, #37867, .T. ) ;
#23064=CARTESIAN_POINT ( 'NONE',  ( 10.00000000000000000, 14.66109333815460225, 73.73191006444577056 ) ) ;
#23066=LINE ( 'NONE', #7654, #22942 ) ;
#23070=AXIS2_PLACEMENT_3D ( 'NONE', #28983, #47817, #47582 ) ;
#23071=VERTEX_POINT ( 'NONE', #4223 ) ;
#23079=CARTESIAN_POINT ( 'NONE',  ( 0.000000000000000000, 46.21855187248719687, -62.20884554313968806 ) ) ;
#23082=ORIENTED_EDGE ( 'NONE', *, *, #17025, .F. ) ;
#23084=AXIS2_PLACEMENT_3D ( 'NONE', #15928, #31107, #30866 ) ;
#23090=AXIS2_PLACEMENT_3D ( 'NONE', #39979, #21609, #24561 ) ;
#23095=ADVANCED_FACE ( 'NONE', ( #34297 ), #12054, .T. ) ;
#23099=CIRCLE ( 'NONE', #4354, 31.99999999999999289 ) ;
#23104=DIRECTION ( 'NONE',  ( -1.000000000000000000, 0.000000000000000000, -0.000000000000000000 ) ) ;
#23112=ADVANCED_FACE ( 'NONE', ( #9553 ), #28404, .T. ) ;
#23117=VECTOR ( 'NONE', #3133, 1000.000000000000000 ) ;
#23121=AXIS2_PLACEMENT_3D ( 'NONE', #32668, #6733, #21659 ) ;
#23122=FACE_OUTER_BOUND ( 'NONE', #46102, .T. ) ;
#23124=VERTEX_POINT ( 'NONE', #13020 ) ;
#23126=ORIENTED_EDGE ( 'NONE', *, *, #10123, .T. ) ;
#23138=VERTEX_POINT ( 'NONE', #13731 ) ;
#23140=VERTEX_POINT ( 'NONE', #2224 ) ;
#23141=CIRCLE ( 'NONE', #36421, 31.99999999999998579 ) ;
#23143=CARTESIAN_POINT ( 'NONE',  ( 0.000000000000000000, -74.65374052328644439, -8.840884882375878107 ) ) ;
#23147=VERTEX_POINT ( 'NONE', #31384 ) ;
#23150=EDGE_CURVE ( 'NONE', #40126, #32923, #6584, .T. ) ;
#23163=EDGE_LOOP ( 'NONE', ( #12138, #20678, #24604, #24055 ) ) ;
#23174=LINE ( 'NONE', #30761, #3383 ) ;
#23189=ORIENTED_EDGE ( 'NONE', *, *, #19450, .T. ) ;
#23191=VECTOR ( 'NONE', #16139, 1000.000000000000000 ) ;
#23192=DIRECTION ( 'NONE',  ( 1.000000000000000000, 0.000000000000000000, 0.000000000000000000 ) ) ;
#23194=ORIENTED_EDGE ( 'NONE', *, *, #4046, .F. ) ;
#23195=VERTEX_POINT ( 'NONE', #46544 ) ;
#23198=DIRECTION ( 'NONE',  ( -1.000000000000000000, 0.000000000000000000, -0.000000000000000000 ) ) ;
#23199=DIRECTION ( 'NONE',  ( 0.000000000000000000, 0.000000000000000000, 1.000000000000000000 ) ) ;
#23205=ORIENTED_EDGE ( 'NONE', *, *, #2107, .T. ) ;
#23208=DIRECTION ( 'NONE',  ( 0.000000000000000000, 1.000000000000000000, 0.000000000000000000 ) ) ;
#23209=CARTESIAN_POINT ( 'NONE',  ( 0.000000000000000000, -81.34940948281344220, 10.30890764327356557 ) ) ;
#23210=EDGE_CURVE ( 'NONE', #31534, #14555, #21473, .T. ) ;
#23211=DIRECTION ( 'NONE',  ( 1.000000000000000000, 0.000000000000000000, 0.000000000000000000 ) ) ;
#23213=EDGE_CURVE ( 'NONE', #29530, #43468, #29266, .T. ) ;
#23215=ORIENTED_EDGE ( 'NONE', *, *, #29244, .T. ) ;
#23222=VERTEX_POINT ( 'NONE', #31871 ) ;
#23224=DIRECTION ( 'NONE',  ( -1.000000000000000000, -0.000000000000000000, 0.000000000000000000 ) ) ;
#23229=DIRECTION ( 'NONE',  ( -1.000000000000000000, 0.000000000000000000, -0.000000000000000000 ) ) ;
#23231=CARTESIAN_POINT ( 'NONE',  ( 0.000000000000000000, -59.75363087400035056, -56.15606465355021015 ) ) ;
#23234=CARTESIAN_POINT ( 'NONE',  ( 10.00000000000000000, 0.000000000000000000, 0.000000000000000000 ) ) ;
#23235=VERTEX_POINT ( 'NONE', #38727 ) ;
#23242=ORIENTED_EDGE ( 'NONE', *, *, #46467, .F. ) ;
#23245=DIRECTION ( 'NONE',  ( -1.000000000000000000, 0.000000000000000000, -0.000000000000000000 ) ) ;
#23255=ADVANCED_FACE ( 'NONE', ( #29376 ), #40158, .T. ) ;
#23259=ORIENTED_EDGE ( 'NONE', *, *, #2769, .T. ) ;
#23260=EDGE_CURVE ( 'NONE', #34421, #13155, #3165, .T. ) ;
#23265=ORIENTED_EDGE ( 'NONE', *, *, #30710, .T. ) ;
#23275=CARTESIAN_POINT ( 'NONE',  ( 0.000000000000000000, -8.840884882374576037, -74.65374052328658649 ) ) ;
#23276=CYLINDRICAL_SURFACE ( 'NONE', #33653, 77.49899999999999523 ) ;
#23279=EDGE_LOOP ( 'NONE', ( #24593, #24759, #30800, #45690 ) ) ;
#23288=EDGE_CURVE ( 'NONE', #37280, #25536, #18352, .T. ) ;
#23290=AXIS2_PLACEMENT_3D ( 'NONE', #31116, #43984, #10452 ) ;
#23291=ORIENTED_EDGE ( 'NONE', *, *, #3087, .F. ) ;
#23295=ORIENTED_EDGE ( 'NONE', *, *, #25354, .F. ) ;
#23297=LINE ( 'NONE', #12296, #26028 ) ;
#23299=DIRECTION ( 'NONE',  ( -1.000000000000000000, -0.000000000000000000, 0.000000000000000000 ) ) ;
#23304=CARTESIAN_POINT ( 'NONE',  ( 10.00000000000000000, -71.27951684758046724, 30.41916302227088309 ) ) ;
#23306=CARTESIAN_POINT ( 'NONE',  ( 10.00000000000000000, 59.03342792756328095, -46.54456581323744757 ) ) ;
#23312=EDGE_CURVE ( 'NONE', #39764, #34627, #18097, .T. ) ;
#23316=CARTESIAN_POINT ( 'NONE',  ( 0.000000000000000000, 56.15606465355042332, -59.75363087400017292 ) ) ;
#23322=CARTESIAN_POINT ( 'NONE',  ( 10.00000000000000000, 81.50828551894240093, -8.966570791699799869 ) ) ;
#23327=VERTEX_POINT ( 'NONE', #7089 ) ;
#23340=AXIS2_PLACEMENT_3D ( 'NONE', #11334, #7409, #22344 ) ;
#23341=CARTESIAN_POINT ( 'NONE',  ( 10.00000000000000000, 62.20884554314086046, -46.21855187248561236 ) ) ;
#23342=EDGE_CURVE ( 'NONE', #25836, #919, #22015, .T. ) ;
#23348=CARTESIAN_POINT ( 'NONE',  ( 10.00000000000000000, 76.69515212746057387, -29.01471420065480089 ) ) ;
#23353=AXIS2_PLACEMENT_3D ( 'NONE', #35222, #39650, #6109 ) ;
#23354=VERTEX_POINT ( 'NONE', #14692 ) ;
#23357=AXIS2_PLACEMENT_3D ( 'NONE', #48410, #37403, #33963 ) ;
#23358=CYLINDRICAL_SURFACE ( 'NONE', #44010, 31.99999999999999289 ) ;
#23364=VERTEX_POINT ( 'NONE', #17626 ) ;
#23367=FACE_OUTER_BOUND ( 'NONE', #37214, .T. ) ;
#23370=CARTESIAN_POINT ( 'NONE',  ( 0.000000000000000000, -74.74816331893404708, -33.71516098798818462 ) ) ;
#23374=ORIENTED_EDGE ( 'NONE', *, *, #18417, .T. ) ;
#23377=CARTESIAN_POINT ( 'NONE',  ( 10.00000000000000000, -62.50884508063395373, -41.76106447765554464 ) ) ;
#23379=VERTEX_POINT ( 'NONE', #25199 ) ;
#23381=DIRECTION ( 'NONE',  ( 0.000000000000000000, 0.000000000000000000, 1.000000000000000000 ) ) ;
#23385=LINE ( 'NONE', #7967, #39751 ) ;
#23390=DIRECTION ( 'NONE',  ( -1.000000000000000000, 0.000000000000000000, 0.000000000000000000 ) ) ;
#23396=ORIENTED_EDGE ( 'NONE', *, *, #15094, .F. ) ;
#23405=CARTESIAN_POINT ( 'NONE',  ( 10.00000000000000000, 0.000000000000000000, 0.000000000000000000 ) ) ;
#23406=ADVANCED_FACE ( 'NONE', ( #15650 ), #8055, .T. ) ;
#23411=ORIENTED_EDGE ( 'NONE', *, *, #14040, .T. ) ;
#23412=FILL_AREA_STYLE ('',( #19013 ) ) ;
#23417=AXIS2_PLACEMENT_3D ( 'NONE', #32000, #46917, #13383 ) ;
#23419=ORIENTED_EDGE ( 'NONE', *, *, #21084, .T. ) ;
#23421=CYLINDRICAL_SURFACE ( 'NONE', #32002, 82.00000000000000000 ) ;
#23425=VECTOR ( 'NONE', #7130, 1000.000000000000000 ) ;
#23430=ORIENTED_EDGE ( 'NONE', *, *, #38916, .T. ) ;
#23432=CARTESIAN_POINT ( 'NONE',  ( 10.00000000000000000, 8.966570791701860443, -81.50828551894217355 ) ) ;
#23434=DIRECTION ( 'NONE',  ( 0.000000000000000000, 0.000000000000000000, 1.000000000000000000 ) ) ;
#23435=ORIENTED_EDGE ( 'NONE', *, *, #44123, .F. ) ;
#23438=ORIENTED_EDGE ( 'NONE', *, *, #15832, .F. ) ;
#23439=DIRECTION ( 'NONE',  ( 0.000000000000000000, 0.000000000000000000, 1.000000000000000000 ) ) ;
#23442=CARTESIAN_POINT ( 'NONE',  ( 0.000000000000000000, 31.47745569255140552, 68.26794271651274926 ) ) ;
#23444=EDGE_LOOP ( 'NONE', ( #11291, #2925, #47225, #36346 ) ) ;
#23448=CARTESIAN_POINT ( 'NONE',  ( 10.00000000000000000, -46.54456581323762521, -59.03342792756313884 ) ) ;
#23450=AXIS2_PLACEMENT_3D ( 'NONE', #28504, #43440, #9896 ) ;
#23451=DIRECTION ( 'NONE',  ( -1.000000000000000000, 0.000000000000000000, -0.000000000000000000 ) ) ;
#23452=ORIENTED_EDGE ( 'NONE', *, *, #42379, .T. ) ;
#23456=CARTESIAN_POINT ( 'NONE',  ( 0.000000000000000000, 0.000000000000000000, 0.000000000000000000 ) ) ;
#23460=CYLINDRICAL_SURFACE ( 'NONE', #27059, 77.49899999999999523 ) ;
#23471=ORIENTED_EDGE ( 'NONE', *, *, #45144, .F. ) ;
#23475=ORIENTED_EDGE ( 'NONE', *, *, #22221, .T. ) ;
#23476=EDGE_CURVE ( 'NONE', #44907, #23020, #28540, .T. ) ;
#23481=CARTESIAN_POINT ( 'NONE',  ( 0.000000000000000000, 0.000000000000000000, 0.000000000000000000 ) ) ;
#23482=AXIS2_PLACEMENT_3D ( 'NONE', #37058, #17734, #43921 ) ;
#23483=AXIS2_PLACEMENT_3D ( 'NONE', #25952, #33774, #30601 ) ;
#23485=EDGE_LOOP ( 'NONE', ( #17192, #10614, #19246, #24510 ) ) ;
#23489=ORIENTED_EDGE ( 'NONE', *, *, #23902, .T. ) ;
#23497=CARTESIAN_POINT ( 'NONE',  ( 0.000000000000000000, 62.50884508063487033, -41.76106447765422303 ) ) ;
#23501=VERTEX_POINT ( 'NONE', #37442 ) ;
#23506=CARTESIAN_POINT ( 'NONE',  ( 10.00000000000000000, 0.000000000000000000, 0.000000000000000000 ) ) ;
#23507=ORIENTED_EDGE ( 'NONE', *, *, #2631, .F. ) ;
#23511=DIRECTION ( 'NONE',  ( -1.000000000000000000, -0.000000000000000000, 0.000000000000000000 ) ) ;
#23517=CYLINDRICAL_SURFACE ( 'NONE', #14603, 31.99999999999998579 ) ;
#23525=ADVANCED_FACE ( 'NONE', ( #36360 ), #13860, .T. ) ;
#23536=ORIENTED_EDGE ( 'NONE', *, *, #3294, .T. ) ;
#23545=SURFACE_STYLE_USAGE ( .BOTH. , #24520 ) ;
#23553=ORIENTED_EDGE ( 'NONE', *, *, #44695, .T. ) ;
#23556=ORIENTED_EDGE ( 'NONE', *, *, #11506, .F. ) ;
#23558=CARTESIAN_POINT ( 'NONE',  ( 10.00000000000000000, 55.20638768913831029, -51.02545421589267960 ) ) ;
#23563=DIRECTION ( 'NONE',  ( 0.000000000000000000, -0.8090169943749403458, -0.5877852522924830181 ) ) ;
#23564=ORIENTED_EDGE ( 'NONE', *, *, #41830, .T. ) ;
#23566=AXIS2_PLACEMENT_3D ( 'NONE', #41462, #7682, #810 ) ;
#23573=CARTESIAN_POINT ( 'NONE',  ( 5.000000000000000000, 27.74655509720779634, -77.16300072079631889 ) ) ;
#23574=DIRECTION ( 'NONE',  ( 0.000000000000000000, 0.000000000000000000, 1.000000000000000000 ) ) ;
#23575=DIRECTION ( 'NONE',  ( -1.000000000000000000, 0.000000000000000000, -0.000000000000000000 ) ) ;
#23576=DIRECTION ( 'NONE',  ( 0.000000000000000000, -0.8910065241883627918, -0.4539904997395570185 ) ) ;
#23578=ADVANCED_FACE ( 'NONE', ( #21674 ), #36594, .T. ) ;
#23582=EDGE_CURVE ( 'NONE', #22554, #43090, #3058, .T. ) ;
#23583=CARTESIAN_POINT ( 'NONE',  ( 10.00000000000000000, -74.65374052328644439, -8.840884882375878107 ) ) ;
#23584=FACE_BOUND ( 'NONE', #15219, .T. ) ;
#23585=EDGE_CURVE ( 'NONE', #29746, #24479, #6501, .T. ) ;
#23589=CARTESIAN_POINT ( 'NONE',  ( 10.00000000000000000, 0.000000000000000000, 0.000000000000000000 ) ) ;
#23594=AXIS2_PLACEMENT_3D ( 'NONE', #13512, #28439, #31167 ) ;
#23595=CIRCLE ( 'NONE', #36868, 77.49900000000000944 ) ;
#23597=CIRCLE ( 'NONE', #15014, 82.00000000000000000 ) ;
#23598=ORIENTED_EDGE ( 'NONE', *, *, #18817, .F. ) ;
#23600=EDGE_CURVE ( 'NONE', #21412, #45983, #12130, .T. ) ;
#23604=ORIENTED_EDGE ( 'NONE', *, *, #23886, .F. ) ;
#23611=ORIENTED_EDGE ( 'NONE', *, *, #16492, .F. ) ;
#23617=DIRECTION ( 'NONE',  ( 0.000000000000000000, 0.000000000000000000, 1.000000000000000000 ) ) ;
#23619=ORIENTED_EDGE ( 'NONE', *, *, #47557, .F. ) ;
#23633=CARTESIAN_POINT ( 'NONE',  ( 10.00000000000000000, 28.89263327155850902, -71.91182617369157981 ) ) ;
#23637=ORIENTED_EDGE ( 'NONE', *, *, #47416, .F. ) ;
#23640=EDGE_CURVE ( 'NONE', #41545, #45965, #9937, .T. ) ;
#23641=CARTESIAN_POINT ( 'NONE',  ( 0.000000000000000000, 0.000000000000000000, 0.000000000000000000 ) ) ;
#23644=EDGE_CURVE ( 'NONE', #3739, #17812, #46501, .T. ) ;
#23655=CARTESIAN_POINT ( 'NONE',  ( 0.000000000000000000, -68.26794271651286294, 31.47745569255117104 ) ) ;
#23656=ORIENTED_EDGE ( 'NONE', *, *, #1437, .F. ) ;
#23658=VECTOR ( 'NONE', #40688, 1000.000000000000000 ) ;
#23659=AXIS2_PLACEMENT_3D ( 'NONE', #19698, #19955, #1854 ) ;
#23664=AXIS2_PLACEMENT_3D ( 'NONE', #8514, #45980, #12445 ) ;
#23671=CARTESIAN_POINT ( 'NONE',  ( 10.00000000000000000, -74.65491531819111515, 23.16904090965678975 ) ) ;
#23674=ORIENTED_EDGE ( 'NONE', *, *, #8142, .F. ) ;
#23675=CARTESIAN_POINT ( 'NONE',  ( 10.00000000000000000, 65.59268652807263322, -36.72794159290169347 ) ) ;
#23677=EDGE_CURVE ( 'NONE', #31653, #14555, #44188, .T. ) ;
#23678=DIRECTION ( 'NONE',  ( -1.000000000000000000, -0.000000000000000000, -0.000000000000000000 ) ) ;
#23684=CARTESIAN_POINT ( 'NONE',  ( 10.00000000000000000, 20.40083707022882820, 72.35432306680490910 ) ) ;
#23687=LINE ( 'NONE', #9720, #44794 ) ;
#23688=CIRCLE ( 'NONE', #15869, 77.49900000000000944 ) ;
#23689=CARTESIAN_POINT ( 'NONE',  ( 10.00000000000000000, -18.89407956138310496, 75.16055320797023853 ) ) ;
#23694=VERTEX_POINT ( 'NONE', #44428 ) ;
#23699=CIRCLE ( 'NONE', #33857, 31.99999999999998224 ) ;
#23701=AXIS2_PLACEMENT_3D ( 'NONE', #39838, #44461, #25370 ) ;
#23702=CARTESIAN_POINT ( 'NONE',  ( 5.000000000000002665, -81.34940948281328588, -10.30890764327469711 ) ) ;
#23707=DIRECTION ( 'NONE',  ( 0.000000000000000000, 0.6494480483301793283, 0.7604059656000345946 ) ) ;
#23711=LINE ( 'NONE', #1689, #15391 ) ;
#23719=EDGE_LOOP ( 'NONE', ( #23489, #8593, #22875, #1730 ) ) ;
#23728=ORIENTED_EDGE ( 'NONE', *, *, #15979, .F. ) ;
#23729=ORIENTED_EDGE ( 'NONE', *, *, #41308, .F. ) ;
#23732=CARTESIAN_POINT ( 'NONE',  ( 10.00000000000000000, 35.91791733033570466, -68.67312586194960033 ) ) ;
#23734=CIRCLE ( 'NONE', #37015, 82.00000000000000000 ) ;
#23735=VECTOR ( 'NONE', #7465, 1000.000000000000000 ) ;
#23745=VERTEX_POINT ( 'NONE', #18945 ) ;
#23747=ORIENTED_EDGE ( 'NONE', *, *, #28789, .T. ) ;
#23749=CARTESIAN_POINT ( 'NONE',  ( 0.000000000000000000, 46.11716303203188261, 67.80270845531904911 ) ) ;
#23751=DIRECTION ( 'NONE',  ( -1.000000000000000000, 0.000000000000000000, -0.000000000000000000 ) ) ;
#23754=ADVANCED_FACE ( 'NONE', ( #33640 ), #7702, .T. ) ;
#23763=AXIS2_PLACEMENT_3D ( 'NONE', #10477, #21960, #33703 ) ;
#23768=CARTESIAN_POINT ( 'NONE',  ( 10.00000000000000000, 70.53064760720316428, -26.01480285779861035 ) ) ;
#23772=AXIS2_PLACEMENT_3D ( 'NONE', #48332, #14812, #25325 ) ;
#23785=CARTESIAN_POINT ( 'NONE',  ( 10.00000000000000000, 31.47745569255237896, -68.26794271651228030 ) ) ;
#23789=VECTOR ( 'NONE', #5524, 1000.000000000000000 ) ;
#23793=ORIENTED_EDGE ( 'NONE', *, *, #11221, .T. ) ;
#23795=CARTESIAN_POINT ( 'NONE',  ( -10.00000000000000000, 0.000000000000000000, 0.000000000000000000 ) ) ;
#23798=EDGE_CURVE ( 'NONE', #18377, #39100, #29979, .T. ) ;
#23802=CARTESIAN_POINT ( 'NONE',  ( 0.000000000000000000, -41.76937507738745836, -62.50329211542482710 ) ) ;
#23805=EDGE_CURVE ( 'NONE', #44086, #33547, #24655, .T. ) ;
#23809=FACE_OUTER_BOUND ( 'NONE', #2547, .T. ) ;
#23811=LINE ( 'NONE', #19632, #29844 ) ;
#23814=CIRCLE ( 'NONE', #40244, 77.49900000000000944 ) ;
#23817=DIRECTION ( 'NONE',  ( -1.000000000000000000, 0.000000000000000000, 0.000000000000000000 ) ) ;
#23818=VERTEX_POINT ( 'NONE', #32370 ) ;
#23822=CIRCLE ( 'NONE', #44804, 31.99999999999999289 ) ;
#23831=CARTESIAN_POINT ( 'NONE',  ( 0.000000000000000000, -75.11725578898466438, -2.956366410621452001 ) ) ;
#23832=EDGE_CURVE ( 'NONE', #33124, #9519, #11393, .T. ) ;
#23840=ORIENTED_EDGE ( 'NONE', *, *, #19269, .F. ) ;
#23842=CARTESIAN_POINT ( 'NONE',  ( 10.00000000000000000, 59.03342792756263435, 46.54456581323825048 ) ) ;
#23855=ORIENTED_EDGE ( 'NONE', *, *, #18980, .T. ) ;
#23866=EDGE_CURVE ( 'NONE', #17444, #43536, #25404, .T. ) ;
#23867=VERTEX_POINT ( 'NONE', #2733 ) ;
#23869=LINE ( 'NONE', #38817, #14543 ) ;
#23873=ORIENTED_EDGE ( 'NONE', *, *, #25333, .F. ) ;
#23877=CARTESIAN_POINT ( 'NONE',  ( 10.00000000000000000, 0.000000000000000000, 0.000000000000000000 ) ) ;
#23879=DIRECTION ( 'NONE',  ( -1.000000000000000000, -0.000000000000000000, 0.000000000000000000 ) ) ;
#23880=CARTESIAN_POINT ( 'NONE',  ( 10.00000000000000000, 77.32052557432841411, 5.256550761633138613 ) ) ;
#23884=ADVANCED_FACE ( 'NONE', ( #39479 ), #5953, .T. ) ;
#23885=ORIENTED_EDGE ( 'NONE', *, *, #10328, .F. ) ;
#23886=EDGE_CURVE ( 'NONE', #44567, #38630, #10578, .T. ) ;
#23893=ORIENTED_EDGE ( 'NONE', *, *, #4266, .T. ) ;
#23898=CIRCLE ( 'NONE', #29378, 31.99999999999999645 ) ;
#23899=AXIS2_PLACEMENT_3D ( 'NONE', #9063, #35961, #5632 ) ;
#23901=FACE_OUTER_BOUND ( 'NONE', #33724, .T. ) ;
#23902=EDGE_CURVE ( 'NONE', #21501, #44761, #28203, .T. ) ;
#23908=AXIS2_PLACEMENT_3D ( 'NONE', #23377, #27797, #42722 ) ;
#23915=VERTEX_POINT ( 'NONE', #43144 ) ;
#23924=ADVANCED_FACE ( 'NONE', ( #21333 ), #21088, .T. ) ;
#23926=CIRCLE ( 'NONE', #38791, 31.99999999999999289 ) ;
#23928=CIRCLE ( 'NONE', #36431, 32.00000000000000711 ) ;
#23929=EDGE_CURVE ( 'NONE', #45282, #23124, #44184, .T. ) ;
#23930=DIRECTION ( 'NONE',  ( -1.000000000000000000, -0.000000000000000000, 0.000000000000000000 ) ) ;
#23932=ORIENTED_EDGE ( 'NONE', *, *, #31584, .T. ) ;
#23936=CIRCLE ( 'NONE', #35642, 82.00000000000000000 ) ;
#23938=EDGE_CURVE ( 'NONE', #47062, #40883, #30921, .T. ) ;
#23944=AXIS2_PLACEMENT_3D ( 'NONE', #40221, #47772, #14019 ) ;
#23945=DIRECTION ( 'NONE',  ( -1.000000000000000000, 0.000000000000000000, 0.000000000000000000 ) ) ;
#23946=CARTESIAN_POINT ( 'NONE',  ( 10.00000000000000000, -8.966570791701267140, 81.50828551894223040 ) ) ;
#23947=DIRECTION ( 'NONE',  ( -1.000000000000000000, 0.000000000000000000, 0.000000000000000000 ) ) ;
#23952=DIRECTION ( 'NONE',  ( -1.000000000000000000, -0.000000000000000000, -0.000000000000000000 ) ) ;
#23955=EDGE_LOOP ( 'NONE', ( #3452, #30646, #40973, #36804 ) ) ;
#23959=DIRECTION ( 'NONE',  ( 0.000000000000000000, 0.3090169943749410120, 0.9510565162951556406 ) ) ;
#23976=CARTESIAN_POINT ( 'NONE',  ( 10.00000000000000000, -28.89263327155797967, 71.91182617369179297 ) ) ;
#23979=FACE_OUTER_BOUND ( 'NONE', #39165, .T. ) ;
#23980=AXIS2_PLACEMENT_3D ( 'NONE', #883, #30762, #22924 ) ;
#23981=FACE_OUTER_BOUND ( 'NONE', #10021, .T. ) ;
#23988=ORIENTED_EDGE ( 'NONE', *, *, #34639, .F. ) ;
#23991=CIRCLE ( 'NONE', #47435, 77.49899999999999523 ) ;
#23992=DIRECTION ( 'NONE',  ( 0.000000000000000000, -0.7071067811865536790, 0.7071067811865414665 ) ) ;
#23995=EDGE_CURVE ( 'NONE', #19224, #15249, #10862, .T. ) ;
#23997=CYLINDRICAL_SURFACE ( 'NONE', #14174, 31.99999999999999289 ) ;
#24000=CYLINDRICAL_SURFACE ( 'NONE', #8000, 31.99999999999999289 ) ;
#24003=ORIENTED_EDGE ( 'NONE', *, *, #436, .F. ) ;
#24005=CARTESIAN_POINT ( 'NONE',  ( 10.00000000000000000, 71.91182617369189245, 28.89263327155772743 ) ) ;
#24008=DIRECTION ( 'NONE',  ( 0.000000000000000000, -0.8910065241883722287, 0.4539904997395383668 ) ) ;
#24013=CARTESIAN_POINT ( 'NONE',  ( 10.00000000000000000, 79.10210256391367523, 21.60688246758613218 ) ) ;
#24014=DIRECTION ( 'NONE',  ( -1.000000000000000000, 0.000000000000000000, 0.000000000000000000 ) ) ;
#24015=CARTESIAN_POINT ( 'NONE',  ( -10.00000000000000000, 0.000000000000000000, 0.000000000000000000 ) ) ;
#24019=AXIS2_PLACEMENT_3D ( 'NONE', #3055, #25570, #40516 ) ;
#24025=FACE_OUTER_BOUND ( 'NONE', #19229, .T. ) ;
#24027=DIRECTION ( 'NONE',  ( 0.000000000000000000, -0.7071067811865389130, -0.7071067811865561215 ) ) ;
#24033=AXIS2_PLACEMENT_3D ( 'NONE', #29489, #10402, #40277 ) ;
#24040=ORIENTED_EDGE ( 'NONE', *, *, #2877, .T. ) ;
#24045=CARTESIAN_POINT ( 'NONE',  ( 5.000000000000002665, -68.55367621811173251, 44.99326035066031437 ) ) ;
#24047=FACE_OUTER_BOUND ( 'NONE', #47797, .T. ) ;
#24049=AXIS2_PLACEMENT_3D ( 'NONE', #13961, #7091, #14693 ) ;
#24050=DIRECTION ( 'NONE',  ( 0.000000000000000000, 0.000000000000000000, 1.000000000000000000 ) ) ;
#24051=EDGE_CURVE ( 'NONE', #5642, #10514, #9039, .T. ) ;
#24052=CARTESIAN_POINT ( 'NONE',  ( 10.00000000000000000, -11.30684508768284680, -76.66974797899850103 ) ) ;
#24053=ORIENTED_EDGE ( 'NONE', *, *, #42458, .T. ) ;
#24054=DIRECTION ( 'NONE',  ( -1.000000000000000000, 0.000000000000000000, -0.000000000000000000 ) ) ;
#24055=ORIENTED_EDGE ( 'NONE', *, *, #6152, .T. ) ;
#24058=ORIENTED_EDGE ( 'NONE', *, *, #14087, .T. ) ;
#24060=CARTESIAN_POINT ( 'NONE',  ( 0.000000000000000000, -14.67089635893658794, -73.72996012237454977 ) ) ;
#24068=DIRECTION ( 'NONE',  ( -1.000000000000000000, -0.000000000000000000, 0.000000000000000000 ) ) ;
#24069=VERTEX_POINT ( 'NONE', #36324 ) ;
#24070=CARTESIAN_POINT ( 'NONE',  ( 10.00000000000000000, 6.903761155837774943, 77.19088730480525840 ) ) ;
#24083=CARTESIAN_POINT ( 'NONE',  ( 10.00000000000000000, -68.27212725128298132, 31.46837873494953541 ) ) ;
#24087=CARTESIAN_POINT ( 'NONE',  ( 5.000000000000002665, 22.90783923731629912, 78.73519480814962890 ) ) ;
#24088=VERTEX_POINT ( 'NONE', #10372 ) ;
#24090=EDGE_CURVE ( 'NONE', #31305, #12188, #10629, .T. ) ;
#24091=LINE ( 'NONE', #20398, #27593 ) ;
#24092=ORIENTED_EDGE ( 'NONE', *, *, #29985, .T. ) ;
#24094=DIRECTION ( 'NONE',  ( 0.000000000000000000, 0.000000000000000000, 1.000000000000000000 ) ) ;
#24096=ORIENTED_EDGE ( 'NONE', *, *, #24919, .F. ) ;
#24097=ADVANCED_FACE ( 'NONE', ( #44630 ), #21638, .T. ) ;
#24100=ADVANCED_FACE ( 'NONE', ( #21862 ), #7436, .T. ) ;
#24106=EDGE_LOOP ( 'NONE', ( #14520, #25463, #20726, #3009 ) ) ;
#24112=DIRECTION ( 'NONE',  ( -1.000000000000000000, 0.000000000000000000, -0.000000000000000000 ) ) ;
#24113=CYLINDRICAL_SURFACE ( 'NONE', #34832, 82.00000000000000000 ) ;
#24120=CARTESIAN_POINT ( 'NONE',  ( 10.00000000000000000, -66.50666863321973210, -39.78640506895676765 ) ) ;
#24121=ADVANCED_FACE ( 'NONE', ( #5387 ), #31591, .T. ) ;
#24131=DIRECTION ( 'NONE',  ( -1.000000000000000000, 0.000000000000000000, -0.000000000000000000 ) ) ;
#24136=DIRECTION ( 'NONE',  ( -1.000000000000000000, -0.000000000000000000, -0.000000000000000000 ) ) ;
#24137=AXIS2_PLACEMENT_3D ( 'NONE', #30991, #42222, #9178 ) ;
#24138=CARTESIAN_POINT ( 'NONE',  ( 0.000000000000000000, -0.8261519478425669583, -77.49459641780886443 ) ) ;
#24139=DIRECTION ( 'NONE',  ( 0.000000000000000000, 0.9510565162951523099, 0.3090169943749513926 ) ) ;
#24149=CARTESIAN_POINT ( 'NONE',  ( 10.00000000000000000, -65.59268652807237743, 36.72794159290217664 ) ) ;
#24150=ORIENTED_EDGE ( 'NONE', *, *, #31810, .F. ) ;
#24153=DIRECTION ( 'NONE',  ( -1.000000000000000000, 0.000000000000000000, 0.000000000000000000 ) ) ;
#24156=ADVANCED_FACE ( 'NONE', ( #20069 ), #12731, .T. ) ;
#24164=CIRCLE ( 'NONE', #5408, 77.49899999999999523 ) ;
#24169=VERTEX_POINT ( 'NONE', #8330 ) ;
#24171=ORIENTED_EDGE ( 'NONE', *, *, #40821, .F. ) ;
#24176=CARTESIAN_POINT ( 'NONE',  ( 10.00000000000000000, -65.58780272294048075, -36.73666225445966660 ) ) ;
#24182=VERTEX_POINT ( 'NONE', #19338 ) ;
#24184=CYLINDRICAL_SURFACE ( 'NONE', #29810, 77.49899999999999523 ) ;
#24187=ORIENTED_EDGE ( 'NONE', *, *, #34655, .F. ) ;
#24190=DIRECTION ( 'NONE',  ( -1.000000000000000000, 0.000000000000000000, 0.000000000000000000 ) ) ;
#24207=CARTESIAN_POINT ( 'NONE',  ( 0.000000000000000000, 14.66109333815564852, -73.73191006444555740 ) ) ;
#24211=EDGE_CURVE ( 'NONE', #8489, #3193, #16640, .T. ) ;
#24221=VERTEX_POINT ( 'NONE', #30861 ) ;
#24225=CIRCLE ( 'NONE', #10955, 77.49900000000000944 ) ;
#24226=DIRECTION ( 'NONE',  ( 0.000000000000000000, 0.000000000000000000, 1.000000000000000000 ) ) ;
#24227=CARTESIAN_POINT ( 'NONE',  ( -10.00000000000000000, 0.000000000000000000, 0.000000000000000000 ) ) ;
#24234=DIRECTION ( 'NONE',  ( 0.000000000000000000, 0.000000000000000000, -1.000000000000000000 ) ) ;
#24243=DIRECTION ( 'NONE',  ( 0.000000000000000000, 0.000000000000000000, 1.000000000000000000 ) ) ;
#24246=FACE_OUTER_BOUND ( 'NONE', #43010, .T. ) ;
#24247=CYLINDRICAL_SURFACE ( 'NONE', #9820, 77.49899999999999523 ) ;
#24250=EDGE_CURVE ( 'NONE', #22099, #27232, #42107, .T. ) ;
#24255=CARTESIAN_POINT ( 'NONE',  ( -10.00000000000000000, 0.000000000000000000, 0.000000000000000000 ) ) ;
#24256=DIRECTION ( 'NONE',  ( 0.000000000000000000, 0.000000000000000000, 1.000000000000000000 ) ) ;
#24268=CARTESIAN_POINT ( 'NONE',  ( 5.000000000000002665, 80.28980883073758434, 16.65972982744963460 ) ) ;
#24276=ORIENTED_EDGE ( 'NONE', *, *, #22539, .T. ) ;
#24293=LINE ( 'NONE', #1545, #45942 ) ;
#24297=CIRCLE ( 'NONE', #46975, 31.99999999999999289 ) ;
#24302=EDGE_LOOP ( 'NONE', ( #47299, #35659, #33556, #6926 ) ) ;
#24304=DIRECTION ( 'NONE',  ( -1.000000000000000000, -0.000000000000000000, 0.000000000000000000 ) ) ;
#24321=DIRECTION ( 'NONE',  ( 1.000000000000000000, 0.000000000000000000, 0.000000000000000000 ) ) ;
#24322=ORIENTED_EDGE ( 'NONE', *, *, #44015, .F. ) ;
#24327=AXIS2_PLACEMENT_3D ( 'NONE', #8934, #13339, #39542 ) ;
#24329=FACE_OUTER_BOUND ( 'NONE', #28036, .T. ) ;
#24344=CARTESIAN_POINT ( 'NONE',  ( 10.00000000000000000, 0.000000000000000000, 0.000000000000000000 ) ) ;
#24345=VERTEX_POINT ( 'NONE', #17593 ) ;
#24346=VERTEX_POINT ( 'NONE', #9774 ) ;
#24348=ORIENTED_EDGE ( 'NONE', *, *, #36461, .T. ) ;
#24354=DIRECTION ( 'NONE',  ( 0.000000000000000000, 0.000000000000000000, 1.000000000000000000 ) ) ;
#24356=DIRECTION ( 'NONE',  ( 0.000000000000000000, 0.000000000000000000, 1.000000000000000000 ) ) ;
#24357=AXIS2_PLACEMENT_3D ( 'NONE', #4570, #15361, #880 ) ;
#24367=AXIS2_PLACEMENT_3D ( 'NONE', #47819, #21403, #13584 ) ;
#24373=ADVANCED_FACE ( 'NONE', ( #43783 ), #10251, .T. ) ;
#24376=EDGE_LOOP ( 'NONE', ( #27648, #7720, #18909, #2042 ) ) ;
#24377=EDGE_CURVE ( 'NONE', #39658, #9486, #18790, .T. ) ;
#24380=ORIENTED_EDGE ( 'NONE', *, *, #44544, .F. ) ;
#24381=FACE_OUTER_BOUND ( 'NONE', #37834, .T. ) ;
#24383=ORIENTED_EDGE ( 'NONE', *, *, #7397, .F. ) ;
#24387=EDGE_LOOP ( 'NONE', ( #16932, #24656, #30534, #43187 ) ) ;
#24391=CARTESIAN_POINT ( 'NONE',  ( 0.000000000000000000, 0.000000000000000000, 0.000000000000000000 ) ) ;
#24393=EDGE_LOOP ( 'NONE', ( #23242, #16627, #38995, #265 ) ) ;
#24398=CARTESIAN_POINT ( 'NONE',  ( 0.000000000000000000, -40.65526001592664329, 71.21200624218782593 ) ) ;
#24401=EDGE_CURVE ( 'NONE', #9128, #3813, #4366, .T. ) ;
#24410=DIRECTION ( 'NONE',  ( -1.000000000000000000, 0.000000000000000000, 0.000000000000000000 ) ) ;
#24411=LINE ( 'NONE', #39346, #15908 ) ;
#24414=ORIENTED_EDGE ( 'NONE', *, *, #31038, .T. ) ;
#24419=CARTESIAN_POINT ( 'NONE',  ( 0.000000000000000000, 0.000000000000000000, 0.000000000000000000 ) ) ;
#24420=VERTEX_POINT ( 'NONE', #21746 ) ;
#24421=AXIS2_PLACEMENT_3D ( 'NONE', #31069, #696, #41832 ) ;
#24427=EDGE_CURVE ( 'NONE', #23222, #4970, #7055, .T. ) ;
#24431=CARTESIAN_POINT ( 'NONE',  ( 10.00000000000000000, -26.01480285779885904, 70.53064760720306481 ) ) ;
#24433=VECTOR ( 'NONE', #37486, 1000.000000000000000 ) ;
#24436=CARTESIAN_POINT ( 'NONE',  ( 0.000000000000000000, -55.16347631942998220, -60.67117009219196433 ) ) ;
#24443=ORIENTED_EDGE ( 'NONE', *, *, #39415, .F. ) ;
#24445=AXIS2_PLACEMENT_3D ( 'NONE', #13805, #9624, #24575 ) ;
#24451=ORIENTED_EDGE ( 'NONE', *, *, #16518, .T. ) ;
#24456=VECTOR ( 'NONE', #20829, 1000.000000000000000 ) ;
#24458=EDGE_CURVE ( 'NONE', #24955, #22527, #33279, .T. ) ;
#24465=AXIS2_PLACEMENT_3D ( 'NONE', #23558, #20134, #12086 ) ;
#24466=EDGE_CURVE ( 'NONE', #44497, #4911, #44255, .T. ) ;
#24467=VECTOR ( 'NONE', #9968, 1000.000000000000000 ) ;
#24468=LINE ( 'NONE', #31353, #14505 ) ;
#24469=FACE_OUTER_BOUND ( 'NONE', #6047, .T. ) ;
#24471=AXIS2_PLACEMENT_3D ( 'NONE', #5596, #41840, #34465 ) ;
#24477=CIRCLE ( 'NONE', #36175, 31.99999999999999289 ) ;
#24479=VERTEX_POINT ( 'NONE', #44022 ) ;
#24481=DIRECTION ( 'NONE',  ( 0.000000000000000000, 0.000000000000000000, 1.000000000000000000 ) ) ;
#24489=EDGE_CURVE ( 'NONE', #38387, #43468, #18066, .T. ) ;
#24492=FACE_OUTER_BOUND ( 'NONE', #32415, .T. ) ;
#24502=EDGE_CURVE ( 'NONE', #9321, #9223, #31773, .T. ) ;
#24503=ORIENTED_EDGE ( 'NONE', *, *, #41648, .T. ) ;
#24505=DIRECTION ( 'NONE',  ( 0.000000000000000000, 0.000000000000000000, 1.000000000000000000 ) ) ;
#24507=AXIS2_PLACEMENT_3D ( 'NONE', #32102, #38967, #13486 ) ;
#24510=ORIENTED_EDGE ( 'NONE', *, *, #25398, .T. ) ;
#24511=ORIENTED_EDGE ( 'NONE', *, *, #43267, .F. ) ;
#24516=AXIS2_PLACEMENT_3D ( 'NONE', #17103, #46013, #38913 ) ;
#24520=SURFACE_SIDE_STYLE ('',( #31891 ) ) ;
#24526=VERTEX_POINT ( 'NONE', #7298 ) ;
#24535=CIRCLE ( 'NONE', #18270, 77.49899999999999523 ) ;
#24536=CARTESIAN_POINT ( 'NONE',  ( -10.00000000000000000, 0.000000000000000000, 0.000000000000000000 ) ) ;
#24545=AXIS2_PLACEMENT_3D ( 'NONE', #4036, #27281, #26552 ) ;
#24546=DIRECTION ( 'NONE',  ( -1.000000000000000000, 0.000000000000000000, 0.000000000000000000 ) ) ;
#24547=DIRECTION ( 'NONE',  ( 0.000000000000000000, 0.000000000000000000, 1.000000000000000000 ) ) ;
#24548=DIRECTION ( 'NONE',  ( -1.000000000000000000, 0.000000000000000000, 0.000000000000000000 ) ) ;
#24551=LINE ( 'NONE', #2503, #39818 ) ;
#24552=DIRECTION ( 'NONE',  ( -1.000000000000000000, 0.000000000000000000, -0.000000000000000000 ) ) ;
#24559=CARTESIAN_POINT ( 'NONE',  ( 5.000000000000002665, 71.21200624218852226, -40.65526001592539984 ) ) ;
#24561=DIRECTION ( 'NONE',  ( 0.000000000000000000, 0.9238795325112878487, -0.3826834323650874503 ) ) ;
#24571=DIRECTION ( 'NONE',  ( 0.000000000000000000, 0.000000000000000000, 1.000000000000000000 ) ) ;
#24575=DIRECTION ( 'NONE',  ( 0.000000000000000000, 0.000000000000000000, 1.000000000000000000 ) ) ;
#24578=AXIS2_PLACEMENT_3D ( 'NONE', #41836, #209, #26175 ) ;
#24579=CIRCLE ( 'NONE', #41808, 31.99999999999999645 ) ;
#24583=ORIENTED_EDGE ( 'NONE', *, *, #9334, .F. ) ;
#24585=AXIS2_PLACEMENT_3D ( 'NONE', #37740, #30407, #11800 ) ;
#24592=ORIENTED_EDGE ( 'NONE', *, *, #18050, .T. ) ;
#24593=ORIENTED_EDGE ( 'NONE', *, *, #42206, .T. ) ;
#24603=CARTESIAN_POINT ( 'NONE',  ( 0.000000000000000000, 0.000000000000000000, 0.000000000000000000 ) ) ;
#24604=ORIENTED_EDGE ( 'NONE', *, *, #8979, .T. ) ;
#24608=CARTESIAN_POINT ( 'NONE',  ( 10.00000000000000000, 74.65374052328648702, 8.840884882375350529 ) ) ;
#24611=DIRECTION ( 'NONE',  ( -1.000000000000000000, -0.000000000000000000, 0.000000000000000000 ) ) ;
#24615=CARTESIAN_POINT ( 'NONE',  ( 0.000000000000000000, 14.67089635893713684, 73.72996012237443608 ) ) ;
#24617=CARTESIAN_POINT ( 'NONE',  ( 0.000000000000000000, 59.03342792756328095, -46.54456581323744757 ) ) ;
#24618=AXIS2_PLACEMENT_3D ( 'NONE', #40267, #6724, #17732 ) ;
#24619=CARTESIAN_POINT ( 'NONE',  ( 0.000000000000000000, 29.01471420065564644, 76.69515212746026123 ) ) ;
#24630=AXIS2_PLACEMENT_3D ( 'NONE', #40855, #48198, #18335 ) ;
#24635=ORIENTED_EDGE ( 'NONE', *, *, #15889, .T. ) ;
#24636=EDGE_CURVE ( 'NONE', #31998, #14073, #36453, .T. ) ;
#24642=CARTESIAN_POINT ( 'NONE',  ( 0.000000000000000000, -14.66109333815513160, 73.73191006444567108 ) ) ;
#24644=DIRECTION ( 'NONE',  ( 0.000000000000000000, 0.8526401643540897357, 0.5224985647159527957 ) ) ;
#24650=CARTESIAN_POINT ( 'NONE',  ( 5.000000000000000000, -51.29473840253270112, 63.97538442413407012 ) ) ;
#24652=VERTEX_POINT ( 'NONE', #45469 ) ;
#24653=CARTESIAN_POINT ( 'NONE',  ( 10.00000000000000000, -69.42325613327466272, 34.44570377933573724 ) ) ;
#24654=AXIS2_PLACEMENT_3D ( 'NONE', #26279, #18904, #7665 ) ;
#24655=CIRCLE ( 'NONE', #1212, 32.00000000000000000 ) ;
#24656=ORIENTED_EDGE ( 'NONE', *, *, #12249, .F. ) ;
#24661=CARTESIAN_POINT ( 'NONE',  ( 10.00000000000000000, 0.000000000000000000, 0.000000000000000000 ) ) ;
#24664=ADVANCED_FACE ( 'NONE', ( #12205 ), #8505, .T. ) ;
#24667=CARTESIAN_POINT ( 'NONE',  ( 10.00000000000000000, 46.11716303203284184, -67.80270845531838120 ) ) ;
#24670=CARTESIAN_POINT ( 'NONE',  ( -10.00000000000000000, 0.000000000000000000, 0.000000000000000000 ) ) ;
#24674=ORIENTED_EDGE ( 'NONE', *, *, #45312, .F. ) ;
#24677=DIRECTION ( 'NONE',  ( 0.000000000000000000, -0.2334453638558921795, -0.9723699203976797767 ) ) ;
#24678=AXIS2_PLACEMENT_3D ( 'NONE', #42958, #9179, #45911 ) ;
#24681=DIRECTION ( 'NONE',  ( -1.000000000000000000, 0.000000000000000000, 0.000000000000000000 ) ) ;
#24685=CARTESIAN_POINT ( 'NONE',  ( 10.00000000000000000, -81.90746397400391743, 3.894527615417593847 ) ) ;
#24687=DIRECTION ( 'NONE',  ( -1.000000000000000000, 0.000000000000000000, 0.000000000000000000 ) ) ;
#24702=CYLINDRICAL_SURFACE ( 'NONE', #21879, 31.99999999999999289 ) ;
#24703=ORIENTED_EDGE ( 'NONE', *, *, #43590, .T. ) ;
#24710=EDGE_CURVE ( 'NONE', #28615, #41574, #5202, .T. ) ;
#24714=CARTESIAN_POINT ( 'NONE',  ( -10.00000000000000000, 0.000000000000000000, 0.000000000000000000 ) ) ;
#24719=DIRECTION ( 'NONE',  ( 1.000000000000000000, -0.000000000000000000, -0.000000000000000000 ) ) ;
#24723=ORIENTED_EDGE ( 'NONE', *, *, #47559, .F. ) ;
#24730=FACE_OUTER_BOUND ( 'NONE', #44063, .T. ) ;
#24731=ORIENTED_EDGE ( 'NONE', *, *, #34338, .F. ) ;
#24735=CARTESIAN_POINT ( 'NONE',  ( 10.00000000000000000, 77.49459641780886443, -0.8261519478433788644 ) ) ;
#24739=DIRECTION ( 'NONE',  ( -1.000000000000000000, 0.000000000000000000, 0.000000000000000000 ) ) ;
#24742=DIRECTION ( 'NONE',  ( -1.000000000000000000, -0.000000000000000000, -0.000000000000000000 ) ) ;
#24750=ORIENTED_EDGE ( 'NONE', *, *, #5423, .F. ) ;
#24751=ORIENTED_EDGE ( 'NONE', *, *, #23060, .F. ) ;
#24759=ORIENTED_EDGE ( 'NONE', *, *, #255, .T. ) ;
#24774=EDGE_LOOP ( 'NONE', ( #34013, #47472, #1886, #10201 ) ) ;
#24789=CARTESIAN_POINT ( 'NONE',  ( 10.00000000000000000, 0.000000000000000000, 0.000000000000000000 ) ) ;
#24791=DIRECTION ( 'NONE',  ( 0.000000000000000000, 0.000000000000000000, -1.000000000000000000 ) ) ;
#24803=AXIS2_PLACEMENT_3D ( 'NONE', #45263, #41843, #12232 ) ;
#24805=DIRECTION ( 'NONE',  ( 0.000000000000000000, 0.000000000000000000, -1.000000000000000000 ) ) ;
#24809=ORIENTED_EDGE ( 'NONE', *, *, #39531, .T. ) ;
#24810=CARTESIAN_POINT ( 'NONE',  ( 0.000000000000000000, 11.30684508768452368, -76.66974797899824523 ) ) ;
#24815=DIRECTION ( 'NONE',  ( 0.000000000000000000, 0.000000000000000000, 1.000000000000000000 ) ) ;
#24817=ORIENTED_EDGE ( 'NONE', *, *, #37337, .F. ) ;
#24832=DIRECTION ( 'NONE',  ( 0.000000000000000000, 0.000000000000000000, 1.000000000000000000 ) ) ;
#24841=DIRECTION ( 'NONE',  ( 0.000000000000000000, -0.9238795325112822976, -0.3826834323651008285 ) ) ;
#24842=DIRECTION ( 'NONE',  ( -1.000000000000000000, -0.000000000000000000, 0.000000000000000000 ) ) ;
#24849=ORIENTED_EDGE ( 'NONE', *, *, #10328, .T. ) ;
#24854=AXIS2_PLACEMENT_3D ( 'NONE', #31362, #39421, #35247 ) ;
#24858=EDGE_CURVE ( 'NONE', #41796, #41833, #23991, .T. ) ;
#24859=CARTESIAN_POINT ( 'NONE',  ( 10.00000000000000000, 55.38113227695782115, 54.21277698773695164 ) ) ;
#24862=EDGE_CURVE ( 'NONE', #31962, #33470, #13831, .T. ) ;
#24873=AXIS2_PLACEMENT_3D ( 'NONE', #19372, #30410, #22814 ) ;
#24876=DIRECTION ( 'NONE',  ( 0.000000000000000000, 0.000000000000000000, 1.000000000000000000 ) ) ;
#24884=CARTESIAN_POINT ( 'NONE',  ( 0.000000000000000000, -62.50884508063453637, 41.76106447765467777 ) ) ;
#24887=VERTEX_POINT ( 'NONE', #2855 ) ;
#24888=CARTESIAN_POINT ( 'NONE',  ( 10.00000000000000000, 72.35432306680485226, -20.40083707022909110 ) ) ;
#24889=ORIENTED_EDGE ( 'NONE', *, *, #13766, .T. ) ;
#24903=DIRECTION ( 'NONE',  ( 0.000000000000000000, 0.000000000000000000, 1.000000000000000000 ) ) ;
#24917=CARTESIAN_POINT ( 'NONE',  ( 10.00000000000000000, 59.75363087400074846, 56.15606465354979804 ) ) ;
#24918=DIRECTION ( 'NONE',  ( 0.000000000000000000, 0.000000000000000000, 1.000000000000000000 ) ) ;
#24919=EDGE_CURVE ( 'NONE', #31513, #46010, #40325, .T. ) ;
#24920=CYLINDRICAL_SURFACE ( 'NONE', #37772, 31.99999999999999289 ) ;
#24924=ORIENTED_EDGE ( 'NONE', *, *, #6963, .F. ) ;
#24925=CIRCLE ( 'NONE', #44492, 32.00000000000000000 ) ;
#24926=ADVANCED_FACE ( 'NONE', ( #12154 ), #15561, .T. ) ;
#24929=CIRCLE ( 'NONE', #48370, 82.00000000000000000 ) ;
#24930=DIRECTION ( 'NONE',  ( -1.000000000000000000, -0.000000000000000000, -0.000000000000000000 ) ) ;
#24931=DIRECTION ( 'NONE',  ( -1.000000000000000000, 0.000000000000000000, 0.000000000000000000 ) ) ;
#24932=CIRCLE ( 'NONE', #23357, 32.00000000000000000 ) ;
#24935=ORIENTED_EDGE ( 'NONE', *, *, #37677, .F. ) ;
#24936=ORIENTED_EDGE ( 'NONE', *, *, #25621, .F. ) ;
#24937=ORIENTED_EDGE ( 'NONE', *, *, #43111, .F. ) ;
#24938=CARTESIAN_POINT ( 'NONE',  ( 0.000000000000000000, 10.30890764327382847, 81.34940948281339956 ) ) ;
#24941=VERTEX_POINT ( 'NONE', #27548 ) ;
#24944=LINE ( 'NONE', #18324, #35336 ) ;
#24945=EDGE_LOOP ( 'NONE', ( #11114, #10802, #16834, #27485 ) ) ;
#24946=CARTESIAN_POINT ( 'NONE',  ( 10.00000000000000000, -31.46837873495025306, 68.27212725128265447 ) ) ;
#24949=CIRCLE ( 'NONE', #37464, 31.99999999999998934 ) ;
#24950=DIRECTION ( 'NONE',  ( -1.000000000000000000, 0.000000000000000000, 0.000000000000000000 ) ) ;
#24955=VERTEX_POINT ( 'NONE', #42476 ) ;
#24956=ORIENTED_EDGE ( 'NONE', *, *, #19029, .F. ) ;
#24957=CIRCLE ( 'NONE', #47624, 31.99999999999999289 ) ;
#24960=CARTESIAN_POINT ( 'NONE',  ( 0.000000000000000000, -55.19960302592029677, -51.03279382321147750 ) ) ;
#24976=ADVANCED_FACE ( 'NONE', ( #42003 ), #45663, .T. ) ;
#24979=CARTESIAN_POINT ( 'NONE',  ( 0.000000000000000000, -74.65374052328654386, 8.840884882374837161 ) ) ;
#24982=VECTOR ( 'NONE', #21769, 1000.000000000000000 ) ;
#24987=CIRCLE ( 'NONE', #10146, 82.00000000000000000 ) ;
#24989=CARTESIAN_POINT ( 'NONE',  ( 10.00000000000000000, 20.40083707022987625, -72.35432306680462489 ) ) ;
#24990=VERTEX_POINT ( 'NONE', #19454 ) ;
#24992=CIRCLE ( 'NONE', #35939, 77.49899999999999523 ) ;
#24994=ORIENTED_EDGE ( 'NONE', *, *, #9337, .F. ) ;
#24996=ORIENTED_EDGE ( 'NONE', *, *, #2107, .F. ) ;
#24997=EDGE_LOOP ( 'NONE', ( #23656, #23793, #10655, #39900 ) ) ;
#25006=DIRECTION ( 'NONE',  ( 1.000000000000000000, -0.000000000000000000, -0.000000000000000000 ) ) ;
#25008=ORIENTED_EDGE ( 'NONE', *, *, #44123, .T. ) ;
#25013=CYLINDRICAL_SURFACE ( 'NONE', #28560, 77.49899999999999523 ) ;
#25016=ORIENTED_EDGE ( 'NONE', *, *, #2373, .T. ) ;
#25018=EDGE_CURVE ( 'NONE', #41574, #15936, #33910, .T. ) ;
#25019=DIRECTION ( 'NONE',  ( 0.000000000000000000, -0.9876883405951394357, 0.1564344650402205716 ) ) ;
#25022=ORIENTED_EDGE ( 'NONE', *, *, #32028, .F. ) ;
#25024=CARTESIAN_POINT ( 'NONE',  ( 10.00000000000000000, -8.830959090342926032, 74.65491531819115778 ) ) ;
#25026=DIRECTION ( 'NONE',  ( -1.000000000000000000, 0.000000000000000000, 0.000000000000000000 ) ) ;
#25028=CIRCLE ( 'NONE', #9377, 31.99999999999998934 ) ;
#25031=AXIS2_PLACEMENT_3D ( 'NONE', #40023, #14069, #47115 ) ;
#25032=EDGE_CURVE ( 'NONE', #11145, #1183, #4470, .T. ) ;
#25037=FACE_OUTER_BOUND ( 'NONE', #21439, .T. ) ;
#25040=DIRECTION ( 'NONE',  ( -1.000000000000000000, 0.000000000000000000, 0.000000000000000000 ) ) ;
#25045=ORIENTED_EDGE ( 'NONE', *, *, #47249, .T. ) ;
#25050=CARTESIAN_POINT ( 'NONE',  ( 0.000000000000000000, 0.000000000000000000, 0.000000000000000000 ) ) ;
#25055=VERTEX_POINT ( 'NONE', #45916 ) ;
#25057=CARTESIAN_POINT ( 'NONE',  ( 0.000000000000000000, -12.93880638057369659, 76.41127070299266677 ) ) ;
#25059=EDGE_CURVE ( 'NONE', #32991, #17592, #21644, .T. ) ;
#25060=AXIS2_PLACEMENT_3D ( 'NONE', #8106, #3467, #45080 ) ;
#25066=ORIENTED_EDGE ( 'NONE', *, *, #41830, .F. ) ;
#25067=ORIENTED_EDGE ( 'NONE', *, *, #5543, .F. ) ;
#25075=EDGE_CURVE ( 'NONE', #15919, #10316, #1366, .T. ) ;
#25091=CARTESIAN_POINT ( 'NONE',  ( 0.000000000000000000, 0.000000000000000000, 0.000000000000000000 ) ) ;
#25097=CARTESIAN_POINT ( 'NONE',  ( 0.000000000000000000, 40.65526001592713357, -71.21200624218752750 ) ) ;
#25098=CIRCLE ( 'NONE', #31387, 82.00000000000000000 ) ;
#25100=ORIENTED_EDGE ( 'NONE', *, *, #45463, .T. ) ;
#25101=AXIS2_PLACEMENT_3D ( 'NONE', #39176, #24014, #27205 ) ;
#25103=VECTOR ( 'NONE', #45425, 1000.000000000000000 ) ;
#25106=VERTEX_POINT ( 'NONE', #46878 ) ;
#25108=FACE_OUTER_BOUND ( 'NONE', #19607, .T. ) ;
#25109=CARTESIAN_POINT ( 'NONE',  ( 10.00000000000000000, -46.21855187248673502, 62.20884554314003623 ) ) ;
#25111=CARTESIAN_POINT ( 'NONE',  ( 10.00000000000000000, 24.73286445877703699, 73.44644590900070114 ) ) ;
#25112=ORIENTED_EDGE ( 'NONE', *, *, #16008, .T. ) ;
#25114=CARTESIAN_POINT ( 'NONE',  ( 0.000000000000000000, 20.40083707022882820, 72.35432306680490910 ) ) ;
#25116=DIRECTION ( 'NONE',  ( -1.000000000000000000, 0.000000000000000000, 0.000000000000000000 ) ) ;
#25118=ORIENTED_EDGE ( 'NONE', *, *, #33797, .F. ) ;
#25122=CIRCLE ( 'NONE', #27487, 82.00000000000000000 ) ;
#25130=EDGE_CURVE ( 'NONE', #30369, #40486, #14598, .T. ) ;
#25138=ORIENTED_EDGE ( 'NONE', *, *, #15379, .F. ) ;
#25140=CARTESIAN_POINT ( 'NONE',  ( 10.00000000000000000, -75.11764819372145041, -2.946379043147127064 ) ) ;
#25141=CARTESIAN_POINT ( 'NONE',  ( 0.000000000000000000, 64.81221759200417409, -50.23322058963276504 ) ) ;
#25159=ORIENTED_EDGE ( 'NONE', *, *, #42558, .T. ) ;
#25169=VERTEX_POINT ( 'NONE', #32190 ) ;
#25170=EDGE_CURVE ( 'NONE', #23354, #37827, #28715, .T. ) ;
#25171=CARTESIAN_POINT ( 'NONE',  ( 5.000000000000002665, -2.543863470247813119, -81.96053171279905314 ) ) ;
#25172=EDGE_CURVE ( 'NONE', #32258, #34421, #38072, .T. ) ;
#25177=ORIENTED_EDGE ( 'NONE', *, *, #17515, .T. ) ;
#25179=CARTESIAN_POINT ( 'NONE',  ( 0.000000000000000000, 0.000000000000000000, 0.000000000000000000 ) ) ;
#25180=CYLINDRICAL_SURFACE ( 'NONE', #19602, 77.49899999999999523 ) ;
#25182=ORIENTED_EDGE ( 'NONE', *, *, #471, .F. ) ;
#25185=DIRECTION ( 'NONE',  ( 1.000000000000000000, 0.000000000000000000, 0.000000000000000000 ) ) ;
#25187=AXIS2_PLACEMENT_3D ( 'NONE', #16178, #16646, #46031 ) ;
#25195=DIRECTION ( 'NONE',  ( -1.000000000000000000, -0.000000000000000000, 0.000000000000000000 ) ) ;
#25198=FACE_OUTER_BOUND ( 'NONE', #40903, .T. ) ;
#25199=CARTESIAN_POINT ( 'NONE',  ( 0.000000000000000000, -49.70050353004932475, 59.46389618801944721 ) ) ;
#25208=AXIS2_PLACEMENT_3D ( 'NONE', #21115, #32396, #36051 ) ;
#25209=DIRECTION ( 'NONE',  ( -1.000000000000000000, -0.000000000000000000, -0.000000000000000000 ) ) ;
#25226=CYLINDRICAL_SURFACE ( 'NONE', #11363, 82.00000000000000000 ) ;
#25230=CARTESIAN_POINT ( 'NONE',  ( 0.000000000000000000, -41.19522573413687638, -65.64334221924953283 ) ) ;
#25231=LINE ( 'NONE', #40435, #20832 ) ;
#25240=DIRECTION ( 'NONE',  ( 0.000000000000000000, 0.000000000000000000, 1.000000000000000000 ) ) ;
#25241=CYLINDRICAL_SURFACE ( 'NONE', #37904, 31.99999999999999289 ) ;
#25247=CIRCLE ( 'NONE', #4167, 77.49899999999999523 ) ;
#25248=CARTESIAN_POINT ( 'NONE',  ( 0.000000000000000000, 77.32052557432841411, 5.256550761633138613 ) ) ;
#25249=CARTESIAN_POINT ( 'NONE',  ( -10.00000000000000000, 0.000000000000000000, 0.000000000000000000 ) ) ;
#25261=DIRECTION ( 'NONE',  ( 0.000000000000000000, 0.000000000000000000, 1.000000000000000000 ) ) ;
#25263=AXIS2_PLACEMENT_3D ( 'NONE', #34180, #5300, #4808 ) ;
#25265=CIRCLE ( 'NONE', #38684, 31.99999999999998934 ) ;
#25267=CIRCLE ( 'NONE', #15920, 31.99999999999998934 ) ;
#25288=AXIS2_PLACEMENT_3D ( 'NONE', #18296, #14395, #37388 ) ;
#25301=DIRECTION ( 'NONE',  ( -1.000000000000000000, 0.000000000000000000, 0.000000000000000000 ) ) ;
#25311=DIRECTION ( 'NONE',  ( -1.000000000000000000, -0.000000000000000000, -0.000000000000000000 ) ) ;
#25318=CYLINDRICAL_SURFACE ( 'NONE', #45121, 31.99999999999999289 ) ;
#25320=DIRECTION ( 'NONE',  ( -1.000000000000000000, 0.000000000000000000, 0.000000000000000000 ) ) ;
#25322=CIRCLE ( 'NONE', #41728, 31.99999999999999289 ) ;
#25325=DIRECTION ( 'NONE',  ( 0.000000000000000000, 0.000000000000000000, 1.000000000000000000 ) ) ;
#25330=CARTESIAN_POINT ( 'NONE',  ( 10.00000000000000000, 15.33399622253481276, 80.55351364060595643 ) ) ;
#25333=EDGE_CURVE ( 'NONE', #47293, #35990, #21874, .T. ) ;
#25337=ORIENTED_EDGE ( 'NONE', *, *, #32982, .T. ) ;
#25346=LINE ( 'NONE', #17766, #38673 ) ;
#25347=CYLINDRICAL_SURFACE ( 'NONE', #32769, 31.99999999999999289 ) ;
#25354=EDGE_CURVE ( 'NONE', #13186, #1317, #2126, .T. ) ;
#25355=ADVANCED_FACE ( 'NONE', ( #33613 ), #15028, .T. ) ;
#25357=CARTESIAN_POINT ( 'NONE',  ( 10.00000000000000000, -81.50828551894220197, -8.966570791701579779 ) ) ;
#25364=CARTESIAN_POINT ( 'NONE',  ( 10.00000000000000000, -28.89263327155797967, 71.91182617369179297 ) ) ;
#25369=CARTESIAN_POINT ( 'NONE',  ( 10.00000000000000000, 41.76937507738788469, 62.50329211542452157 ) ) ;
#25370=DIRECTION ( 'NONE',  ( -1.000000000000000000, 0.000000000000000000, -0.000000000000000000 ) ) ;
#25379=VERTEX_POINT ( 'NONE', #1309 ) ;
#25380=AXIS2_PLACEMENT_3D ( 'NONE', #43164, #31251, #42023 ) ;
#25393=CARTESIAN_POINT ( 'NONE',  ( 10.00000000000000000, 75.11764819372149304, -2.946379043146603482 ) ) ;
#25396=EDGE_LOOP ( 'NONE', ( #26042, #29060, #11281, #48277 ) ) ;
#25398=EDGE_CURVE ( 'NONE', #31758, #42670, #15433, .T. ) ;
#25400=CARTESIAN_POINT ( 'NONE',  ( 5.000000000000000000, 64.81221759200417409, -50.23322058963276504 ) ) ;
#25404=CIRCLE ( 'NONE', #27821, 31.99999999999999289 ) ;
#25409=ORIENTED_EDGE ( 'NONE', *, *, #43590, .F. ) ;
#25418=LINE ( 'NONE', #43558, #10323 ) ;
#25419=AXIS2_PLACEMENT_3D ( 'NONE', #45755, #46485, #20519 ) ;
#25422=VERTEX_POINT ( 'NONE', #11370 ) ;
#25423=ORIENTED_EDGE ( 'NONE', *, *, #30862, .T. ) ;
#25424=CARTESIAN_POINT ( 'NONE',  ( 10.00000000000000000, 68.27212725128275395, 31.46837873495001503 ) ) ;
#25426=FACE_OUTER_BOUND ( 'NONE', #4629, .T. ) ;
#25427=ORIENTED_EDGE ( 'NONE', *, *, #38803, .T. ) ;
#25432=ORIENTED_EDGE ( 'NONE', *, *, #10008, .F. ) ;
#25439=EDGE_CURVE ( 'NONE', #25379, #16993, #15280, .T. ) ;
#25445=AXIS2_PLACEMENT_3D ( 'NONE', #18696, #45371, #25560 ) ;
#25453=EDGE_CURVE ( 'NONE', #39100, #17495, #35721, .T. ) ;
#25454=CARTESIAN_POINT ( 'NONE',  ( -10.00000000000000000, 0.000000000000000000, 0.000000000000000000 ) ) ;
#25455=EDGE_CURVE ( 'NONE', #31088, #39870, #45595, .T. ) ;
#25459=DIRECTION ( 'NONE',  ( 0.000000000000000000, 0.000000000000000000, -1.000000000000000000 ) ) ;
#25462=AXIS2_PLACEMENT_3D ( 'NONE', #21608, #14016, #44360 ) ;
#25463=ORIENTED_EDGE ( 'NONE', *, *, #31867, .T. ) ;
#25464=EDGE_CURVE ( 'NONE', #13511, #47663, #15508, .T. ) ;
#25468=CARTESIAN_POINT ( 'NONE',  ( 10.00000000000000000, -73.44644590900078640, 24.73286445877676343 ) ) ;
#25472=VECTOR ( 'NONE', #12400, 1000.000000000000000 ) ;
#25481=DIRECTION ( 'NONE',  ( -1.000000000000000000, -0.000000000000000000, 0.000000000000000000 ) ) ;
#25490=CLOSED_SHELL ( 'NONE', ( #22584, #16169, #7547, #40713, #30442, #8840, #31133, #22641, #38174, #36806, #47135, #13147, #32394, #2222, #8432, #16203, #19214, #22379, #19169, #11766, #23525, #17302, #24926, #26655, #15000, #33165, #46144, #5012, #15321, #18341, #5861, #1849, #48392, #25585, #42103, #24373, #13665, #35974, #5608, #30735, #26368, #37894, #14252, #7065, #43014, #27707, #47572, #23884, #38074, #292, #47450, #23095, #24156, #5831, #13008, #15546, #28416, #7644, #31772, #23050, #11444, #8397, #21293, #11826, #19797, #31208, #34404, #6902, #5809, #41374, #16216, #13277, #30494, #36401, #7726, #11946, #23924, #41136, #19862, #22088, #29974, #23112, #45309, #43045, #6154, #48062, #44268, #28122, #35185, #38498, #5045, #37744, #7047, #39702, #17501, #17558, #2851, #10563, #24097, #31396, #1954, #17182, #24121, #43113, #13532, #29210, #20111, #31028, #21315, #44622, #47538, #47334, #12167, #37195, #14309, #20218, #19605, #45396, #14934, #19075, #31281, #8884, #44395, #1964, #28179, #18619, #8718, #26519, #13667, #32676, #39359, #22947, #26854, #20057, #39998, #12503, #23255, #7349, #6440, #22443, #18665, #42167, #35090, #9020, #2576, #43511, #45875, #10676, #8007, #2587, #38955, #4874, #26026, #29071, #9231, #40879, #1465, #30953, #48339, #47301, #20338, #40184, #29998, #17821, #19433, #33594, #47341, #23754, #2025, #12660, #37808, #20550, #44466, #8890, #1346, #28678, #15234, #27402, #2433, #29495, #40467, #26771, #35707, #44432, #44921, #42184, #22826, #17827, #41194, #13822, #26510, #21749, #35241, #3411, #42822, #38796, #39368, #20230, #32711, #7915, #32933, #42596, #46370, #34676, #19271, #39179, #6659, #19881, #48219, #972, #25355, #22452, #11677, #36697, #20912, #35744, #2323, #8726, #42251, #47517, #20070, #21516, #17938, #9952, #29063, #46826, #37564, #23406, #25574, #13888, #37629, #4480, #23578, #25784, #33043, #46097, #45229, #38534, #44589, #24664, #31142, #11572, #34290, #24976, #4712, #5877, #32918, #38029, #34192, #22276, #37027, #44421, #36753, #12448, #8508, #1247, #20588, #34342, #16370, #16467, #31683, #28939, #37516, #37840, #17355, #7522, #11042, #43868, #39460, #20371, #29906, #26361, #2865, #14930, #7688, #18116, #35040, #1163, #12735, #22487, #28999, #41, #22272, #8524, #8254, #10619, #8067, #20282, #27136, #22785, #34748, #32222, #18672, #2239, #5061, #19131, #53, #24100, #5762, #43764, #26013, #20994, #17783, #46057, #26322, #42393, #34551, #30816, #4420, #47203, #26922, #29621, #1995, #21426, #28497, #45941, #28996, #8393, #27314, #38468, #42865, #39912, #42719, #17117, #7883, #11829, #26913, #4662, #35180, #5154, #8661, #991, #46258 ) ) ;
#25497=DIRECTION ( 'NONE',  ( -1.000000000000000000, 0.000000000000000000, 0.000000000000000000 ) ) ;
#25501=ORIENTED_EDGE ( 'NONE', *, *, #22969, .F. ) ;
#25504=DIRECTION ( 'NONE',  ( -1.000000000000000000, 0.000000000000000000, -0.000000000000000000 ) ) ;
#25513=CARTESIAN_POINT ( 'NONE',  ( 10.00000000000000000, 46.54456581323888997, -59.03342792756214408 ) ) ;
#25524=VERTEX_POINT ( 'NONE', #5955 ) ;
#25526=EDGE_CURVE ( 'NONE', #29354, #46298, #24293, .T. ) ;
#25527=CARTESIAN_POINT ( 'NONE',  ( 10.00000000000000000, -55.16347631943084195, 60.67117009219116852 ) ) ;
#25536=VERTEX_POINT ( 'NONE', #6183 ) ;
#25538=DIRECTION ( 'NONE',  ( 0.000000000000000000, -0.2334453638559125521, 0.9723699203976750027 ) ) ;
#25541=DIRECTION ( 'NONE',  ( -1.000000000000000000, 0.000000000000000000, 0.000000000000000000 ) ) ;
#25544=ORIENTED_EDGE ( 'NONE', *, *, #37455, .F. ) ;
#25546=ORIENTED_EDGE ( 'NONE', *, *, #33559, .T. ) ;
#25550=DIRECTION ( 'NONE',  ( 0.000000000000000000, 0.5877852522924685852, 0.8090169943749507819 ) ) ;
#25554=CARTESIAN_POINT ( 'NONE',  ( 10.00000000000000000, 68.27212725128275395, 31.46837873495001503 ) ) ;
#25558=DIRECTION ( 'NONE',  ( -1.000000000000000000, -0.000000000000000000, -0.000000000000000000 ) ) ;
#25560=DIRECTION ( 'NONE',  ( 0.000000000000000000, -0.5224985647159559043, 0.8526401643540879594 ) ) ;
#25562=AXIS2_PLACEMENT_3D ( 'NONE', #347, #26054, #19418 ) ;
#25565=DIRECTION ( 'NONE',  ( 0.000000000000000000, 0.7604059656000276002, 0.6494480483301877660 ) ) ;
#25570=DIRECTION ( 'NONE',  ( -1.000000000000000000, 0.000000000000000000, 0.000000000000000000 ) ) ;
#25571=CARTESIAN_POINT ( 'NONE',  ( 10.00000000000000000, -40.65526001592664329, 71.21200624218782593 ) ) ;
#25574=ADVANCED_FACE ( 'NONE', ( #36025 ), #39724, .T. ) ;
#25577=EDGE_CURVE ( 'NONE', #17516, #42227, #42908, .T. ) ;
#25585=ADVANCED_FACE ( 'NONE', ( #16953 ), #35794, .T. ) ;
#25597=ORIENTED_EDGE ( 'NONE', *, *, #37577, .F. ) ;
#25606=ORIENTED_EDGE ( 'NONE', *, *, #28954, .T. ) ;
#25614=EDGE_CURVE ( 'NONE', #32530, #43867, #28206, .T. ) ;
#25620=DIRECTION ( 'NONE',  ( -1.000000000000000000, 0.000000000000000000, 0.000000000000000000 ) ) ;
#25621=EDGE_CURVE ( 'NONE', #9834, #34570, #34208, .T. ) ;
#25624=CARTESIAN_POINT ( 'NONE',  ( 0.000000000000000000, -68.27212725128298132, 31.46837873494953541 ) ) ;
#25629=FACE_OUTER_BOUND ( 'NONE', #30282, .T. ) ;
#25631=CARTESIAN_POINT ( 'NONE',  ( 10.00000000000000000, 12.93880638057426502, -76.41127070299258150 ) ) ;
#25638=CIRCLE ( 'NONE', #48320, 31.99999999999999289 ) ;
#25647=CIRCLE ( 'NONE', #24137, 32.00000000000000000 ) ;
#25648=CYLINDRICAL_SURFACE ( 'NONE', #840, 82.00000000000000000 ) ;
#25662=ORIENTED_EDGE ( 'NONE', *, *, #37638, .T. ) ;
#25663=VERTEX_POINT ( 'NONE', #48001 ) ;
#25664=DIRECTION ( 'NONE',  ( 0.000000000000000000, 0.000000000000000000, 1.000000000000000000 ) ) ;
#25667=ORIENTED_EDGE ( 'NONE', *, *, #3692, .T. ) ;
#25668=EDGE_CURVE ( 'NONE', #3891, #17338, #33418, .T. ) ;
#25676=DIRECTION ( 'NONE',  ( 0.000000000000000000, -1.000000000000000000, -0.000000000000000000 ) ) ;
#25679=AXIS2_PLACEMENT_3D ( 'NONE', #29296, #40071, #36396 ) ;
#25684=ORIENTED_EDGE ( 'NONE', *, *, #9433, .F. ) ;
#25687=EDGE_LOOP ( 'NONE', ( #1911, #37909, #41316, #30684 ) ) ;
#25688=ORIENTED_EDGE ( 'NONE', *, *, #37922, .F. ) ;
#25698=VERTEX_POINT ( 'NONE', #44577 ) ;
#25699=LINE ( 'NONE', #18114, #4987 ) ;
#25702=ORIENTED_EDGE ( 'NONE', *, *, #21819, .F. ) ;
#25707=EDGE_LOOP ( 'NONE', ( #29543, #9165, #948, #34452 ) ) ;
#25716=CARTESIAN_POINT ( 'NONE',  ( 0.000000000000000000, 0.000000000000000000, 0.000000000000000000 ) ) ;
#25723=ORIENTED_EDGE ( 'NONE', *, *, #255, .F. ) ;
#25724=EDGE_LOOP ( 'NONE', ( #6130, #40198, #204, #33120 ) ) ;
#25739=DIRECTION ( 'NONE',  ( -1.000000000000000000, 0.000000000000000000, 0.000000000000000000 ) ) ;
#25741=CARTESIAN_POINT ( 'NONE',  ( 0.000000000000000000, -3.894527615417340272, -81.90746397400393164 ) ) ;
#25747=CARTESIAN_POINT ( 'NONE',  ( 5.000000000000002665, -3.894527615418464705, 81.90746397400387480 ) ) ;
#25750=ORIENTED_EDGE ( 'NONE', *, *, #5599, .F. ) ;
#25751=EDGE_CURVE ( 'NONE', #28131, #16520, #43622, .T. ) ;
#25753=VECTOR ( 'NONE', #8355, 1000.000000000000000 ) ;
#25755=AXIS2_PLACEMENT_3D ( 'NONE', #43493, #36128, #24876 ) ;
#25756=EDGE_LOOP ( 'NONE', ( #3918, #20911, #23855, #36375 ) ) ;
#25766=ORIENTED_EDGE ( 'NONE', *, *, #34535, .F. ) ;
#25768=CARTESIAN_POINT ( 'NONE',  ( 10.00000000000000000, -73.73191006444582740, 14.66109333815435889 ) ) ;
#25769=FACE_OUTER_BOUND ( 'NONE', #3512, .T. ) ;
#25775=CARTESIAN_POINT ( 'NONE',  ( 0.000000000000000000, 62.20884554314086046, -46.21855187248561236 ) ) ;
#25776=EDGE_CURVE ( 'NONE', #5074, #25422, #12325, .T. ) ;
#25777=AXIS2_PLACEMENT_3D ( 'NONE', #3900, #18813, #11501 ) ;
#25778=DIRECTION ( 'NONE',  ( 0.000000000000000000, 0.1564344650402244019, 0.9876883405951387696 ) ) ;
#25780=AXIS2_PLACEMENT_3D ( 'NONE', #5017, #19935, #35104 ) ;
#25782=ORIENTED_EDGE ( 'NONE', *, *, #24636, .F. ) ;
#25784=ADVANCED_FACE ( 'NONE', ( #15223 ), #4199, .T. ) ;
#25786=VECTOR ( 'NONE', #19087, 1000.000000000000000 ) ;
#25790=ORIENTED_EDGE ( 'NONE', *, *, #46609, .T. ) ;
#25803=CARTESIAN_POINT ( 'NONE',  ( 10.00000000000000000, -56.15606465355001120, 59.75363087400054951 ) ) ;
#25807=FACE_OUTER_BOUND ( 'NONE', #37422, .T. ) ;
#25813=AXIS2_PLACEMENT_3D ( 'NONE', #36848, #18502, #10688 ) ;
#25818=VERTEX_POINT ( 'NONE', #30389 ) ;
#25819=DIRECTION ( 'NONE',  ( 0.000000000000000000, 0.000000000000000000, 1.000000000000000000 ) ) ;
#25834=DIRECTION ( 'NONE',  ( 1.000000000000000000, -0.000000000000000000, 0.000000000000000000 ) ) ;
#25836=VERTEX_POINT ( 'NONE', #37719 ) ;
#25837=VERTEX_POINT ( 'NONE', #15685 ) ;
#25841=EDGE_CURVE ( 'NONE', #33636, #21412, #27981, .T. ) ;
#25847=CARTESIAN_POINT ( 'NONE',  ( 10.00000000000000000, 0.000000000000000000, 0.000000000000000000 ) ) ;
#25859=AXIS2_PLACEMENT_3D ( 'NONE', #30317, #11951, #18563 ) ;
#25869=ORIENTED_EDGE ( 'NONE', *, *, #15046, .F. ) ;
#25871=VECTOR ( 'NONE', #19048, 1000.000000000000000 ) ;
#25873=EDGE_CURVE ( 'NONE', #773, #697, #43589, .T. ) ;
#25878=ORIENTED_EDGE ( 'NONE', *, *, #40898, .T. ) ;
#25883=ORIENTED_EDGE ( 'NONE', *, *, #12286, .F. ) ;
#25888=VECTOR ( 'NONE', #32305, 1000.000000000000000 ) ;
#25892=ORIENTED_EDGE ( 'NONE', *, *, #10737, .F. ) ;
#25898=CIRCLE ( 'NONE', #32177, 77.49899999999999523 ) ;
#25901=DIRECTION ( 'NONE',  ( 0.000000000000000000, 0.000000000000000000, 1.000000000000000000 ) ) ;
#25905=FACE_OUTER_BOUND ( 'NONE', #12804, .T. ) ;
#25915=DIRECTION ( 'NONE',  ( -1.000000000000000000, 0.000000000000000000, 0.000000000000000000 ) ) ;
#25917=CARTESIAN_POINT ( 'NONE',  ( 10.00000000000000000, 0.000000000000000000, 0.000000000000000000 ) ) ;
#25933=DIRECTION ( 'NONE',  ( 0.000000000000000000, 0.000000000000000000, 1.000000000000000000 ) ) ;
#25943=ORIENTED_EDGE ( 'NONE', *, *, #11934, .F. ) ;
#25948=ORIENTED_EDGE ( 'NONE', *, *, #41969, .F. ) ;
#25951=CIRCLE ( 'NONE', #964, 32.00000000000000000 ) ;
#25952=CARTESIAN_POINT ( 'NONE',  ( 10.00000000000000000, 0.000000000000000000, 0.000000000000000000 ) ) ;
#25955=CARTESIAN_POINT ( 'NONE',  ( 10.00000000000000000, -72.35432306680469594, -20.40083707022958848 ) ) ;
#25956=AXIS2_PLACEMENT_3D ( 'NONE', #13222, #8564, #43079 ) ;
#25957=ORIENTED_EDGE ( 'NONE', *, *, #35656, .T. ) ;
#25958=DIRECTION ( 'NONE',  ( -1.000000000000000000, 0.000000000000000000, 0.000000000000000000 ) ) ;
#25962=EDGE_CURVE ( 'NONE', #45908, #7240, #11583, .T. ) ;
#25978=CARTESIAN_POINT ( 'NONE',  ( 0.000000000000000000, -65.59268652807237743, 36.72794159290217664 ) ) ;
#25979=DIRECTION ( 'NONE',  ( -1.000000000000000000, 0.000000000000000000, -0.000000000000000000 ) ) ;
#25984=EDGE_CURVE ( 'NONE', #18404, #22099, #13917, .T. ) ;
#25988=CARTESIAN_POINT ( 'NONE',  ( 10.00000000000000000, 0.000000000000000000, 0.000000000000000000 ) ) ;
#25996=CIRCLE ( 'NONE', #43954, 77.49899999999999523 ) ;
#25999=EDGE_LOOP ( 'NONE', ( #30073, #16545, #3810, #6476 ) ) ;
#26000=DIRECTION ( 'NONE',  ( 0.000000000000000000, 0.000000000000000000, 1.000000000000000000 ) ) ;
#26013=ADVANCED_FACE ( 'NONE', ( #20308 ), #39168, .T. ) ;
#26021=CARTESIAN_POINT ( 'NONE',  ( 10.00000000000000000, -26.01480285779785362, -70.53064760720343429 ) ) ;
#26022=AXIS2_PLACEMENT_3D ( 'NONE', #40474, #29447, #6930 ) ;
#26024=CARTESIAN_POINT ( 'NONE',  ( 0.000000000000000000, 28.89263327155746097, 71.91182617369197771 ) ) ;
#26025=DIRECTION ( 'NONE',  ( 0.000000000000000000, 0.000000000000000000, 1.000000000000000000 ) ) ;
#26026=ADVANCED_FACE ( 'NONE', ( #12996 ), #16186, .T. ) ;
#26028=VECTOR ( 'NONE', #34785, 1000.000000000000000 ) ;
#26033=EDGE_LOOP ( 'NONE', ( #34447, #20872, #1405, #13943 ) ) ;
#26036=CARTESIAN_POINT ( 'NONE',  ( 0.000000000000000000, -50.23322058963298531, -64.81221759200398935 ) ) ;
#26042=ORIENTED_EDGE ( 'NONE', *, *, #17040, .F. ) ;
#26044=CIRCLE ( 'NONE', #24471, 32.00000000000000000 ) ;
#26046=CARTESIAN_POINT ( 'NONE',  ( 0.000000000000000000, -71.87247863392443037, 39.47590169984818687 ) ) ;
#26054=DIRECTION ( 'NONE',  ( -1.000000000000000000, -0.000000000000000000, -0.000000000000000000 ) ) ;
#26058=AXIS2_PLACEMENT_3D ( 'NONE', #34245, #45042, #12246 ) ;
#26060=EDGE_CURVE ( 'NONE', #26190, #12875, #42052, .T. ) ;
#26061=CYLINDRICAL_SURFACE ( 'NONE', #46738, 31.99999999999999289 ) ;
#26062=DIRECTION ( 'NONE',  ( 0.000000000000000000, 0.000000000000000000, 1.000000000000000000 ) ) ;
#26068=EDGE_CURVE ( 'NONE', #26881, #31305, #32675, .T. ) ;
#26071=AXIS2_PLACEMENT_3D ( 'NONE', #47907, #40816, #7277 ) ;
#26077=CIRCLE ( 'NONE', #19018, 31.99999999999998934 ) ;
#26080=AXIS2_PLACEMENT_3D ( 'NONE', #35980, #2214, #6609 ) ;
#26082=CIRCLE ( 'NONE', #4993, 82.00000000000000000 ) ;
#26090=AXIS2_PLACEMENT_3D ( 'NONE', #43129, #16228, #24050 ) ;
#26092=DIRECTION ( 'NONE',  ( -1.000000000000000000, 0.000000000000000000, -0.000000000000000000 ) ) ;
#26094=ORIENTED_EDGE ( 'NONE', *, *, #41897, .T. ) ;
#26096=DIRECTION ( 'NONE',  ( 0.000000000000000000, 0.9723699203976756689, 0.2334453638559094157 ) ) ;
#26097=EDGE_LOOP ( 'NONE', ( #24935, #11525, #39326, #4895 ) ) ;
#26102=DIRECTION ( 'NONE',  ( -1.000000000000000000, -0.000000000000000000, -0.000000000000000000 ) ) ;
#26106=LINE ( 'NONE', #18748, #25103 ) ;
#26113=CYLINDRICAL_SURFACE ( 'NONE', #30989, 77.49899999999999523 ) ;
#26115=VECTOR ( 'NONE', #39734, 1000.000000000000000 ) ;
#26119=DIRECTION ( 'NONE',  ( 0.000000000000000000, -0.9723699203976789995, 0.2334453638558956490 ) ) ;
#26120=DIRECTION ( 'NONE',  ( 0.000000000000000000, 1.000000000000000000, 3.469446951953614978E-15 ) ) ;
#26124=ORIENTED_EDGE ( 'NONE', *, *, #6520, .F. ) ;
#26126=VECTOR ( 'NONE', #47073, 1000.000000000000000 ) ;
#26134=CIRCLE ( 'NONE', #12858, 31.99999999999999289 ) ;
#26138=CARTESIAN_POINT ( 'NONE',  ( 0.000000000000000000, -17.28742895386139722, 75.54627589209937355 ) ) ;
#26145=CARTESIAN_POINT ( 'NONE',  ( 10.00000000000000000, -11.30684508768395524, 76.66974797899831628 ) ) ;
#26148=EDGE_CURVE ( 'NONE', #41584, #33852, #30355, .T. ) ;
#26149=ORIENTED_EDGE ( 'NONE', *, *, #6940, .F. ) ;
#26150=AXIS2_PLACEMENT_3D ( 'NONE', #41942, #1037, #16464 ) ;
#26151=DIRECTION ( 'NONE',  ( -1.000000000000000000, -0.000000000000000000, -0.000000000000000000 ) ) ;
#26159=DIRECTION ( 'NONE',  ( -1.000000000000000000, -0.000000000000000000, 0.000000000000000000 ) ) ;
#26161=AXIS2_PLACEMENT_3D ( 'NONE', #48006, #29653, #3957 ) ;
#26168=FACE_OUTER_BOUND ( 'NONE', #8216, .T. ) ;
#26169=CARTESIAN_POINT ( 'NONE',  ( 0.000000000000000000, 0.000000000000000000, 0.000000000000000000 ) ) ;
#26171=ORIENTED_EDGE ( 'NONE', *, *, #17025, .T. ) ;
#26175=DIRECTION ( 'NONE',  ( 0.000000000000000000, 0.000000000000000000, -1.000000000000000000 ) ) ;
#26189=DIRECTION ( 'NONE',  ( 0.000000000000000000, 0.000000000000000000, 1.000000000000000000 ) ) ;
#26190=VERTEX_POINT ( 'NONE', #15350 ) ;
#26200=ORIENTED_EDGE ( 'NONE', *, *, #31867, .F. ) ;
#26213=AXIS2_PLACEMENT_3D ( 'NONE', #25024, #13534, #43409 ) ;
#26215=ORIENTED_EDGE ( 'NONE', *, *, #40153, .T. ) ;
#26219=FACE_OUTER_BOUND ( 'NONE', #19625, .T. ) ;
#26228=AXIS2_PLACEMENT_3D ( 'NONE', #15982, #38014, #30661 ) ;
#26234=CARTESIAN_POINT ( 'NONE',  ( 5.000000000000002665, -22.90783923731575911, -78.73519480814978522 ) ) ;
#26236=CARTESIAN_POINT ( 'NONE',  ( 0.000000000000000000, 0.000000000000000000, 0.000000000000000000 ) ) ;
#26238=CARTESIAN_POINT ( 'NONE',  ( 10.00000000000000000, 11.30684508768452545, -76.66974797899825944 ) ) ;
#26256=AXIS2_PLACEMENT_3D ( 'NONE', #5449, #30669, #45590 ) ;
#26257=DIRECTION ( 'NONE',  ( 0.000000000000000000, 0.000000000000000000, -1.000000000000000000 ) ) ;
#26258=EDGE_CURVE ( 'NONE', #8436, #40486, #31006, .T. ) ;
#26260=ORIENTED_EDGE ( 'NONE', *, *, #48300, .F. ) ;
#26263=ORIENTED_EDGE ( 'NONE', *, *, #4269, .F. ) ;
#26264=DIRECTION ( 'NONE',  ( -1.000000000000000000, 0.000000000000000000, -0.000000000000000000 ) ) ;
#26273=ORIENTED_EDGE ( 'NONE', *, *, #8061, .T. ) ;
#26276=DIRECTION ( 'NONE',  ( -1.000000000000000000, -0.000000000000000000, 0.000000000000000000 ) ) ;
#26277=CIRCLE ( 'NONE', #32525, 82.00000000000000000 ) ;
#26278=DIRECTION ( 'NONE',  ( -1.000000000000000000, 0.000000000000000000, 0.000000000000000000 ) ) ;
#26279=CARTESIAN_POINT ( 'NONE',  ( 0.000000000000000000, 0.000000000000000000, 0.000000000000000000 ) ) ;
#26280=ORIENTED_EDGE ( 'NONE', *, *, #35909, .T. ) ;
#26285=CARTESIAN_POINT ( 'NONE',  ( 10.00000000000000000, 41.19522573413731692, 65.64334221924924861 ) ) ;
#26287=ORIENTED_EDGE ( 'NONE', *, *, #40833, .F. ) ;
#26290=ORIENTED_EDGE ( 'NONE', *, *, #14363, .F. ) ;
#26295=VERTEX_POINT ( 'NONE', #26591 ) ;
#26305=FACE_OUTER_BOUND ( 'NONE', #19493, .T. ) ;
#26312=CYLINDRICAL_SURFACE ( 'NONE', #5294, 31.99999999999999289 ) ;
#26314=AXIS2_PLACEMENT_3D ( 'NONE', #36158, #20995, #39123 ) ;
#26315=CARTESIAN_POINT ( 'NONE',  ( 0.000000000000000000, 0.000000000000000000, 0.000000000000000000 ) ) ;
#26319=VERTEX_POINT ( 'NONE', #19704 ) ;
#26321=ORIENTED_EDGE ( 'NONE', *, *, #30580, .T. ) ;
#26322=ADVANCED_FACE ( 'NONE', ( #38096 ), #26829, .T. ) ;
#26323=VECTOR ( 'NONE', #30042, 1000.000000000000000 ) ;
#26325=VERTEX_POINT ( 'NONE', #641 ) ;
#26328=AXIS2_PLACEMENT_3D ( 'NONE', #30692, #4282, #34118 ) ;
#26332=CARTESIAN_POINT ( 'NONE',  ( 10.00000000000000000, 2.946379043146343246, 75.11764819372150725 ) ) ;
#26333=DIRECTION ( 'NONE',  ( 0.000000000000000000, 0.000000000000000000, 1.000000000000000000 ) ) ;
#26337=VERTEX_POINT ( 'NONE', #41765 ) ;
#26339=DIRECTION ( 'NONE',  ( -1.000000000000000000, 0.000000000000000000, -0.000000000000000000 ) ) ;
#26341=DIRECTION ( 'NONE',  ( 0.000000000000000000, 0.8526401643540897357, 0.5224985647159531288 ) ) ;
#26343=AXIS2_PLACEMENT_3D ( 'NONE', #30226, #37554, #1067 ) ;
#26347=LINE ( 'NONE', #18261, #28548 ) ;
#26348=DIRECTION ( 'NONE',  ( -1.000000000000000000, 0.000000000000000000, -0.000000000000000000 ) ) ;
#26350=CARTESIAN_POINT ( 'NONE',  ( 10.00000000000000000, 0.000000000000000000, 0.000000000000000000 ) ) ;
#26353=CIRCLE ( 'NONE', #2892, 31.99999999999999645 ) ;
#26361=ADVANCED_FACE ( 'NONE', ( #19464 ), #5290, .T. ) ;
#26365=DIRECTION ( 'NONE',  ( 0.000000000000000000, 0.000000000000000000, 1.000000000000000000 ) ) ;
#26368=ADVANCED_FACE ( 'NONE', ( #45672 ), #12163, .T. ) ;
#26373=AXIS2_PLACEMENT_3D ( 'NONE', #21152, #13833, #17005 ) ;
#26378=EDGE_CURVE ( 'NONE', #38979, #46234, #987, .T. ) ;
#26384=ORIENTED_EDGE ( 'NONE', *, *, #28878, .F. ) ;
#26387=EDGE_LOOP ( 'NONE', ( #3778, #19918, #18059, #11032 ) ) ;
#26389=DIRECTION ( 'NONE',  ( 0.000000000000000000, 0.000000000000000000, -1.000000000000000000 ) ) ;
#26391=CIRCLE ( 'NONE', #16226, 77.49899999999999523 ) ;
#26392=ORIENTED_EDGE ( 'NONE', *, *, #23585, .F. ) ;
#26398=DIRECTION ( 'NONE',  ( -1.000000000000000000, -0.000000000000000000, -0.000000000000000000 ) ) ;
#26402=ORIENTED_EDGE ( 'NONE', *, *, #19095, .F. ) ;
#26403=DIRECTION ( 'NONE',  ( 0.000000000000000000, 0.000000000000000000, 1.000000000000000000 ) ) ;
#26409=CARTESIAN_POINT ( 'NONE',  ( 10.00000000000000000, 62.50329211542435104, 41.76937507738811917 ) ) ;
#26415=EDGE_LOOP ( 'NONE', ( #25409, #37531, #25943, #9285 ) ) ;
#26416=ORIENTED_EDGE ( 'NONE', *, *, #27466, .F. ) ;
#26422=CYLINDRICAL_SURFACE ( 'NONE', #7103, 31.99999999999999289 ) ;
#26428=CIRCLE ( 'NONE', #43606, 31.99999999999999645 ) ;
#26442=CIRCLE ( 'NONE', #3791, 77.49900000000000944 ) ;
#26448=ORIENTED_EDGE ( 'NONE', *, *, #33590, .F. ) ;
#26451=CARTESIAN_POINT ( 'NONE',  ( -10.00000000000000000, 0.000000000000000000, 0.000000000000000000 ) ) ;
#26453=AXIS2_PLACEMENT_3D ( 'NONE', #45, #17923, #44128 ) ;
#26461=ORIENTED_EDGE ( 'NONE', *, *, #17282, .F. ) ;
#26472=CARTESIAN_POINT ( 'NONE',  ( 10.00000000000000000, -68.26794271651286294, 31.47745569255117104 ) ) ;
#26475=CARTESIAN_POINT ( 'NONE',  ( 10.00000000000000000, -74.65491531819111515, -8.830959090343204920 ) ) ;
#26477=CARTESIAN_POINT ( 'NONE',  ( -10.00000000000000000, 0.000000000000000000, 0.000000000000000000 ) ) ;
#26480=AXIS2_PLACEMENT_3D ( 'NONE', #20924, #13827, #10634 ) ;
#26482=CYLINDRICAL_SURFACE ( 'NONE', #36060, 32.00000000000000000 ) ;
#26491=CARTESIAN_POINT ( 'NONE',  ( 10.00000000000000000, -5.256550761633413060, 77.32052557432841411 ) ) ;
#26492=DIRECTION ( 'NONE',  ( 0.000000000000000000, 0.9510565162951544194, -0.3090169943749446757 ) ) ;
#26496=AXIS2_PLACEMENT_3D ( 'NONE', #21294, #10284, #21780 ) ;
#26502=DIRECTION ( 'NONE',  ( 0.000000000000000000, 0.000000000000000000, 1.000000000000000000 ) ) ;
#26503=ORIENTED_EDGE ( 'NONE', *, *, #46315, .T. ) ;
#26508=ORIENTED_EDGE ( 'NONE', *, *, #34535, .T. ) ;
#26509=CIRCLE ( 'NONE', #45272, 31.99999999999999289 ) ;
#26510=ADVANCED_FACE ( 'NONE', ( #28046 ), #9422, .T. ) ;
#26513=ORIENTED_EDGE ( 'NONE', *, *, #31869, .T. ) ;
#26518=VERTEX_POINT ( 'NONE', #91 ) ;
#26519=ADVANCED_FACE ( 'NONE', ( #22615 ), #7454, .T. ) ;
#26533=LINE ( 'NONE', #338, #33126 ) ;
#26538=CARTESIAN_POINT ( 'NONE',  ( 0.000000000000000000, 0.000000000000000000, 0.000000000000000000 ) ) ;
#26547=CARTESIAN_POINT ( 'NONE',  ( 10.00000000000000000, -55.19960302592104284, 51.03279382321070301 ) ) ;
#26552=DIRECTION ( 'NONE',  ( 0.000000000000000000, -0.9969173337331271867, -0.07845909572785571273 ) ) ;
#26554=EDGE_LOOP ( 'NONE', ( #34193, #18378, #20418, #8088 ) ) ;
#26559=DIRECTION ( 'NONE',  ( -1.000000000000000000, 0.000000000000000000, 0.000000000000000000 ) ) ;
#26561=AXIS2_PLACEMENT_3D ( 'NONE', #45261, #33995, #29839 ) ;
#26562=EDGE_CURVE ( 'NONE', #27232, #20085, #33834, .T. ) ;
#26564=VECTOR ( 'NONE', #38551, 1000.000000000000000 ) ;
#26567=CIRCLE ( 'NONE', #36691, 31.99999999999999289 ) ;
#26572=EDGE_CURVE ( 'NONE', #19224, #23745, #15890, .T. ) ;
#26573=ORIENTED_EDGE ( 'NONE', *, *, #46315, .F. ) ;
#26575=DIRECTION ( 'NONE',  ( 0.000000000000000000, 0.000000000000000000, 1.000000000000000000 ) ) ;
#26579=ORIENTED_EDGE ( 'NONE', *, *, #29940, .F. ) ;
#26591=CARTESIAN_POINT ( 'NONE',  ( 0.000000000000000000, 16.00000000000000000, 2.500000000000000000 ) ) ;
#26595=CARTESIAN_POINT ( 'NONE',  ( 0.000000000000000000, -81.96053171279903893, 2.543863470248094227 ) ) ;
#26597=ORIENTED_EDGE ( 'NONE', *, *, #25059, .F. ) ;
#26598=DIRECTION ( 'NONE',  ( -1.000000000000000000, 0.000000000000000000, 0.000000000000000000 ) ) ;
#26599=VERTEX_POINT ( 'NONE', #6965 ) ;
#26600=ORIENTED_EDGE ( 'NONE', *, *, #38815, .T. ) ;
#26601=DIRECTION ( 'NONE',  ( -1.000000000000000000, -0.000000000000000000, 0.000000000000000000 ) ) ;
#26602=DIRECTION ( 'NONE',  ( 0.000000000000000000, -0.5224985647159379187, -0.8526401643540989506 ) ) ;
#26606=DIRECTION ( 'NONE',  ( 0.000000000000000000, 0.000000000000000000, 1.000000000000000000 ) ) ;
#26635=ORIENTED_EDGE ( 'NONE', *, *, #31584, .F. ) ;
#26638=ORIENTED_EDGE ( 'NONE', *, *, #22932, .T. ) ;
#26640=CARTESIAN_POINT ( 'NONE',  ( 0.000000000000000000, 76.69515212746057387, -29.01471420065480089 ) ) ;
#26650=FACE_OUTER_BOUND ( 'NONE', #16631, .T. ) ;
#26655=ADVANCED_FACE ( 'NONE', ( #27265 ), #12340, .T. ) ;
#26665=CARTESIAN_POINT ( 'NONE',  ( 5.000000000000000000, -74.74816331893404708, -33.71516098798818462 ) ) ;
#26666=EDGE_CURVE ( 'NONE', #39708, #45284, #24477, .T. ) ;
#26669=ORIENTED_EDGE ( 'NONE', *, *, #38145, .F. ) ;
#26671=DIRECTION ( 'NONE',  ( -1.000000000000000000, 0.000000000000000000, 0.000000000000000000 ) ) ;
#26674=AXIS2_PLACEMENT_3D ( 'NONE', #30401, #46053, #19586 ) ;
#26686=CARTESIAN_POINT ( 'NONE',  ( 0.000000000000000000, 6.903761155838878061, -77.19088730480517313 ) ) ;
#26690=ORIENTED_EDGE ( 'NONE', *, *, #39586, .T. ) ;
#26691=EDGE_CURVE ( 'NONE', #26325, #37458, #30686, .T. ) ;
#26696=EDGE_CURVE ( 'NONE', #36602, #3853, #18973, .T. ) ;
#26705=CIRCLE ( 'NONE', #15772, 31.99999999999998934 ) ;
#26710=DIRECTION ( 'NONE',  ( 0.000000000000000000, -0.5877852522924625900, -0.8090169943749551118 ) ) ;
#26713=DIRECTION ( 'NONE',  ( -1.000000000000000000, 0.000000000000000000, -0.000000000000000000 ) ) ;
#26714=CARTESIAN_POINT ( 'NONE',  ( 10.00000000000000000, 44.99326035066149387, -68.55367621811095091 ) ) ;
#26715=CIRCLE ( 'NONE', #29848, 82.00000000000000000 ) ;
#26716=DIRECTION ( 'NONE',  ( 0.000000000000000000, -0.3826834323650970537, 0.9238795325112838519 ) ) ;
#26718=DIRECTION ( 'NONE',  ( 0.000000000000000000, 0.000000000000000000, 1.000000000000000000 ) ) ;
#26720=LINE ( 'NONE', #23043, #25753 ) ;
#26728=AXIS2_PLACEMENT_3D ( 'NONE', #1915, #46702, #23439 ) ;
#26729=CARTESIAN_POINT ( 'NONE',  ( 10.00000000000000000, 2.543863470248371783, 81.96053171279901051 ) ) ;
#26741=AXIS2_PLACEMENT_3D ( 'NONE', #17499, #32906, #44180 ) ;
#26749=EDGE_CURVE ( 'NONE', #45907, #39835, #47910, .T. ) ;
#26752=ORIENTED_EDGE ( 'NONE', *, *, #4595, .T. ) ;
#26757=DIRECTION ( 'NONE',  ( 0.000000000000000000, 0.9510565162951544194, -0.3090169943749446757 ) ) ;
#26761=CARTESIAN_POINT ( 'NONE',  ( 0.000000000000000000, 0.000000000000000000, 0.000000000000000000 ) ) ;
#26771=ADVANCED_FACE ( 'NONE', ( #16964 ), #28711, .T. ) ;
#26774=CARTESIAN_POINT ( 'NONE',  ( 10.00000000000000000, -75.16055320797016748, -18.89407956138335365 ) ) ;
#26787=DIRECTION ( 'NONE',  ( -1.000000000000000000, -0.000000000000000000, -0.000000000000000000 ) ) ;
#26788=ORIENTED_EDGE ( 'NONE', *, *, #42517, .F. ) ;
#26789=AXIS2_PLACEMENT_3D ( 'NONE', #3060, #18713, #29502 ) ;
#26793=VERTEX_POINT ( 'NONE', #35318 ) ;
#26800=EDGE_CURVE ( 'NONE', #2137, #28615, #42445, .T. ) ;
#26802=CIRCLE ( 'NONE', #1012, 77.49899999999999523 ) ;
#26805=CARTESIAN_POINT ( 'NONE',  ( 5.000000000000002665, -81.96053171279901051, -2.543863470249246195 ) ) ;
#26819=ORIENTED_EDGE ( 'NONE', *, *, #17855, .T. ) ;
#26822=CARTESIAN_POINT ( 'NONE',  ( 5.000000000000002665, 29.01471420065674423, -76.69515212745984911 ) ) ;
#26825=CARTESIAN_POINT ( 'NONE',  ( 10.00000000000000000, -67.80270845531921964, 46.11716303203163392 ) ) ;
#26828=FACE_OUTER_BOUND ( 'NONE', #26387, .T. ) ;
#26829=CYLINDRICAL_SURFACE ( 'NONE', #3325, 77.49899999999999523 ) ;
#26843=LINE ( 'NONE', #30038, #38895 ) ;
#26844=AXIS2_PLACEMENT_3D ( 'NONE', #29607, #29849, #22014 ) ;
#26845=EDGE_CURVE ( 'NONE', #38558, #23222, #36968, .T. ) ;
#26847=CARTESIAN_POINT ( 'NONE',  ( 10.00000000000000000, 0.000000000000000000, 0.000000000000000000 ) ) ;
#26849=AXIS2_PLACEMENT_3D ( 'NONE', #7850, #22780, #31059 ) ;
#26854=ADVANCED_FACE ( 'NONE', ( #21100 ), #35077, .T. ) ;
#26864=LINE ( 'NONE', #14884, #31234 ) ;
#26870=VERTEX_POINT ( 'NONE', #36039 ) ;
#26871=DIRECTION ( 'NONE',  ( -1.000000000000000000, 0.000000000000000000, 0.000000000000000000 ) ) ;
#26874=EDGE_LOOP ( 'NONE', ( #4549, #40701, #19350, #10816 ) ) ;
#26876=DIRECTION ( 'NONE',  ( 0.000000000000000000, 0.000000000000000000, 1.000000000000000000 ) ) ;
#26877=EDGE_CURVE ( 'NONE', #32425, #43019, #24551, .T. ) ;
#26878=CARTESIAN_POINT ( 'NONE',  ( 10.00000000000000000, -20.41045688087772092, -72.35160999960838524 ) ) ;
#26881=VERTEX_POINT ( 'NONE', #12815 ) ;
#26885=VERTEX_POINT ( 'NONE', #25248 ) ;
#26886=CARTESIAN_POINT ( 'NONE',  ( 10.00000000000000000, 0.000000000000000000, 0.000000000000000000 ) ) ;
#26888=VECTOR ( 'NONE', #1855, 1000.000000000000000 ) ;
#26889=CIRCLE ( 'NONE', #19846, 82.00000000000000000 ) ;
#26897=CIRCLE ( 'NONE', #5801, 31.99999999999998934 ) ;
#26900=DIRECTION ( 'NONE',  ( -1.000000000000000000, 0.000000000000000000, -0.000000000000000000 ) ) ;
#26902=CIRCLE ( 'NONE', #10476, 31.99999999999999289 ) ;
#26907=LINE ( 'NONE', #1445, #37755 ) ;
#26908=DIRECTION ( 'NONE',  ( 0.000000000000000000, -0.2334453638559126909, 0.9723699203976748917 ) ) ;
#26913=ADVANCED_FACE ( 'NONE', ( #3218 ), #39970, .T. ) ;
#26922=ADVANCED_FACE ( 'NONE', ( #44112 ), #3473, .T. ) ;
#26924=VECTOR ( 'NONE', #698, 1000.000000000000000 ) ;
#26926=AXIS2_PLACEMENT_3D ( 'NONE', #7672, #30430, #37293 ) ;
#26931=ORIENTED_EDGE ( 'NONE', *, *, #6268, .F. ) ;
#26932=AXIS2_PLACEMENT_3D ( 'NONE', #33658, #40309, #26333 ) ;
#26935=CIRCLE ( 'NONE', #41021, 31.99999999999999289 ) ;
#26940=ORIENTED_EDGE ( 'NONE', *, *, #23995, .T. ) ;
#26945=VERTEX_POINT ( 'NONE', #11320 ) ;
#26954=DIRECTION ( 'NONE',  ( 0.000000000000000000, 0.000000000000000000, 1.000000000000000000 ) ) ;
#26957=AXIS2_PLACEMENT_3D ( 'NONE', #44765, #45487, #41588 ) ;
#26961=ORIENTED_EDGE ( 'NONE', *, *, #33269, .T. ) ;
#26963=CIRCLE ( 'NONE', #12125, 82.00000000000000000 ) ;
#26965=EDGE_LOOP ( 'NONE', ( #30484, #4125, #27677, #37928 ) ) ;
#26976=DIRECTION ( 'NONE',  ( 0.000000000000000000, 0.000000000000000000, 1.000000000000000000 ) ) ;
#26977=CARTESIAN_POINT ( 'NONE',  ( 0.000000000000000000, 0.000000000000000000, 0.000000000000000000 ) ) ;
#26992=ORIENTED_EDGE ( 'NONE', *, *, #32506, .F. ) ;
#26994=CYLINDRICAL_SURFACE ( 'NONE', #34604, 31.99999999999998579 ) ;
#26995=CIRCLE ( 'NONE', #44977, 31.99999999999998934 ) ;
#27002=AXIS2_PLACEMENT_3D ( 'NONE', #18130, #9588, #20871 ) ;
#27005=DIRECTION ( 'NONE',  ( 0.000000000000000000, 0.000000000000000000, 1.000000000000000000 ) ) ;
#27007=CIRCLE ( 'NONE', #34009, 31.99999999999998579 ) ;
#27016=EDGE_LOOP ( 'NONE', ( #12063, #18175, #31068, #31706 ) ) ;
#27021=CARTESIAN_POINT ( 'NONE',  ( 0.000000000000000000, 16.65972982745046238, -80.28980883073738539 ) ) ;
#27026=DIRECTION ( 'NONE',  ( 0.000000000000000000, 0.000000000000000000, 1.000000000000000000 ) ) ;
#27032=CARTESIAN_POINT ( 'NONE',  ( 10.00000000000000000, 68.67312586194995561, 35.91791733033500122 ) ) ;
#27039=EDGE_CURVE ( 'NONE', #21719, #22698, #47762, .T. ) ;
#27040=VERTEX_POINT ( 'NONE', #40451 ) ;
#27044=CARTESIAN_POINT ( 'NONE',  ( 10.00000000000000000, -76.41127070299280888, 12.93880638057289012 ) ) ;
#27049=AXIS2_PLACEMENT_3D ( 'NONE', #39559, #21167, #17743 ) ;
#27051=AXIS2_PLACEMENT_3D ( 'NONE', #805, #42673, #45599 ) ;
#27052=ORIENTED_EDGE ( 'NONE', *, *, #2055, .F. ) ;
#27057=CIRCLE ( 'NONE', #27876, 82.00000000000000000 ) ;
#27059=AXIS2_PLACEMENT_3D ( 'NONE', #41595, #33998, #34234 ) ;
#27065=ORIENTED_EDGE ( 'NONE', *, *, #14044, .T. ) ;
#27069=DIRECTION ( 'NONE',  ( 0.000000000000000000, 0.4539904997395413089, 0.8910065241883705633 ) ) ;
#27070=CARTESIAN_POINT ( 'NONE',  ( 10.00000000000000000, 73.95703589264006439, -23.16143007188350822 ) ) ;
#27081=DIRECTION ( 'NONE',  ( 0.000000000000000000, -0.8090169943749532244, 0.5877852522924652545 ) ) ;
#27082=CARTESIAN_POINT ( 'NONE',  ( 10.00000000000000178, 0.000000000000000000, 0.000000000000000000 ) ) ;
#27084=CARTESIAN_POINT ( 'NONE',  ( -10.00000000000000000, 0.000000000000000000, 0.000000000000000000 ) ) ;
#27087=CARTESIAN_POINT ( 'NONE',  ( 10.00000000000000000, 0.000000000000000000, 0.000000000000000000 ) ) ;
#27092=DIRECTION ( 'NONE',  ( 0.000000000000000000, 0.000000000000000000, 1.000000000000000000 ) ) ;
#27096=EDGE_CURVE ( 'NONE', #48217, #18490, #37979, .T. ) ;
#27103=ORIENTED_EDGE ( 'NONE', *, *, #40898, .F. ) ;
#27105=CARTESIAN_POINT ( 'NONE',  ( 10.00000000000000000, -65.58780272294100655, 36.73666225445870737 ) ) ;
#27108=ORIENTED_EDGE ( 'NONE', *, *, #30250, .T. ) ;
#27110=CARTESIAN_POINT ( 'NONE',  ( 5.000000000000002665, -22.90783923731686045, 78.73519480814945837 ) ) ;
#27112=ORIENTED_EDGE ( 'NONE', *, *, #23866, .F. ) ;
#27115=EDGE_CURVE ( 'NONE', #37098, #24652, #16195, .T. ) ;
#27119=EDGE_CURVE ( 'NONE', #47457, #21501, #24949, .T. ) ;
#27120=ORIENTED_EDGE ( 'NONE', *, *, #9998, .T. ) ;
#27126=DIRECTION ( 'NONE',  ( 0.000000000000000000, 0.000000000000000000, 1.000000000000000000 ) ) ;
#27136=ADVANCED_FACE ( 'NONE', ( #12041 ), #22565, .T. ) ;
#27147=ORIENTED_EDGE ( 'NONE', *, *, #30966, .T. ) ;
#27156=EDGE_CURVE ( 'NONE', #39835, #3149, #26720, .T. ) ;
#27157=DIRECTION ( 'NONE',  ( 1.000000000000000000, -0.000000000000000000, 0.000000000000000000 ) ) ;
#27159=CARTESIAN_POINT ( 'NONE',  ( 10.00000000000000000, -74.65491531819111515, 23.16904090965678975 ) ) ;
#27162=CARTESIAN_POINT ( 'NONE',  ( 10.00000000000000000, 0.000000000000000000, 0.000000000000000000 ) ) ;
#27164=ORIENTED_EDGE ( 'NONE', *, *, #38351, .T. ) ;
#27167=ORIENTED_EDGE ( 'NONE', *, *, #11828, .F. ) ;
#27172=CARTESIAN_POINT ( 'NONE',  ( 0.000000000000000000, 75.11725578898467859, 2.956366410620910656 ) ) ;
#27201=CARTESIAN_POINT ( 'NONE',  ( 0.000000000000000000, 0.000000000000000000, 0.000000000000000000 ) ) ;
#27205=DIRECTION ( 'NONE',  ( 0.000000000000000000, 0.6494480483301793283, 0.7604059656000345946 ) ) ;
#27216=DIRECTION ( 'NONE',  ( 0.000000000000000000, 0.000000000000000000, 1.000000000000000000 ) ) ;
#27219=CARTESIAN_POINT ( 'NONE',  ( 10.00000000000000000, -81.96053171279899630, -2.543863470249235981 ) ) ;
#27220=FACE_OUTER_BOUND ( 'NONE', #45742, .T. ) ;
#27224=ORIENTED_EDGE ( 'NONE', *, *, #7584, .F. ) ;
#27232=VERTEX_POINT ( 'NONE', #35018 ) ;
#27241=AXIS2_PLACEMENT_3D ( 'NONE', #10046, #28881, #43814 ) ;
#27245=CIRCLE ( 'NONE', #28057, 31.99999999999998934 ) ;
#27258=CARTESIAN_POINT ( 'NONE',  ( 10.00000000000000000, 55.38113227695858143, -54.21277698773617715 ) ) ;
#27265=FACE_OUTER_BOUND ( 'NONE', #2947, .T. ) ;
#27275=DIRECTION ( 'NONE',  ( -1.000000000000000000, -0.000000000000000000, 0.000000000000000000 ) ) ;
#27279=ORIENTED_EDGE ( 'NONE', *, *, #15682, .T. ) ;
#27281=DIRECTION ( 'NONE',  ( -1.000000000000000000, -0.000000000000000000, 0.000000000000000000 ) ) ;
#27285=DIRECTION ( 'NONE',  ( -1.000000000000000000, 0.000000000000000000, 0.000000000000000000 ) ) ;
#27291=VERTEX_POINT ( 'NONE', #27447 ) ;
#27294=ORIENTED_EDGE ( 'NONE', *, *, #10211, .T. ) ;
#27298=CARTESIAN_POINT ( 'NONE',  ( 10.00000000000000000, -73.44644590900043113, -24.73286445877782924 ) ) ;
#27303=ORIENTED_EDGE ( 'NONE', *, *, #47834, .F. ) ;
#27304=EDGE_CURVE ( 'NONE', #16330, #32691, #15626, .T. ) ;
#27306=DIRECTION ( 'NONE',  ( -1.000000000000000000, -0.000000000000000000, -0.000000000000000000 ) ) ;
#27307=CARTESIAN_POINT ( 'NONE',  ( 5.000000000000000000, -60.67117009219176538, 55.16347631943019536 ) ) ;
#27309=VERTEX_POINT ( 'NONE', #36929 ) ;
#27314=ADVANCED_FACE ( 'NONE', ( #18343 ), #37191, .T. ) ;
#27315=FACE_OUTER_BOUND ( 'NONE', #34020, .T. ) ;
#27328=CIRCLE ( 'NONE', #38251, 77.49900000000000944 ) ;
#27329=LINE ( 'NONE', #27823, #25472 ) ;
#27334=CARTESIAN_POINT ( 'NONE',  ( 10.00000000000000000, 0.000000000000000000, 0.000000000000000000 ) ) ;
#27336=CARTESIAN_POINT ( 'NONE',  ( 10.00000000000000000, -27.74655509720723501, 77.16300072079651784 ) ) ;
#27345=AXIS2_PLACEMENT_3D ( 'NONE', #46799, #32350, #47031 ) ;
#27349=ORIENTED_EDGE ( 'NONE', *, *, #37164, .F. ) ;
#27350=VECTOR ( 'NONE', #43143, 1000.000000000000000 ) ;
#27354=VERTEX_POINT ( 'NONE', #40617 ) ;
#27358=CARTESIAN_POINT ( 'NONE',  ( 10.00000000000000000, 0.000000000000000000, 0.000000000000000000 ) ) ;
#27379=ORIENTED_EDGE ( 'NONE', *, *, #39115, .T. ) ;
#27383=AXIS2_PLACEMENT_3D ( 'NONE', #23481, #33767, #8070 ) ;
#27387=DIRECTION ( 'NONE',  ( -1.000000000000000000, -0.000000000000000000, -0.000000000000000000 ) ) ;
#27399=LINE ( 'NONE', #8775, #17461 ) ;
#27402=ADVANCED_FACE ( 'NONE', ( #14685 ), #7082, .T. ) ;
#27409=EDGE_CURVE ( 'NONE', #40538, #16837, #1562, .T. ) ;
#27412=AXIS2_PLACEMENT_3D ( 'NONE', #34317, #16702, #20355 ) ;
#27420=EDGE_CURVE ( 'NONE', #37633, #17307, #29368, .T. ) ;
#27423=CIRCLE ( 'NONE', #40692, 31.99999999999999289 ) ;
#27427=ORIENTED_EDGE ( 'NONE', *, *, #40179, .F. ) ;
#27432=DIRECTION ( 'NONE',  ( -1.000000000000000000, -0.000000000000000000, -0.000000000000000000 ) ) ;
#27433=ORIENTED_EDGE ( 'NONE', *, *, #20225, .T. ) ;
#27442=LINE ( 'NONE', #15940, #36953 ) ;
#27443=FACE_OUTER_BOUND ( 'NONE', #37511, .T. ) ;
#27446=FACE_OUTER_BOUND ( 'NONE', #16593, .T. ) ;
#27447=CARTESIAN_POINT ( 'NONE',  ( 10.00000000000000000, -76.66974797899844418, 11.30684508768314522 ) ) ;
#27458=CARTESIAN_POINT ( 'NONE',  ( 10.00000000000000000, 75.16055320797030959, 18.89407956138283851 ) ) ;
#27459=DIRECTION ( 'NONE',  ( -1.000000000000000000, 0.000000000000000000, 0.000000000000000000 ) ) ;
#27463=EDGE_CURVE ( 'NONE', #36004, #32527, #19515, .T. ) ;
#27466=EDGE_CURVE ( 'NONE', #24420, #14894, #8555, .T. ) ;
#27470=FACE_OUTER_BOUND ( 'NONE', #10844, .T. ) ;
#27475=ORIENTED_EDGE ( 'NONE', *, *, #14819, .T. ) ;
#27478=EDGE_CURVE ( 'NONE', #30509, #38853, #33745, .T. ) ;
#27481=DIRECTION ( 'NONE',  ( 1.000000000000000000, -0.000000000000000000, 0.000000000000000000 ) ) ;
#27485=ORIENTED_EDGE ( 'NONE', *, *, #34467, .T. ) ;
#27487=AXIS2_PLACEMENT_3D ( 'NONE', #38327, #26102, #41052 ) ;
#27497=DIRECTION ( 'NONE',  ( -1.000000000000000000, 0.000000000000000000, -0.000000000000000000 ) ) ;
#27512=DIRECTION ( 'NONE',  ( 0.000000000000000000, -0.7071067811865389130, -0.7071067811865561215 ) ) ;
#27513=CARTESIAN_POINT ( 'NONE',  ( 10.00000000000000000, 72.35432306680485226, -20.40083707022909110 ) ) ;
#27515=CARTESIAN_POINT ( 'NONE',  ( 10.00000000000000000, 67.80270845531889279, 46.11716303203210998 ) ) ;
#27523=CARTESIAN_POINT ( 'NONE',  ( 0.000000000000000000, -11.30684508768395524, 76.66974797899831628 ) ) ;
#27524=EDGE_CURVE ( 'NONE', #38555, #30674, #12489, .T. ) ;
#27527=EDGE_CURVE ( 'NONE', #17470, #37239, #28894, .T. ) ;
#27528=CIRCLE ( 'NONE', #19675, 31.99999999999999289 ) ;
#27536=AXIS2_PLACEMENT_3D ( 'NONE', #24419, #32029, #31802 ) ;
#27541=DIRECTION ( 'NONE',  ( -1.000000000000000000, -0.000000000000000000, -0.000000000000000000 ) ) ;
#27545=ORIENTED_EDGE ( 'NONE', *, *, #14822, .T. ) ;
#27546=ORIENTED_EDGE ( 'NONE', *, *, #8906, .F. ) ;
#27548=CARTESIAN_POINT ( 'NONE',  ( 10.00000000000000000, -0.8261519478436571973, 77.49459641780886443 ) ) ;
#27549=VERTEX_POINT ( 'NONE', #7809 ) ;
#27554=DIRECTION ( 'NONE',  ( -1.000000000000000000, -0.000000000000000000, -0.000000000000000000 ) ) ;
#27563=DIRECTION ( 'NONE',  ( -1.000000000000000000, 0.000000000000000000, -0.000000000000000000 ) ) ;
#27565=DIRECTION ( 'NONE',  ( -1.000000000000000000, 0.000000000000000000, 0.000000000000000000 ) ) ;
#27566=CIRCLE ( 'NONE', #10360, 31.99999999999999289 ) ;
#27569=DIRECTION ( 'NONE',  ( -1.000000000000000000, -0.000000000000000000, -0.000000000000000000 ) ) ;
#27573=FACE_OUTER_BOUND ( 'NONE', #21632, .T. ) ;
#27577=EDGE_CURVE ( 'NONE', #21411, #5642, #48423, .T. ) ;
#27579=AXIS2_PLACEMENT_3D ( 'NONE', #36774, #2286, #17205 ) ;
#27582=ORIENTED_EDGE ( 'NONE', *, *, #21673, .F. ) ;
#27583=EDGE_CURVE ( 'NONE', #22222, #17705, #40058, .T. ) ;
#27593=VECTOR ( 'NONE', #35826, 1000.000000000000000 ) ;
#27595=ORIENTED_EDGE ( 'NONE', *, *, #36962, .T. ) ;
#27599=VERTEX_POINT ( 'NONE', #3073 ) ;
#27602=VERTEX_POINT ( 'NONE', #14604 ) ;
#27604=ORIENTED_EDGE ( 'NONE', *, *, #45262, .F. ) ;
#27615=AXIS2_PLACEMENT_3D ( 'NONE', #28166, #17375, #13956 ) ;
#27616=CARTESIAN_POINT ( 'NONE',  ( 10.00000000000000000, 75.11725578898472122, -2.956366410619845730 ) ) ;
#27618=VERTEX_POINT ( 'NONE', #3315 ) ;
#27622=VECTOR ( 'NONE', #4853, 1000.000000000000000 ) ;
#27623=CARTESIAN_POINT ( 'NONE',  ( 5.000000000000000000, -67.80270845531921964, 46.11716303203163392 ) ) ;
#27640=EDGE_CURVE ( 'NONE', #14073, #371, #33610, .T. ) ;
#27648=ORIENTED_EDGE ( 'NONE', *, *, #11743, .F. ) ;
#27649=CIRCLE ( 'NONE', #10455, 31.99999999999999289 ) ;
#27659=CARTESIAN_POINT ( 'NONE',  ( 10.00000000000000000, 0.000000000000000000, 0.000000000000000000 ) ) ;
#27666=DIRECTION ( 'NONE',  ( 0.000000000000000000, 0.000000000000000000, 1.000000000000000000 ) ) ;
#27669=FACE_OUTER_BOUND ( 'NONE', #19639, .T. ) ;
#27670=CIRCLE ( 'NONE', #21405, 31.99999999999999289 ) ;
#27673=EDGE_LOOP ( 'NONE', ( #10579, #21919, #10499, #27052 ) ) ;
#27676=CYLINDRICAL_SURFACE ( 'NONE', #28973, 77.49899999999999523 ) ;
#27677=ORIENTED_EDGE ( 'NONE', *, *, #14370, .T. ) ;
#27679=ORIENTED_EDGE ( 'NONE', *, *, #20353, .F. ) ;
#27682=DIRECTION ( 'NONE',  ( -1.000000000000000000, 0.000000000000000000, 0.000000000000000000 ) ) ;
#27701=CIRCLE ( 'NONE', #36956, 31.99999999999998579 ) ;
#27705=EDGE_CURVE ( 'NONE', #25524, #46560, #2844, .T. ) ;
#27707=ADVANCED_FACE ( 'NONE', ( #10433 ), #6996, .T. ) ;
#27708=VERTEX_POINT ( 'NONE', #17770 ) ;
#27711=FACE_OUTER_BOUND ( 'NONE', #6539, .T. ) ;
#27713=CIRCLE ( 'NONE', #11329, 32.00000000000000000 ) ;
#27723=LINE ( 'NONE', #1528, #30526 ) ;
#27724=CIRCLE ( 'NONE', #17536, 82.00000000000000000 ) ;
#27734=DIRECTION ( 'NONE',  ( -1.000000000000000000, -0.000000000000000000, -0.000000000000000000 ) ) ;
#27746=CIRCLE ( 'NONE', #8972, 12.50000000000000000 ) ;
#27755=EDGE_LOOP ( 'NONE', ( #42657, #1400, #4727, #43258 ) ) ;
#27781=CARTESIAN_POINT ( 'NONE',  ( 0.000000000000000000, -50.95692526931286181, -58.39081064771806240 ) ) ;
#27789=DIRECTION ( 'NONE',  ( -1.000000000000000000, 0.000000000000000000, 0.000000000000000000 ) ) ;
#27790=ORIENTED_EDGE ( 'NONE', *, *, #24858, .T. ) ;
#27797=DIRECTION ( 'NONE',  ( -1.000000000000000000, 0.000000000000000000, 0.000000000000000000 ) ) ;
#27798=CARTESIAN_POINT ( 'NONE',  ( 10.00000000000000000, 0.000000000000000000, 0.000000000000000000 ) ) ;
#27805=EDGE_LOOP ( 'NONE', ( #41403, #41756, #34136, #15444 ) ) ;
#27809=CYLINDRICAL_SURFACE ( 'NONE', #23659, 31.99999999999999289 ) ;
#27821=AXIS2_PLACEMENT_3D ( 'NONE', #40197, #14238, #9844 ) ;
#27823=CARTESIAN_POINT ( 'NONE',  ( 10.00000000000000000, -46.21855187248583974, -62.20884554314070414 ) ) ;
#27825=DIRECTION ( 'NONE',  ( 0.000000000000000000, 0.000000000000000000, 1.000000000000000000 ) ) ;
#27829=DIRECTION ( 'NONE',  ( 0.000000000000000000, -0.8526401643540970632, 0.5224985647159411384 ) ) ;
#27831=ORIENTED_EDGE ( 'NONE', *, *, #15794, .F. ) ;
#27844=EDGE_CURVE ( 'NONE', #47293, #7344, #35991, .T. ) ;
#27858=ORIENTED_EDGE ( 'NONE', *, *, #33734, .T. ) ;
#27859=AXIS2_PLACEMENT_3D ( 'NONE', #26472, #41406, #11782 ) ;
#27861=CARTESIAN_POINT ( 'NONE',  ( 10.00000000000000000, 62.20884554314020676, 46.21855187248652896 ) ) ;
#27863=CARTESIAN_POINT ( 'NONE',  ( -10.00000000000000000, 0.000000000000000000, 0.000000000000000000 ) ) ;
#27864=ORIENTED_EDGE ( 'NONE', *, *, #25962, .T. ) ;
#27866=ORIENTED_EDGE ( 'NONE', *, *, #27409, .F. ) ;
#27873=CARTESIAN_POINT ( 'NONE',  ( 10.00000000000000000, 0.000000000000000000, 0.000000000000000000 ) ) ;
#27876=AXIS2_PLACEMENT_3D ( 'NONE', #41943, #19631, #1038 ) ;
#27881=DIRECTION ( 'NONE',  ( -1.000000000000000000, -0.000000000000000000, -0.000000000000000000 ) ) ;
#27883=EDGE_CURVE ( 'NONE', #697, #21394, #798, .T. ) ;
#27893=DIRECTION ( 'NONE',  ( 0.000000000000000000, 0.000000000000000000, 1.000000000000000000 ) ) ;
#27894=LINE ( 'NONE', #42809, #2555 ) ;
#27898=DIRECTION ( 'NONE',  ( 0.000000000000000000, 0.000000000000000000, 1.000000000000000000 ) ) ;
#27899=DIRECTION ( 'NONE',  ( -1.000000000000000000, -0.000000000000000000, 0.000000000000000000 ) ) ;
#27900=DIRECTION ( 'NONE',  ( -1.000000000000000000, 0.000000000000000000, -0.000000000000000000 ) ) ;
#27902=AXIS2_PLACEMENT_3D ( 'NONE', #14442, #29601, #7327 ) ;
#27905=EDGE_CURVE ( 'NONE', #47056, #38428, #41450, .T. ) ;
#27906=ORIENTED_EDGE ( 'NONE', *, *, #41058, .T. ) ;
#27913=EDGE_CURVE ( 'NONE', #39808, #32517, #37529, .T. ) ;
#27915=ORIENTED_EDGE ( 'NONE', *, *, #2005, .F. ) ;
#27916=ORIENTED_EDGE ( 'NONE', *, *, #31750, .F. ) ;
#27917=ORIENTED_EDGE ( 'NONE', *, *, #25455, .T. ) ;
#27918=AXIS2_PLACEMENT_3D ( 'NONE', #10887, #22136, #11615 ) ;
#27920=DIRECTION ( 'NONE',  ( -1.000000000000000000, -0.000000000000000000, 0.000000000000000000 ) ) ;
#27921=ORIENTED_EDGE ( 'NONE', *, *, #40117, .F. ) ;
#27922=CARTESIAN_POINT ( 'NONE',  ( 10.00000000000000000, -77.19088730480528682, 6.903761155837488062 ) ) ;
#27923=ORIENTED_EDGE ( 'NONE', *, *, #46973, .T. ) ;
#27925=LINE ( 'NONE', #16888, #1707 ) ;
#27931=FACE_OUTER_BOUND ( 'NONE', #6897, .T. ) ;
#27935=DIRECTION ( 'NONE',  ( 0.000000000000000000, 0.3090169943749480619, -0.9510565162951533091 ) ) ;
#27936=VERTEX_POINT ( 'NONE', #2083 ) ;
#27940=LINE ( 'NONE', #21276, #12134 ) ;
#27941=ORIENTED_EDGE ( 'NONE', *, *, #33364, .T. ) ;
#27950=DIRECTION ( 'NONE',  ( -1.000000000000000000, 0.000000000000000000, 0.000000000000000000 ) ) ;
#27952=CARTESIAN_POINT ( 'NONE',  ( 10.00000000000000000, -26.02418014898260878, -70.52718814184285634 ) ) ;
#27963=AXIS2_PLACEMENT_3D ( 'NONE', #41189, #3723, #8113 ) ;
#27965=ORIENTED_EDGE ( 'NONE', *, *, #19931, .T. ) ;
#27971=DIRECTION ( 'NONE',  ( -1.000000000000000000, 0.000000000000000000, 0.000000000000000000 ) ) ;
#27975=ORIENTED_EDGE ( 'NONE', *, *, #46910, .F. ) ;
#27980=CARTESIAN_POINT ( 'NONE',  ( 10.00000000000000000, 50.23322058963440639, -64.81221759200288091 ) ) ;
#27981=CIRCLE ( 'NONE', #10783, 77.49899999999999523 ) ;
#27984=DIRECTION ( 'NONE',  ( 0.000000000000000000, 0.000000000000000000, -1.000000000000000000 ) ) ;
#27989=VECTOR ( 'NONE', #48275, 1000.000000000000000 ) ;
#27990=DIRECTION ( 'NONE',  ( 0.000000000000000000, 0.000000000000000000, 1.000000000000000000 ) ) ;
#28000=DIRECTION ( 'NONE',  ( 0.000000000000000000, 0.8090169943749488946, -0.5877852522924712497 ) ) ;
#28002=LINE ( 'NONE', #39247, #28685 ) ;
#28005=COLOUR_RGB ( '', 0.66274510, 0.83137255, 0.94901961) ;
#28007=CIRCLE ( 'NONE', #15489, 31.99999999999998934 ) ;
#28009=ORIENTED_EDGE ( 'NONE', *, *, #24502, .T. ) ;
#28010=LINE ( 'NONE', #9386, #33121 ) ;
#28012=EDGE_LOOP ( 'NONE', ( #45477, #37354, #5146, #7359 ) ) ;
#28016=DIRECTION ( 'NONE',  ( -1.000000000000000000, -0.000000000000000000, 0.000000000000000000 ) ) ;
#28019=CIRCLE ( 'NONE', #45211, 31.99999999999999645 ) ;
#28029=ORIENTED_EDGE ( 'NONE', *, *, #26068, .T. ) ;
#28035=CIRCLE ( 'NONE', #1448, 77.49899999999999523 ) ;
#28036=EDGE_LOOP ( 'NONE', ( #37180, #167, #13749, #30423 ) ) ;
#28041=DIRECTION ( 'NONE',  ( 0.000000000000000000, -0.9510565162951500895, -0.3090169943749583870 ) ) ;
#28043=CARTESIAN_POINT ( 'NONE',  ( 0.000000000000000000, 67.80270845531887858, 46.11716303203210998 ) ) ;
#28046=FACE_OUTER_BOUND ( 'NONE', #9944, .T. ) ;
#28052=VERTEX_POINT ( 'NONE', #26046 ) ;
#28054=AXIS2_PLACEMENT_3D ( 'NONE', #46497, #13198, #20527 ) ;
#28057=AXIS2_PLACEMENT_3D ( 'NONE', #36795, #3262, #14050 ) ;
#28058=DIRECTION ( 'NONE',  ( 0.000000000000000000, -0.8526401643540859610, -0.5224985647159591240 ) ) ;
#28063=DIRECTION ( 'NONE',  ( 1.000000000000000000, 0.000000000000000000, 0.000000000000000000 ) ) ;
#28084=DIRECTION ( 'NONE',  ( -1.000000000000000000, 0.000000000000000000, -0.000000000000000000 ) ) ;
#28085=CARTESIAN_POINT ( 'NONE',  ( 0.000000000000000000, -67.80270845531855173, -46.11716303203261447 ) ) ;
#28092=DIRECTION ( 'NONE',  ( -1.000000000000000000, 0.000000000000000000, 0.000000000000000000 ) ) ;
#28093=LINE ( 'NONE', #43023, #6139 ) ;
#28094=CARTESIAN_POINT ( 'NONE',  ( 0.000000000000000000, -73.72996012237429397, -14.67089635893794508 ) ) ;
#28095=DIRECTION ( 'NONE',  ( -1.000000000000000000, 0.000000000000000000, -0.000000000000000000 ) ) ;
#28096=FACE_OUTER_BOUND ( 'NONE', #16994, .T. ) ;
#28100=CARTESIAN_POINT ( 'NONE',  ( 10.00000000000000000, 0.000000000000000000, 0.000000000000000000 ) ) ;
#28106=CARTESIAN_POINT ( 'NONE',  ( 5.000000000000000000, -56.15606465354917276, -59.75363087400133111 ) ) ;
#28109=CARTESIAN_POINT ( 'NONE',  ( 10.00000000000000000, 65.64334221924909230, 41.19522573413756561 ) ) ;
#28113=CARTESIAN_POINT ( 'NONE',  ( 10.00000000000000000, -77.49459641780886443, 0.8261519478428377417 ) ) ;
#28115=DIRECTION ( 'NONE',  ( -1.000000000000000000, 0.000000000000000000, 0.000000000000000000 ) ) ;
#28116=CARTESIAN_POINT ( 'NONE',  ( 0.000000000000000000, -59.46389618801999433, 49.70050353004867816 ) ) ;
#28122=ADVANCED_FACE ( 'NONE', ( #11848, #40505 ), #18694, .F. ) ;
#28129=CARTESIAN_POINT ( 'NONE',  ( 0.000000000000000000, 0.000000000000000000, 0.000000000000000000 ) ) ;
#28131=VERTEX_POINT ( 'NONE', #22131 ) ;
#28132=ORIENTED_EDGE ( 'NONE', *, *, #44320, .F. ) ;
#28146=DIRECTION ( 'NONE',  ( -1.000000000000000000, 0.000000000000000000, 0.000000000000000000 ) ) ;
#28147=VERTEX_POINT ( 'NONE', #38777 ) ;
#28148=CARTESIAN_POINT ( 'NONE',  ( 0.000000000000000000, 0.000000000000000000, 0.000000000000000000 ) ) ;
#28166=CARTESIAN_POINT ( 'NONE',  ( 0.000000000000000000, 14.66109333815460225, 73.73191006444577056 ) ) ;
#28173=CARTESIAN_POINT ( 'NONE',  ( 10.00000000000000000, -64.81221759200306565, -50.23322058963418613 ) ) ;
#28177=AXIS2_PLACEMENT_3D ( 'NONE', #15288, #7918, #45137 ) ;
#28178=AXIS2_PLACEMENT_3D ( 'NONE', #34995, #27920, #12490 ) ;
#28179=ADVANCED_FACE ( 'NONE', ( #8892 ), #5464, .T. ) ;
#28181=ORIENTED_EDGE ( 'NONE', *, *, #38803, .F. ) ;
#28183=CIRCLE ( 'NONE', #7064, 82.00000000000000000 ) ;
#28184=VECTOR ( 'NONE', #25979, 1000.000000000000000 ) ;
#28188=LINE ( 'NONE', #24045, #13575 ) ;
#28200=DIRECTION ( 'NONE',  ( -1.000000000000000000, 0.000000000000000000, -0.000000000000000000 ) ) ;
#28202=CARTESIAN_POINT ( 'NONE',  ( -10.00000000000000000, 0.000000000000000000, 0.000000000000000000 ) ) ;
#28203=LINE ( 'NONE', #28916, #43429 ) ;
#28206=LINE ( 'NONE', #9590, #5304 ) ;
#28211=ORIENTED_EDGE ( 'NONE', *, *, #2055, .T. ) ;
#28226=APPLICATION_CONTEXT ( 'automotive_design' ) ;
#28228=CARTESIAN_POINT ( 'NONE',  ( 0.000000000000000000, 0.000000000000000000, 0.000000000000000000 ) ) ;
#28235=EDGE_CURVE ( 'NONE', #36392, #42650, #21944, .T. ) ;
#28236=DIRECTION ( 'NONE',  ( -1.000000000000000000, -0.000000000000000000, 0.000000000000000000 ) ) ;
#28241=VECTOR ( 'NONE', #14553, 1000.000000000000000 ) ;
#28243=VECTOR ( 'NONE', #16893, 1000.000000000000000 ) ;
#28249=CIRCLE ( 'NONE', #46217, 77.49899999999999523 ) ;
#28251=ORIENTED_EDGE ( 'NONE', *, *, #16518, .F. ) ;
#28259=DIRECTION ( 'NONE',  ( 0.000000000000000000, 0.000000000000000000, 1.000000000000000000 ) ) ;
#28261=CARTESIAN_POINT ( 'NONE',  ( 0.000000000000000000, -55.16347631943085617, 60.67117009219118273 ) ) ;
#28263=VERTEX_POINT ( 'NONE', #30687 ) ;
#28266=DIRECTION ( 'NONE',  ( 0.000000000000000000, 0.000000000000000000, 1.000000000000000000 ) ) ;
#28267=FACE_OUTER_BOUND ( 'NONE', #23163, .T. ) ;
#28269=FACE_OUTER_BOUND ( 'NONE', #36395, .T. ) ;
#28277=ORIENTED_EDGE ( 'NONE', *, *, #13967, .F. ) ;
#28278=AXIS2_PLACEMENT_3D ( 'NONE', #12324, #1306, #38991 ) ;
#28280=EDGE_CURVE ( 'NONE', #25663, #31426, #41963, .T. ) ;
#28283=EDGE_CURVE ( 'NONE', #40440, #32991, #1796, .T. ) ;
#28288=DIRECTION ( 'NONE',  ( -1.000000000000000000, 0.000000000000000000, -0.000000000000000000 ) ) ;
#28289=ORIENTED_EDGE ( 'NONE', *, *, #25172, .T. ) ;
#28292=ORIENTED_EDGE ( 'NONE', *, *, #27640, .T. ) ;
#28293=EDGE_CURVE ( 'NONE', #15099, #41560, #46599, .T. ) ;
#28296=EDGE_CURVE ( 'NONE', #28502, #17893, #5535, .T. ) ;
#28305=VERTEX_POINT ( 'NONE', #6198 ) ;
#28310=ORIENTED_EDGE ( 'NONE', *, *, #16406, .T. ) ;
#28313=EDGE_LOOP ( 'NONE', ( #32693, #27475, #30180, #42268 ) ) ;
#28316=DIRECTION ( 'NONE',  ( 0.000000000000000000, 0.000000000000000000, 1.000000000000000000 ) ) ;
#28347=ORIENTED_EDGE ( 'NONE', *, *, #12425, .T. ) ;
#28360=CARTESIAN_POINT ( 'NONE',  ( 0.000000000000000000, -62.20884554313985149, -46.21855187248698371 ) ) ;
#28362=EDGE_LOOP ( 'NONE', ( #32528, #23435, #20168, #10442 ) ) ;
#28381=ORIENTED_EDGE ( 'NONE', *, *, #22695, .T. ) ;
#28385=CYLINDRICAL_SURFACE ( 'NONE', #20410, 31.99999999999998579 ) ;
#28386=AXIS2_PLACEMENT_3D ( 'NONE', #23831, #45364, #46104 ) ;
#28394=CARTESIAN_POINT ( 'NONE',  ( 10.00000000000000000, 0.000000000000000000, 0.000000000000000000 ) ) ;
#28396=DIRECTION ( 'NONE',  ( -1.000000000000000000, 0.000000000000000000, 0.000000000000000000 ) ) ;
#28404=CYLINDRICAL_SURFACE ( 'NONE', #7399, 82.00000000000000000 ) ;
#28405=CARTESIAN_POINT ( 'NONE',  ( 10.00000000000000000, 73.44644590900094272, -24.73286445877628026 ) ) ;
#28408=CARTESIAN_POINT ( 'NONE',  ( 10.00000000000000000, 0.000000000000000000, 0.000000000000000000 ) ) ;
#28411=EDGE_CURVE ( 'NONE', #34606, #36756, #3202, .T. ) ;
#28416=ADVANCED_FACE ( 'NONE', ( #39495 ), #2504, .T. ) ;
#28417=CYLINDRICAL_SURFACE ( 'NONE', #33844, 31.99999999999999289 ) ;
#28423=VERTEX_POINT ( 'NONE', #2271 ) ;
#28439=DIRECTION ( 'NONE',  ( -1.000000000000000000, -0.000000000000000000, -0.000000000000000000 ) ) ;
#28444=CARTESIAN_POINT ( 'NONE',  ( 10.00000000000000000, 77.32052557432849937, -5.256550761632002633 ) ) ;
#28448=CARTESIAN_POINT ( 'NONE',  ( 10.00000000000000000, -65.58780272294100655, 36.73666225445870737 ) ) ;
#28449=ORIENTED_EDGE ( 'NONE', *, *, #33105, .F. ) ;
#28456=DIRECTION ( 'NONE',  ( 0.000000000000000000, 0.000000000000000000, 1.000000000000000000 ) ) ;
#28462=DIRECTION ( 'NONE',  ( -1.000000000000000000, 0.000000000000000000, -0.000000000000000000 ) ) ;
#28465=CARTESIAN_POINT ( 'NONE',  ( 10.00000000000000000, -80.55351364060599906, 15.33399622253456940 ) ) ;
#28473=LINE ( 'NONE', #14258, #40297 ) ;
#28475=DIRECTION ( 'NONE',  ( 0.000000000000000000, 0.3826834323650841752, 0.9238795325112891810 ) ) ;
#28479=CARTESIAN_POINT ( 'NONE',  ( 0.000000000000000000, 0.000000000000000000, 0.000000000000000000 ) ) ;
#28480=FACE_OUTER_BOUND ( 'NONE', #24387, .T. ) ;
#28482=EDGE_LOOP ( 'NONE', ( #7834, #21700, #6567, #16435 ) ) ;
#28483=DIRECTION ( 'NONE',  ( 1.000000000000000000, -0.000000000000000000, -0.000000000000000000 ) ) ;
#28485=CARTESIAN_POINT ( 'NONE',  ( 0.000000000000000000, 0.000000000000000000, 0.000000000000000000 ) ) ;
#28493=DIRECTION ( 'NONE',  ( -1.000000000000000000, -0.000000000000000000, 0.000000000000000000 ) ) ;
#28494=ORIENTED_EDGE ( 'NONE', *, *, #46359, .T. ) ;
#28495=AXIS2_PLACEMENT_3D ( 'NONE', #12322, #27734, #42666 ) ;
#28496=VERTEX_POINT ( 'NONE', #22333 ) ;
#28497=ADVANCED_FACE ( 'NONE', ( #3220 ), #26482, .T. ) ;
#28501=DIRECTION ( 'NONE',  ( -1.000000000000000000, 0.000000000000000000, 0.000000000000000000 ) ) ;
#28502=VERTEX_POINT ( 'NONE', #4211 ) ;
#28504=CARTESIAN_POINT ( 'NONE',  ( 0.000000000000000000, 0.000000000000000000, 0.000000000000000000 ) ) ;
#28511=AXIS2_PLACEMENT_3D ( 'NONE', #29773, #44707, #19245 ) ;
#28519=EDGE_CURVE ( 'NONE', #4582, #17307, #11047, .T. ) ;
#28525=DIRECTION ( 'NONE',  ( 0.000000000000000000, -0.9876883405951359940, -0.1564344650402420267 ) ) ;
#28531=ORIENTED_EDGE ( 'NONE', *, *, #21101, .F. ) ;
#28539=AXIS2_PLACEMENT_3D ( 'NONE', #20669, #6230, #35348 ) ;
#28540=CIRCLE ( 'NONE', #8196, 31.99999999999998934 ) ;
#28541=FACE_OUTER_BOUND ( 'NONE', #47388, .T. ) ;
#28545=AXIS2_PLACEMENT_3D ( 'NONE', #20209, #27563, #42491 ) ;
#28546=ORIENTED_EDGE ( 'NONE', *, *, #36974, .T. ) ;
#28547=DIRECTION ( 'NONE',  ( 0.000000000000000000, 0.000000000000000000, 1.000000000000000000 ) ) ;
#28548=VECTOR ( 'NONE', #48131, 1000.000000000000000 ) ;
#28552=VERTEX_POINT ( 'NONE', #36996 ) ;
#28553=AXIS2_PLACEMENT_3D ( 'NONE', #4155, #7330, #18816 ) ;
#28560=AXIS2_PLACEMENT_3D ( 'NONE', #40447, #21598, #6903 ) ;
#28567=DIRECTION ( 'NONE',  ( -1.000000000000000000, 0.000000000000000000, 0.000000000000000000 ) ) ;
#28574=ORIENTED_EDGE ( 'NONE', *, *, #41729, .T. ) ;
#28585=DIRECTION ( 'NONE',  ( -1.000000000000000000, 0.000000000000000000, 0.000000000000000000 ) ) ;
#28588=ORIENTED_EDGE ( 'NONE', *, *, #29218, .F. ) ;
#28593=CARTESIAN_POINT ( 'NONE',  ( 10.00000000000000000, -77.32052557432837148, -5.256550761633697277 ) ) ;
#28606=DIRECTION ( 'NONE',  ( 0.000000000000000000, -0.1564344650402381687, 0.9876883405951365491 ) ) ;
#28608=ORIENTED_EDGE ( 'NONE', *, *, #31766, .F. ) ;
#28609=VERTEX_POINT ( 'NONE', #4921 ) ;
#28610=ORIENTED_EDGE ( 'NONE', *, *, #43769, .T. ) ;
#28614=CARTESIAN_POINT ( 'NONE',  ( 0.000000000000000000, 63.18004540533092239, -44.88180994100307686 ) ) ;
#28615=VERTEX_POINT ( 'NONE', #12755 ) ;
#28617=DIRECTION ( 'NONE',  ( 0.000000000000000000, 0.000000000000000000, 1.000000000000000000 ) ) ;
#28626=DIRECTION ( 'NONE',  ( 0.000000000000000000, 0.000000000000000000, 1.000000000000000000 ) ) ;
#28637=EDGE_LOOP ( 'NONE', ( #11217, #26508, #39865, #31643 ) ) ;
#28641=ORIENTED_EDGE ( 'NONE', *, *, #10167, .T. ) ;
#28643=DIRECTION ( 'NONE',  ( 0.000000000000000000, 0.000000000000000000, 1.000000000000000000 ) ) ;
#28644=ORIENTED_EDGE ( 'NONE', *, *, #15817, .F. ) ;
#28653=ORIENTED_EDGE ( 'NONE', *, *, #8512, .T. ) ;
#28654=CIRCLE ( 'NONE', #7548, 32.00000000000000000 ) ;
#28658=DIRECTION ( 'NONE',  ( 0.000000000000000000, 0.000000000000000000, 1.000000000000000000 ) ) ;
#28660=CIRCLE ( 'NONE', #37248, 77.49900000000000944 ) ;
#28661=DIRECTION ( 'NONE',  ( -1.000000000000000000, 0.000000000000000000, 0.000000000000000000 ) ) ;
#28666=AXIS2_PLACEMENT_3D ( 'NONE', #19258, #22684, #18539 ) ;
#28672=CIRCLE ( 'NONE', #26328, 77.49899999999999523 ) ;
#28674=EDGE_CURVE ( 'NONE', #18434, #43657, #22748, .T. ) ;
#28678=ADVANCED_FACE ( 'NONE', ( #41646 ), #15466, .T. ) ;
#28679=VECTOR ( 'NONE', #6323, 1000.000000000000000 ) ;
#28683=VERTEX_POINT ( 'NONE', #758 ) ;
#28685=VECTOR ( 'NONE', #42926, 1000.000000000000000 ) ;
#28688=FACE_OUTER_BOUND ( 'NONE', #36890, .T. ) ;
#28692=CARTESIAN_POINT ( 'NONE',  ( 10.00000000000000000, -17.28742895386139722, 75.54627589209937355 ) ) ;
#28694=DIRECTION ( 'NONE',  ( -1.000000000000000000, 0.000000000000000000, -0.000000000000000000 ) ) ;
#28703=EDGE_CURVE ( 'NONE', #18490, #18399, #33748, .T. ) ;
#28705=ORIENTED_EDGE ( 'NONE', *, *, #37922, .T. ) ;
#28709=VERTEX_POINT ( 'NONE', #43751 ) ;
#28711=CYLINDRICAL_SURFACE ( 'NONE', #10400, 77.49899999999999523 ) ;
#28713=EDGE_CURVE ( 'NONE', #14416, #40294, #26705, .T. ) ;
#28714=DIRECTION ( 'NONE',  ( -1.000000000000000000, -0.000000000000000000, -0.000000000000000000 ) ) ;
#28715=CIRCLE ( 'NONE', #26373, 77.49899999999999523 ) ;
#28718=CARTESIAN_POINT ( 'NONE',  ( 5.000000000000002665, -39.47590169984897557, 71.87247863392401825 ) ) ;
#28719=CARTESIAN_POINT ( 'NONE',  ( 10.00000000000000000, -41.76106447765443619, -62.50884508063471401 ) ) ;
#28720=AXIS2_PLACEMENT_3D ( 'NONE', #19718, #22681, #30289 ) ;
#28721=DIRECTION ( 'NONE',  ( 0.000000000000000000, 0.000000000000000000, 1.000000000000000000 ) ) ;
#28726=VERTEX_POINT ( 'NONE', #14634 ) ;
#28732=EDGE_CURVE ( 'NONE', #2823, #3259, #36855, .T. ) ;
#28747=CARTESIAN_POINT ( 'NONE',  ( 10.00000000000000000, 0.000000000000000000, 0.000000000000000000 ) ) ;
#28750=DIRECTION ( 'NONE',  ( -1.000000000000000000, -0.000000000000000000, -0.000000000000000000 ) ) ;
#28764=DIRECTION ( 'NONE',  ( 1.000000000000000000, -0.000000000000000000, -0.000000000000000000 ) ) ;
#28768=ORIENTED_EDGE ( 'NONE', *, *, #36720, .F. ) ;
#28770=CARTESIAN_POINT ( 'NONE',  ( 10.00000000000000000, 46.53671651294032330, -59.03961581697353012 ) ) ;
#28773=EDGE_CURVE ( 'NONE', #34988, #19466, #45455, .T. ) ;
#28775=DIRECTION ( 'NONE',  ( 1.000000000000000000, 0.000000000000000000, 0.000000000000000000 ) ) ;
#28777=DIRECTION ( 'NONE',  ( -1.000000000000000000, -0.000000000000000000, 0.000000000000000000 ) ) ;
#28783=ORIENTED_EDGE ( 'NONE', *, *, #22914, .T. ) ;
#28788=ORIENTED_EDGE ( 'NONE', *, *, #6394, .F. ) ;
#28789=EDGE_CURVE ( 'NONE', #41579, #35990, #15008, .T. ) ;
#28792=EDGE_CURVE ( 'NONE', #20404, #7367, #5610, .T. ) ;
#28800=FACE_OUTER_BOUND ( 'NONE', #22232, .T. ) ;
#28806=VERTEX_POINT ( 'NONE', #25141 ) ;
#28812=CARTESIAN_POINT ( 'NONE',  ( 0.000000000000000000, -21.60688246758642705, 79.10210256391360417 ) ) ;
#28813=AXIS2_PLACEMENT_3D ( 'NONE', #34379, #37348, #129 ) ;
#28818=ORIENTED_EDGE ( 'NONE', *, *, #9482, .F. ) ;
#28820=VERTEX_POINT ( 'NONE', #10465 ) ;
#28828=CARTESIAN_POINT ( 'NONE',  ( 0.000000000000000000, 74.65491531819118620, 23.16904090965733332 ) ) ;
#28838=EDGE_CURVE ( 'NONE', #41574, #35415, #17324, .T. ) ;
#28848=MECHANICAL_DESIGN_GEOMETRIC_PRESENTATION_REPRESENTATION('',(#15484),#38160);
#28864=CYLINDRICAL_SURFACE ( 'NONE', #32259, 82.00000000000000000 ) ;
#28866=ORIENTED_EDGE ( 'NONE', *, *, #7186, .F. ) ;
#28868=VECTOR ( 'NONE', #24153, 1000.000000000000000 ) ;
#28876=AXIS2_PLACEMENT_3D ( 'NONE', #41219, #7675, #44637 ) ;
#28878=EDGE_CURVE ( 'NONE', #10782, #23867, #40780, .T. ) ;
#28879=CARTESIAN_POINT ( 'NONE',  ( 5.000000000000000000, -55.16347631942998220, -60.67117009219196433 ) ) ;
#28881=DIRECTION ( 'NONE',  ( -1.000000000000000000, 0.000000000000000000, -0.000000000000000000 ) ) ;
#28883=EDGE_CURVE ( 'NONE', #30814, #9128, #46238, .T. ) ;
#28885=ORIENTED_EDGE ( 'NONE', *, *, #28883, .T. ) ;
#28889=DIRECTION ( 'NONE',  ( 1.000000000000000000, 0.000000000000000000, -0.000000000000000000 ) ) ;
#28894=CIRCLE ( 'NONE', #25777, 77.49899999999999523 ) ;
#28896=DIRECTION ( 'NONE',  ( -1.000000000000000000, 0.000000000000000000, -0.000000000000000000 ) ) ;
#28903=CARTESIAN_POINT ( 'NONE',  ( 0.000000000000000000, 17.28742895386084655, 75.54627589209950145 ) ) ;
#28910=ORIENTED_EDGE ( 'NONE', *, *, #2631, .T. ) ;
#28916=CARTESIAN_POINT ( 'NONE',  ( 5.000000000000002665, -80.55351364060599906, 15.33399622253456585 ) ) ;
#28919=ORIENTED_EDGE ( 'NONE', *, *, #21370, .F. ) ;
#28922=CARTESIAN_POINT ( 'NONE',  ( 10.00000000000000000, 2.946379043147425492, -75.11764819372145041 ) ) ;
#28924=DIRECTION ( 'NONE',  ( 0.000000000000000000, -0.3826834323650772363, -0.9238795325112919565 ) ) ;
#28938=CIRCLE ( 'NONE', #14096, 77.49899999999999523 ) ;
#28939=ADVANCED_FACE ( 'NONE', ( #12176 ), #34179, .T. ) ;
#28943=LINE ( 'NONE', #25747, #47222 ) ;
#28944=LINE ( 'NONE', #21617, #12333 ) ;
#28946=EDGE_CURVE ( 'NONE', #39579, #28806, #36100, .T. ) ;
#28948=CIRCLE ( 'NONE', #23566, 31.99999999999999289 ) ;
#28953=CYLINDRICAL_SURFACE ( 'NONE', #22191, 77.49899999999999523 ) ;
#28954=EDGE_CURVE ( 'NONE', #12529, #15618, #3845, .T. ) ;
#28957=ORIENTED_EDGE ( 'NONE', *, *, #26877, .T. ) ;
#28960=DIRECTION ( 'NONE',  ( -1.000000000000000000, -0.000000000000000000, -0.000000000000000000 ) ) ;
#28964=DIRECTION ( 'NONE',  ( 1.000000000000000000, 0.000000000000000000, 0.000000000000000000 ) ) ;
#28965=ORIENTED_EDGE ( 'NONE', *, *, #16082, .F. ) ;
#28966=DIRECTION ( 'NONE',  ( 0.000000000000000000, 0.000000000000000000, -1.000000000000000000 ) ) ;
#28970=ORIENTED_EDGE ( 'NONE', *, *, #12897, .F. ) ;
#28973=AXIS2_PLACEMENT_3D ( 'NONE', #38442, #12743, #9072 ) ;
#28978=CIRCLE ( 'NONE', #4777, 82.00000000000000000 ) ;
#28981=VERTEX_POINT ( 'NONE', #37131 ) ;
#28983=CARTESIAN_POINT ( 'NONE',  ( 0.000000000000000000, -2.946379043145784582, -75.11764819372150725 ) ) ;
#28986=EDGE_LOOP ( 'NONE', ( #30388, #16481, #23728, #29830 ) ) ;
#28987=CARTESIAN_POINT ( 'NONE',  ( 0.000000000000000000, 1.530808498934191521E-15, -12.50000000000000000 ) ) ;
#28988=DIRECTION ( 'NONE',  ( -1.000000000000000000, 0.000000000000000000, 0.000000000000000000 ) ) ;
#28993=ORIENTED_EDGE ( 'NONE', *, *, #10719, .F. ) ;
#28994=ORIENTED_EDGE ( 'NONE', *, *, #16008, .F. ) ;
#28996=ADVANCED_FACE ( 'NONE', ( #45208 ), #39303, .T. ) ;
#28999=ADVANCED_FACE ( 'NONE', ( #5779 ), #20700, .T. ) ;
#29002=CARTESIAN_POINT ( 'NONE',  ( 10.00000000000000000, 24.73286445877808148, -73.44644590900034586 ) ) ;
#29025=CARTESIAN_POINT ( 'NONE',  ( 10.00000000000000000, 50.95692526931328104, 58.39081064771769292 ) ) ;
#29028=VERTEX_POINT ( 'NONE', #20450 ) ;
#29030=ORIENTED_EDGE ( 'NONE', *, *, #26060, .T. ) ;
#29039=ORIENTED_EDGE ( 'NONE', *, *, #21488, .F. ) ;
#29055=DIRECTION ( 'NONE',  ( -1.000000000000000000, 0.000000000000000000, 0.000000000000000000 ) ) ;
#29056=ORIENTED_EDGE ( 'NONE', *, *, #24051, .F. ) ;
#29060=ORIENTED_EDGE ( 'NONE', *, *, #28293, .F. ) ;
#29063=ADVANCED_FACE ( 'NONE', ( #46661 ), #13124, .T. ) ;
#29064=DIRECTION ( 'NONE',  ( 0.000000000000000000, -0.5224985647159380298, -0.8526401643540988395 ) ) ;
#29071=ADVANCED_FACE ( 'NONE', ( #9431 ), #38339, .T. ) ;
#29072=ORIENTED_EDGE ( 'NONE', *, *, #25751, .T. ) ;
#29074=ORIENTED_EDGE ( 'NONE', *, *, #3294, .F. ) ;
#29075=ORIENTED_EDGE ( 'NONE', *, *, #38235, .T. ) ;
#29076=CIRCLE ( 'NONE', #26741, 77.49900000000000944 ) ;
#29082=CARTESIAN_POINT ( 'NONE',  ( 10.00000000000000000, 18.89407956138362010, -75.16055320797013906 ) ) ;
#29089=ORIENTED_EDGE ( 'NONE', *, *, #19067, .F. ) ;
#29091=ORIENTED_EDGE ( 'NONE', *, *, #37932, .T. ) ;
#29093=CARTESIAN_POINT ( 'NONE',  ( 0.000000000000000000, -81.90746397400386059, -3.894527615418773347 ) ) ;
#29095=EDGE_LOOP ( 'NONE', ( #7426, #47732, #13059, #36653 ) ) ;
#29097=VECTOR ( 'NONE', #27275, 1000.000000000000000 ) ;
#29101=ORIENTED_EDGE ( 'NONE', *, *, #44320, .T. ) ;
#29111=EDGE_CURVE ( 'NONE', #39094, #28609, #42395, .T. ) ;
#29112=CARTESIAN_POINT ( 'NONE',  ( 0.000000000000000000, -65.58780272294048075, -36.73666225445966660 ) ) ;
#29113=CYLINDRICAL_SURFACE ( 'NONE', #18541, 32.00000000000000000 ) ;
#29115=DIRECTION ( 'NONE',  ( 0.000000000000000000, 0.000000000000000000, 1.000000000000000000 ) ) ;
#29122=ORIENTED_EDGE ( 'NONE', *, *, #32639, .T. ) ;
#29124=VERTEX_POINT ( 'NONE', #32450 ) ;
#29130=ORIENTED_EDGE ( 'NONE', *, *, #46467, .T. ) ;
#29135=AXIS2_PLACEMENT_3D ( 'NONE', #26409, #30325, #689 ) ;
#29138=AXIS2_PLACEMENT_3D ( 'NONE', #16354, #31791, #13163 ) ;
#29146=CIRCLE ( 'NONE', #24445, 82.00000000000000000 ) ;
#29147=EDGE_CURVE ( 'NONE', #40538, #20444, #29076, .T. ) ;
#29149=DIRECTION ( 'NONE',  ( 0.000000000000000000, -0.8090169943749531134, 0.5877852522924653655 ) ) ;
#29154=DIRECTION ( 'NONE',  ( -1.000000000000000000, 0.000000000000000000, -0.000000000000000000 ) ) ;
#29156=CARTESIAN_POINT ( 'NONE',  ( 10.00000000000000000, 0.000000000000000000, 0.000000000000000000 ) ) ;
#29160=VERTEX_POINT ( 'NONE', #24619 ) ;
#29164=CARTESIAN_POINT ( 'NONE',  ( 10.00000000000000000, -20.40083707022829174, -72.35432306680507963 ) ) ;
#29169=EDGE_CURVE ( 'NONE', #16520, #40761, #11125, .T. ) ;
#29178=CARTESIAN_POINT ( 'NONE',  ( -10.00000000000000000, 0.000000000000000000, 0.000000000000000000 ) ) ;
#29182=CIRCLE ( 'NONE', #234, 77.49899999999999523 ) ;
#29183=CIRCLE ( 'NONE', #45601, 31.99999999999999289 ) ;
#29207=ORIENTED_EDGE ( 'NONE', *, *, #23886, .T. ) ;
#29210=ADVANCED_FACE ( 'NONE', ( #2566 ), #14318, .T. ) ;
#29212=ORIENTED_EDGE ( 'NONE', *, *, #25453, .F. ) ;
#29214=VECTOR ( 'NONE', #24842, 1000.000000000000000 ) ;
#29218=EDGE_CURVE ( 'NONE', #15461, #28709, #18895, .T. ) ;
#29219=ORIENTED_EDGE ( 'NONE', *, *, #40833, .T. ) ;
#29222=ORIENTED_EDGE ( 'NONE', *, *, #7186, .T. ) ;
#29223=DIRECTION ( 'NONE',  ( 0.000000000000000000, 0.000000000000000000, 1.000000000000000000 ) ) ;
#29225=DIRECTION ( 'NONE',  ( 0.000000000000000000, 0.000000000000000000, -1.000000000000000000 ) ) ;
#29228=AXIS2_PLACEMENT_3D ( 'NONE', #21359, #42692, #24805 ) ;
#29232=ORIENTED_EDGE ( 'NONE', *, *, #26258, .F. ) ;
#29234=DIRECTION ( 'NONE',  ( -1.000000000000000000, -0.000000000000000000, -0.000000000000000000 ) ) ;
#29237=CARTESIAN_POINT ( 'NONE',  ( 10.00000000000000000, 0.000000000000000000, 0.000000000000000000 ) ) ;
#29238=FACE_OUTER_BOUND ( 'NONE', #27673, .T. ) ;
#29240=DIRECTION ( 'NONE',  ( 1.000000000000000000, -0.000000000000000000, -0.000000000000000000 ) ) ;
#29244=EDGE_CURVE ( 'NONE', #17337, #41232, #20945, .T. ) ;
#29249=CARTESIAN_POINT ( 'NONE',  ( 10.00000000000000000, 74.65491531819105830, 8.830959090343693418 ) ) ;
#29250=DIRECTION ( 'NONE',  ( -1.000000000000000000, 0.000000000000000000, -0.000000000000000000 ) ) ;
#29251=CYLINDRICAL_SURFACE ( 'NONE', #20590, 32.00000000000000000 ) ;
#29264=ORIENTED_EDGE ( 'NONE', *, *, #9933, .F. ) ;
#29266=CIRCLE ( 'NONE', #40217, 82.00000000000000000 ) ;
#29267=VERTEX_POINT ( 'NONE', #44902 ) ;
#29270=AXIS2_PLACEMENT_3D ( 'NONE', #43055, #12715, #12476 ) ;
#29274=VERTEX_POINT ( 'NONE', #19194 ) ;
#29275=EDGE_CURVE ( 'NONE', #38428, #2295, #19689, .T. ) ;
#29278=DIRECTION ( 'NONE',  ( 0.000000000000000000, 0.000000000000000000, 1.000000000000000000 ) ) ;
#29279=VERTEX_POINT ( 'NONE', #99 ) ;
#29281=ORIENTED_EDGE ( 'NONE', *, *, #41969, .T. ) ;
#29287=CARTESIAN_POINT ( 'NONE',  ( 5.000000000000002665, 78.73519480814985627, -22.90783923731548199 ) ) ;
#29289=CARTESIAN_POINT ( 'NONE',  ( 10.00000000000000000, 39.47590169984943742, -71.87247863392373404 ) ) ;
#29295=AXIS2_PLACEMENT_3D ( 'NONE', #9661, #32194, #28266 ) ;
#29296=CARTESIAN_POINT ( 'NONE',  ( 10.00000000000000000, -74.65491531819124305, 8.830959090342128448 ) ) ;
#29309=EDGE_LOOP ( 'NONE', ( #8361, #30469, #48342, #4307 ) ) ;
#29315=DIRECTION ( 'NONE',  ( -1.000000000000000000, -0.000000000000000000, -0.000000000000000000 ) ) ;
#29323=CIRCLE ( 'NONE', #14469, 77.49899999999999523 ) ;
#29326=ORIENTED_EDGE ( 'NONE', *, *, #18419, .F. ) ;
#29327=ORIENTED_EDGE ( 'NONE', *, *, #28838, .F. ) ;
#29329=VECTOR ( 'NONE', #12099, 1000.000000000000000 ) ;
#29331=CARTESIAN_POINT ( 'NONE',  ( -10.00000000000000000, 0.000000000000000000, 0.000000000000000000 ) ) ;
#29333=CIRCLE ( 'NONE', #28539, 31.99999999999998934 ) ;
#29334=AXIS2_PLACEMENT_3D ( 'NONE', #32645, #17945, #36079 ) ;
#29335=DIRECTION ( 'NONE',  ( -1.000000000000000000, 0.000000000000000000, -0.000000000000000000 ) ) ;
#29347=EDGE_CURVE ( 'NONE', #10009, #9517, #47075, .T. ) ;
#29353=ORIENTED_EDGE ( 'NONE', *, *, #33535, .F. ) ;
#29354=VERTEX_POINT ( 'NONE', #25803 ) ;
#29356=VECTOR ( 'NONE', #32152, 1000.000000000000000 ) ;
#29360=CARTESIAN_POINT ( 'NONE',  ( 10.00000000000000000, 0.000000000000000000, 0.000000000000000000 ) ) ;
#29365=CARTESIAN_POINT ( 'NONE',  ( 10.00000000000000000, -75.54627589209955829, 17.28742895386058009 ) ) ;
#29368=LINE ( 'NONE', #47481, #24982 ) ;
#29376=FACE_OUTER_BOUND ( 'NONE', #29446, .T. ) ;
#29378=AXIS2_PLACEMENT_3D ( 'NONE', #30441, #4729, #19641 ) ;
#29380=VERTEX_POINT ( 'NONE', #15049 ) ;
#29387=VECTOR ( 'NONE', #4518, 1000.000000000000000 ) ;
#29388=CARTESIAN_POINT ( 'NONE',  ( 5.000000000000002665, -81.50828551894220197, -8.966570791701590437 ) ) ;
#29390=EDGE_CURVE ( 'NONE', #26518, #13379, #25951, .T. ) ;
#29394=CYLINDRICAL_SURFACE ( 'NONE', #46138, 77.49899999999999523 ) ;
#29398=ORIENTED_EDGE ( 'NONE', *, *, #20967, .T. ) ;
#29403=VECTOR ( 'NONE', #14415, 1000.000000000000000 ) ;
#29405=EDGE_CURVE ( 'NONE', #10399, #47783, #10348, .T. ) ;
#29419=CARTESIAN_POINT ( 'NONE',  ( 10.00000000000000000, 0.000000000000000000, 0.000000000000000000 ) ) ;
#29421=VERTEX_POINT ( 'NONE', #35327 ) ;
#29422=CARTESIAN_POINT ( 'NONE',  ( 5.000000000000002665, 81.90746397400387480, 3.894527615418187150 ) ) ;
#29423=CARTESIAN_POINT ( 'NONE',  ( 10.00000000000000000, 5.256550761633969060, -77.32052557432835727 ) ) ;
#29425=CARTESIAN_POINT ( 'NONE',  ( 10.00000000000000000, 0.000000000000000000, 0.000000000000000000 ) ) ;
#29426=CIRCLE ( 'NONE', #13017, 31.99999999999998934 ) ;
#29428=DIRECTION ( 'NONE',  ( -1.000000000000000000, -0.000000000000000000, 0.000000000000000000 ) ) ;
#29430=AXIS2_PLACEMENT_3D ( 'NONE', #25716, #33555, #22048 ) ;
#29433=CYLINDRICAL_SURFACE ( 'NONE', #10657, 31.99999999999998579 ) ;
#29434=VERTEX_POINT ( 'NONE', #27515 ) ;
#29437=DIRECTION ( 'NONE',  ( -1.000000000000000000, -0.000000000000000000, -0.000000000000000000 ) ) ;
#29441=CARTESIAN_POINT ( 'NONE',  ( 10.00000000000000000, -6.903761155838323837, 77.19088730480521576 ) ) ;
#29445=CARTESIAN_POINT ( 'NONE',  ( 10.00000000000000000, 0.000000000000000000, 0.000000000000000000 ) ) ;
#29446=EDGE_LOOP ( 'NONE', ( #15538, #6901, #19888, #9499 ) ) ;
#29447=DIRECTION ( 'NONE',  ( -1.000000000000000000, -0.000000000000000000, 0.000000000000000000 ) ) ;
#29455=EDGE_CURVE ( 'NONE', #17495, #44907, #16495, .T. ) ;
#29460=DIRECTION ( 'NONE',  ( 0.000000000000000000, 0.7604059656000322631, -0.6494480483301821039 ) ) ;
#29463=CARTESIAN_POINT ( 'NONE',  ( 10.00000000000000000, -73.73191006444582740, 14.66109333815435889 ) ) ;
#29470=CARTESIAN_POINT ( 'NONE',  ( 10.00000000000000000, -60.67117009219176538, 55.16347631943019536 ) ) ;
#29474=ORIENTED_EDGE ( 'NONE', *, *, #28235, .F. ) ;
#29475=DIRECTION ( 'NONE',  ( 0.000000000000000000, -0.2334453638558921240, -0.9723699203976797767 ) ) ;
#29476=CIRCLE ( 'NONE', #12307, 77.49899999999999523 ) ;
#29479=FACE_OUTER_BOUND ( 'NONE', #41826, .T. ) ;
#29486=ORIENTED_EDGE ( 'NONE', *, *, #15379, .T. ) ;
#29487=AXIS2_PLACEMENT_3D ( 'NONE', #43640, #2508, #28475 ) ;
#29489=CARTESIAN_POINT ( 'NONE',  ( 10.00000000000000000, 0.000000000000000000, 0.000000000000000000 ) ) ;
#29492=LINE ( 'NONE', #43933, #23735 ) ;
#29494=CIRCLE ( 'NONE', #24019, 77.49899999999999523 ) ;
#29495=ADVANCED_FACE ( 'NONE', ( #39248 ), #38529, .T. ) ;
#29496=LINE ( 'NONE', #22400, #2895 ) ;
#29500=EDGE_CURVE ( 'NONE', #29885, #13511, #35357, .T. ) ;
#29502=DIRECTION ( 'NONE',  ( 0.000000000000000000, 0.3090169943749483394, -0.9510565162951534202 ) ) ;
#29503=ORIENTED_EDGE ( 'NONE', *, *, #25962, .F. ) ;
#29512=EDGE_CURVE ( 'NONE', #1317, #17390, #30957, .T. ) ;
#29514=ORIENTED_EDGE ( 'NONE', *, *, #42095, .T. ) ;
#29515=AXIS2_PLACEMENT_3D ( 'NONE', #14018, #10337, #34292 ) ;
#29517=DIRECTION ( 'NONE',  ( -1.000000000000000000, -0.000000000000000000, 0.000000000000000000 ) ) ;
#29519=ORIENTED_EDGE ( 'NONE', *, *, #23063, .T. ) ;
#29521=EDGE_LOOP ( 'NONE', ( #10536, #44334, #39216, #40040 ) ) ;
#29522=ORIENTED_EDGE ( 'NONE', *, *, #34927, .F. ) ;
#29525=PRODUCT_DEFINITION ( 'UNKNOWN', '', #17044, #40877 ) ;
#29530=VERTEX_POINT ( 'NONE', #16263 ) ;
#29534=DIRECTION ( 'NONE',  ( 1.000000000000000000, 0.000000000000000000, 0.000000000000000000 ) ) ;
#29543=ORIENTED_EDGE ( 'NONE', *, *, #22102, .F. ) ;
#29544=CARTESIAN_POINT ( 'NONE',  ( 10.00000000000000000, -30.41916302227164337, 71.27951684758015460 ) ) ;
#29545=ORIENTED_EDGE ( 'NONE', *, *, #28296, .F. ) ;
#29546=CIRCLE ( 'NONE', #8435, 31.99999999999999289 ) ;
#29547=LINE ( 'NONE', #45207, #2702 ) ;
#29559=EDGE_CURVE ( 'NONE', #8522, #48048, #40091, .T. ) ;
#29572=CIRCLE ( 'NONE', #30358, 77.49900000000000944 ) ;
#29575=CIRCLE ( 'NONE', #41327, 82.00000000000000000 ) ;
#29576=EDGE_CURVE ( 'NONE', #21501, #24420, #29917, .T. ) ;
#29595=CARTESIAN_POINT ( 'NONE',  ( 10.00000000000000000, 34.94270380257639630, 74.18225833017902460 ) ) ;
#29601=DIRECTION ( 'NONE',  ( -1.000000000000000000, -0.000000000000000000, -0.000000000000000000 ) ) ;
#29607=CARTESIAN_POINT ( 'NONE',  ( 0.000000000000000000, 0.000000000000000000, 0.000000000000000000 ) ) ;
#29608=CARTESIAN_POINT ( 'NONE',  ( 10.00000000000000000, 0.000000000000000000, 0.000000000000000000 ) ) ;
#29610=AXIS2_PLACEMENT_3D ( 'NONE', #19167, #48304, #26025 ) ;
#29611=DIRECTION ( 'NONE',  ( 0.000000000000000000, 0.000000000000000000, 1.000000000000000000 ) ) ;
#29616=CYLINDRICAL_SURFACE ( 'NONE', #40116, 31.99999999999999289 ) ;
#29619=EDGE_CURVE ( 'NONE', #33614, #3193, #25996, .T. ) ;
#29620=AXIS2_PLACEMENT_3D ( 'NONE', #13733, #28661, #2225 ) ;
#29621=ADVANCED_FACE ( 'NONE', ( #2995 ), #9870, .T. ) ;
#29624=ORIENTED_EDGE ( 'NONE', *, *, #18937, .F. ) ;
#29627=ORIENTED_EDGE ( 'NONE', *, *, #23342, .F. ) ;
#29631=DIRECTION ( 'NONE',  ( -1.000000000000000000, 0.000000000000000000, 0.000000000000000000 ) ) ;
#29632=AXIS2_PLACEMENT_3D ( 'NONE', #1410, #38618, #8986 ) ;
#29633=ORIENTED_EDGE ( 'NONE', *, *, #7397, .T. ) ;
#29641=DIRECTION ( 'NONE',  ( -1.000000000000000000, 0.000000000000000000, 0.000000000000000000 ) ) ;
#29642=DIRECTION ( 'NONE',  ( -1.000000000000000000, 0.000000000000000000, 0.000000000000000000 ) ) ;
#29643=EDGE_LOOP ( 'NONE', ( #41615, #31491, #22053, #9058 ) ) ;
#29647=ORIENTED_EDGE ( 'NONE', *, *, #22877, .F. ) ;
#29649=ORIENTED_EDGE ( 'NONE', *, *, #14519, .T. ) ;
#29652=CARTESIAN_POINT ( 'NONE',  ( 10.00000000000000000, -65.59268652807183742, -36.72794159290312166 ) ) ;
#29653=DIRECTION ( 'NONE',  ( -1.000000000000000000, -0.000000000000000000, 0.000000000000000000 ) ) ;
#29657=DIRECTION ( 'NONE',  ( 0.000000000000000000, 0.000000000000000000, 1.000000000000000000 ) ) ;
#29659=DIRECTION ( 'NONE',  ( -1.000000000000000000, 0.000000000000000000, 0.000000000000000000 ) ) ;
#29664=DIRECTION ( 'NONE',  ( 0.000000000000000000, 0.000000000000000000, 1.000000000000000000 ) ) ;
#29665=CYLINDRICAL_SURFACE ( 'NONE', #46620, 82.00000000000000000 ) ;
#29669=DIRECTION ( 'NONE',  ( -1.000000000000000000, 0.000000000000000000, -0.000000000000000000 ) ) ;
#29678=AXIS2_PLACEMENT_3D ( 'NONE', #21445, #14105, #43957 ) ;
#29680=EDGE_CURVE ( 'NONE', #25106, #12844, #22572, .T. ) ;
#29685=VERTEX_POINT ( 'NONE', #48273 ) ;
#29690=CARTESIAN_POINT ( 'NONE',  ( 10.00000000000000000, 0.000000000000000000, 0.000000000000000000 ) ) ;
#29691=DIRECTION ( 'NONE',  ( -1.000000000000000000, 0.000000000000000000, -0.000000000000000000 ) ) ;
#29696=DIRECTION ( 'NONE',  ( 0.000000000000000000, 0.2334453638559060296, -0.9723699203976764460 ) ) ;
#29702=ORIENTED_EDGE ( 'NONE', *, *, #25751, .F. ) ;
#29710=CARTESIAN_POINT ( 'NONE',  ( 0.000000000000000000, 26.02418014898310261, 70.52718814184268581 ) ) ;
#29712=ORIENTED_EDGE ( 'NONE', *, *, #37162, .T. ) ;
#29721=DIRECTION ( 'NONE',  ( -1.000000000000000000, 0.000000000000000000, -0.000000000000000000 ) ) ;
#29725=CARTESIAN_POINT ( 'NONE',  ( 0.000000000000000000, 0.000000000000000000, 0.000000000000000000 ) ) ;
#29727=EDGE_CURVE ( 'NONE', #30166, #38428, #15244, .T. ) ;
#29737=ORIENTED_EDGE ( 'NONE', *, *, #20476, .T. ) ;
#29745=CARTESIAN_POINT ( 'NONE',  ( 5.000000000000002665, -79.10210256391383155, 21.60688246758557796 ) ) ;
#29746=VERTEX_POINT ( 'NONE', #26729 ) ;
#29750=AXIS2_PLACEMENT_3D ( 'NONE', #16849, #6076, #34703 ) ;
#29752=CARTESIAN_POINT ( 'NONE',  ( 10.00000000000000000, -24.73286445877653961, -73.44644590900085745 ) ) ;
#29759=DIRECTION ( 'NONE',  ( 0.000000000000000000, 0.000000000000000000, 1.000000000000000000 ) ) ;
#29763=ORIENTED_EDGE ( 'NONE', *, *, #10436, .F. ) ;
#29770=DIRECTION ( 'NONE',  ( 0.000000000000000000, 0.000000000000000000, 1.000000000000000000 ) ) ;
#29773=CARTESIAN_POINT ( 'NONE',  ( 10.00000000000000000, 0.000000000000000000, 0.000000000000000000 ) ) ;
#29791=CARTESIAN_POINT ( 'NONE',  ( 5.000000000000000000, -46.11716303203136391, -67.80270845531939017 ) ) ;
#29793=CIRCLE ( 'NONE', #37581, 82.00000000000000000 ) ;
#29796=EDGE_CURVE ( 'NONE', #9950, #9128, #22340, .T. ) ;
#29797=LINE ( 'NONE', #48395, #17467 ) ;
#29798=ORIENTED_EDGE ( 'NONE', *, *, #7746, .F. ) ;
#29808=ORIENTED_EDGE ( 'NONE', *, *, #32337, .F. ) ;
#29810=AXIS2_PLACEMENT_3D ( 'NONE', #28100, #10208, #5587 ) ;
#29812=ORIENTED_EDGE ( 'NONE', *, *, #40514, .F. ) ;
#29815=ORIENTED_EDGE ( 'NONE', *, *, #33746, .F. ) ;
#29830=ORIENTED_EDGE ( 'NONE', *, *, #29390, .T. ) ;
#29835=DIRECTION ( 'NONE',  ( -1.000000000000000000, 0.000000000000000000, 0.000000000000000000 ) ) ;
#29839=DIRECTION ( 'NONE',  ( 0.000000000000000000, 0.2334453638558991184, 0.9723699203976781114 ) ) ;
#29844=VECTOR ( 'NONE', #1780, 1000.000000000000000 ) ;
#29845=CARTESIAN_POINT ( 'NONE',  ( 5.000000000000002665, -10.30890764327323872, -81.34940948281348483 ) ) ;
#29848=AXIS2_PLACEMENT_3D ( 'NONE', #44452, #22180, #29759 ) ;
#29849=DIRECTION ( 'NONE',  ( -1.000000000000000000, -0.000000000000000000, 0.000000000000000000 ) ) ;
#29850=CARTESIAN_POINT ( 'NONE',  ( 10.00000000000000000, -39.78640506895653317, 66.50666863321987421 ) ) ;
#29852=CYLINDRICAL_SURFACE ( 'NONE', #12314, 31.99999999999999289 ) ;
#29853=CIRCLE ( 'NONE', #47048, 31.99999999999999289 ) ;
#29859=DIRECTION ( 'NONE',  ( -1.000000000000000000, 0.000000000000000000, -0.000000000000000000 ) ) ;
#29871=CYLINDRICAL_SURFACE ( 'NONE', #37572, 31.99999999999999289 ) ;
#29873=ORIENTED_EDGE ( 'NONE', *, *, #8569, .T. ) ;
#29883=DIRECTION ( 'NONE',  ( -1.000000000000000000, 0.000000000000000000, 0.000000000000000000 ) ) ;
#29885=VERTEX_POINT ( 'NONE', #27219 ) ;
#29890=DIRECTION ( 'NONE',  ( -1.000000000000000000, -0.000000000000000000, 0.000000000000000000 ) ) ;
#29892=ORIENTED_EDGE ( 'NONE', *, *, #35603, .T. ) ;
#29895=VECTOR ( 'NONE', #11927, 1000.000000000000000 ) ;
#29904=VERTEX_POINT ( 'NONE', #19597 ) ;
#29906=ADVANCED_FACE ( 'NONE', ( #37990 ), #1006, .T. ) ;
#29910=AXIS2_PLACEMENT_3D ( 'NONE', #13232, #43088, #9537 ) ;
#29914=AXIS2_PLACEMENT_3D ( 'NONE', #8378, #20583, #1518 ) ;
#29915=DIRECTION ( 'NONE',  ( -1.000000000000000000, -0.000000000000000000, -0.000000000000000000 ) ) ;
#29917=CIRCLE ( 'NONE', #25208, 82.00000000000000000 ) ;
#29918=EDGE_CURVE ( 'NONE', #2128, #25169, #12769, .T. ) ;
#29920=AXIS2_PLACEMENT_3D ( 'NONE', #29652, #6667, #25240 ) ;
#29923=CARTESIAN_POINT ( 'NONE',  ( 10.00000000000000000, -8.830959090341869100, -74.65491531819127147 ) ) ;
#29928=VECTOR ( 'NONE', #11868, 1000.000000000000000 ) ;
#29933=EDGE_CURVE ( 'NONE', #42774, #21856, #26802, .T. ) ;
#29940=EDGE_CURVE ( 'NONE', #21411, #17540, #23297, .T. ) ;
#29941=EDGE_CURVE ( 'NONE', #7495, #8522, #21349, .T. ) ;
#29944=CYLINDRICAL_SURFACE ( 'NONE', #11862, 31.99999999999998579 ) ;
#29947=CARTESIAN_POINT ( 'NONE',  ( 10.00000000000000000, 26.01480285779933510, -70.53064760720289428 ) ) ;
#29950=EDGE_CURVE ( 'NONE', #23745, #15994, #17625, .T. ) ;
#29951=AXIS2_PLACEMENT_3D ( 'NONE', #31481, #19958, #12626 ) ;
#29962=DIRECTION ( 'NONE',  ( -1.000000000000000000, 0.000000000000000000, 0.000000000000000000 ) ) ;
#29968=DIRECTION ( 'NONE',  ( -1.000000000000000000, 0.000000000000000000, 0.000000000000000000 ) ) ;
#29974=ADVANCED_FACE ( 'NONE', ( #25198 ), #5911, .T. ) ;
#29975=ORIENTED_EDGE ( 'NONE', *, *, #43121, .F. ) ;
#29978=DIRECTION ( 'NONE',  ( -1.000000000000000000, 0.000000000000000000, 0.000000000000000000 ) ) ;
#29979=LINE ( 'NONE', #32915, #5907 ) ;
#29982=ORIENTED_EDGE ( 'NONE', *, *, #38, .T. ) ;
#29984=CIRCLE ( 'NONE', #8068, 31.99999999999998934 ) ;
#29985=EDGE_CURVE ( 'NONE', #28552, #15863, #32326, .T. ) ;
#29989=AXIS2_PLACEMENT_3D ( 'NONE', #5071, #38353, #8721 ) ;
#29995=AXIS2_PLACEMENT_3D ( 'NONE', #4032, #22624, #11389 ) ;
#29998=ADVANCED_FACE ( 'NONE', ( #13730 ), #20573, .T. ) ;
#30000=DIRECTION ( 'NONE',  ( 0.000000000000000000, 0.000000000000000000, 1.000000000000000000 ) ) ;
#30006=EDGE_LOOP ( 'NONE', ( #44115, #25016, #42538, #25544 ) ) ;
#30008=EDGE_CURVE ( 'NONE', #36384, #42951, #8841, .T. ) ;
#30009=CARTESIAN_POINT ( 'NONE',  ( 0.000000000000000000, 73.44644590900094272, -24.73286445877628026 ) ) ;
#30013=ORIENTED_EDGE ( 'NONE', *, *, #21770, .F. ) ;
#30030=ORIENTED_EDGE ( 'NONE', *, *, #30667, .T. ) ;
#30038=CARTESIAN_POINT ( 'NONE',  ( 10.00000000000000000, 76.66974797899852945, -11.30684508768257679 ) ) ;
#30042=DIRECTION ( 'NONE',  ( -1.000000000000000000, -0.000000000000000000, 0.000000000000000000 ) ) ;
#30043=CARTESIAN_POINT ( 'NONE',  ( 10.00000000000000000, -75.11725578898470701, 2.956366410620372864 ) ) ;
#30044=CIRCLE ( 'NONE', #20639, 31.99999999999999645 ) ;
#30047=DIRECTION ( 'NONE',  ( -1.000000000000000000, -0.000000000000000000, -0.000000000000000000 ) ) ;
#30050=EDGE_LOOP ( 'NONE', ( #20670, #11872, #43313, #42909 ) ) ;
#30053=ORIENTED_EDGE ( 'NONE', *, *, #43676, .T. ) ;
#30065=EDGE_CURVE ( 'NONE', #40628, #24345, #3349, .T. ) ;
#30069=ORIENTED_EDGE ( 'NONE', *, *, #21723, .F. ) ;
#30072=AXIS2_PLACEMENT_3D ( 'NONE', #9806, #39439, #1749 ) ;
#30073=ORIENTED_EDGE ( 'NONE', *, *, #36381, .T. ) ;
#30074=CARTESIAN_POINT ( 'NONE',  ( 5.000000000000002665, -8.966570791701281351, 81.50828551894224461 ) ) ;
#30075=ORIENTED_EDGE ( 'NONE', *, *, #24250, .T. ) ;
#30076=VECTOR ( 'NONE', #13899, 1000.000000000000000 ) ;
#30086=DIRECTION ( 'NONE',  ( -1.000000000000000000, 0.000000000000000000, -0.000000000000000000 ) ) ;
#30088=ORIENTED_EDGE ( 'NONE', *, *, #12065, .T. ) ;
#30091=DIRECTION ( 'NONE',  ( 0.000000000000000000, 0.000000000000000000, 1.000000000000000000 ) ) ;
#30100=AXIS2_PLACEMENT_3D ( 'NONE', #9976, #37316, #20993 ) ;
#30102=CARTESIAN_POINT ( 'NONE',  ( 0.000000000000000000, -39.47590169984793818, -71.87247863392457248 ) ) ;
#30104=AXIS2_PLACEMENT_3D ( 'NONE', #1314, #11603, #22849 ) ;
#30118=CYLINDRICAL_SURFACE ( 'NONE', #26058, 32.00000000000000000 ) ;
#30124=DIRECTION ( 'NONE',  ( -1.000000000000000000, 0.000000000000000000, 0.000000000000000000 ) ) ;
#30125=ORIENTED_EDGE ( 'NONE', *, *, #36381, .F. ) ;
#30126=VERTEX_POINT ( 'NONE', #6860 ) ;
#30128=ORIENTED_EDGE ( 'NONE', *, *, #44008, .F. ) ;
#30142=ORIENTED_EDGE ( 'NONE', *, *, #42558, .F. ) ;
#30156=DIRECTION ( 'NONE',  ( -1.000000000000000000, 0.000000000000000000, 0.000000000000000000 ) ) ;
#30164=CARTESIAN_POINT ( 'NONE',  ( 10.00000000000000000, 51.02545421589324803, 55.20638768913779870 ) ) ;
#30166=VERTEX_POINT ( 'NONE', #14691 ) ;
#30171=AXIS2_PLACEMENT_3D ( 'NONE', #17569, #13424, #2395 ) ;
#30176=CYLINDRICAL_SURFACE ( 'NONE', #44440, 77.49899999999999523 ) ;
#30178=EDGE_CURVE ( 'NONE', #48063, #39870, #13560, .T. ) ;
#30180=ORIENTED_EDGE ( 'NONE', *, *, #34184, .T. ) ;
#30185=CARTESIAN_POINT ( 'NONE',  ( 10.00000000000000000, -62.50329211542465657, 41.76937507738766442 ) ) ;
#30192=ORIENTED_EDGE ( 'NONE', *, *, #2270, .F. ) ;
#30203=CYLINDRICAL_SURFACE ( 'NONE', #43352, 31.99999999999999289 ) ;
#30204=CYLINDRICAL_SURFACE ( 'NONE', #13238, 32.00000000000000000 ) ;
#30210=CARTESIAN_POINT ( 'NONE',  ( 10.00000000000000000, 46.21855187248719687, -62.20884554313968806 ) ) ;
#30211=ORIENTED_EDGE ( 'NONE', *, *, #13421, .F. ) ;
#30212=VERTEX_POINT ( 'NONE', #11260 ) ;
#30222=CARTESIAN_POINT ( 'NONE',  ( 10.00000000000000000, 63.18004540533092239, -44.88180994100307686 ) ) ;
#30226=CARTESIAN_POINT ( 'NONE',  ( 10.00000000000000000, 0.000000000000000000, 0.000000000000000000 ) ) ;
#30232=CIRCLE ( 'NONE', #16153, 82.00000000000000000 ) ;
#30233=DIRECTION ( 'NONE',  ( -1.000000000000000000, 0.000000000000000000, 0.000000000000000000 ) ) ;
#30238=FACE_OUTER_BOUND ( 'NONE', #32975, .T. ) ;
#30242=CIRCLE ( 'NONE', #10709, 77.49899999999999523 ) ;
#30250=EDGE_CURVE ( 'NONE', #4970, #17460, #29984, .T. ) ;
#30263=ORIENTED_EDGE ( 'NONE', *, *, #9279, .T. ) ;
#30264=ORIENTED_EDGE ( 'NONE', *, *, #47119, .F. ) ;
#30265=ORIENTED_EDGE ( 'NONE', *, *, #44801, .T. ) ;
#30273=DIRECTION ( 'NONE',  ( -1.000000000000000000, -0.000000000000000000, -0.000000000000000000 ) ) ;
#30281=DIRECTION ( 'NONE',  ( -1.000000000000000000, 0.000000000000000000, 0.000000000000000000 ) ) ;
#30282=EDGE_LOOP ( 'NONE', ( #20067, #36593, #8745, #38720 ) ) ;
#30289=DIRECTION ( 'NONE',  ( 0.000000000000000000, 0.9876883405951371042, 0.1564344650402347547 ) ) ;
#30290=AXIS2_PLACEMENT_3D ( 'NONE', #34826, #22844, #23563 ) ;
#30292=CARTESIAN_POINT ( 'NONE',  ( 5.000000000000002665, -78.73519480814938731, -22.90783923731713756 ) ) ;
#30294=EDGE_CURVE ( 'NONE', #39398, #15461, #27399, .T. ) ;
#30295=AXIS2_PLACEMENT_3D ( 'NONE', #41072, #47434, #7531 ) ;
#30297=PRESENTATION_STYLE_ASSIGNMENT (( #4355 ) ) ;
#30299=VERTEX_POINT ( 'NONE', #16149 ) ;
#30310=AXIS2_PLACEMENT_3D ( 'NONE', #39917, #6387, #34354 ) ;
#30315=CARTESIAN_POINT ( 'NONE',  ( 0.000000000000000000, -72.35432306680498016, 20.40083707022857951 ) ) ;
#30317=CARTESIAN_POINT ( 'NONE',  ( 0.000000000000000000, -14.67089635893764665, 73.72996012237435082 ) ) ;
#30325=DIRECTION ( 'NONE',  ( -1.000000000000000000, 0.000000000000000000, 0.000000000000000000 ) ) ;
#30326=ORIENTED_EDGE ( 'NONE', *, *, #46531, .F. ) ;
#30330=FACE_OUTER_BOUND ( 'NONE', #24302, .T. ) ;
#30337=CARTESIAN_POINT ( 'NONE',  ( 0.000000000000000000, 35.91791733033475253, 68.67312586195009771 ) ) ;
#30345=DIRECTION ( 'NONE',  ( 0.000000000000000000, -0.07845909572785234043, 0.9969173337331274087 ) ) ;
#30355=CIRCLE ( 'NONE', #14696, 32.00000000000000000 ) ;
#30358=AXIS2_PLACEMENT_3D ( 'NONE', #17377, #9324, #9807 ) ;
#30368=EDGE_CURVE ( 'NONE', #2137, #29124, #47439, .T. ) ;
#30369=VERTEX_POINT ( 'NONE', #28116 ) ;
#30373=VECTOR ( 'NONE', #20105, 1000.000000000000000 ) ;
#30377=CARTESIAN_POINT ( 'NONE',  ( 0.000000000000000000, -73.95703589263958122, -23.16143007188506431 ) ) ;
#30384=DIRECTION ( 'NONE',  ( 0.000000000000000000, 0.000000000000000000, -1.000000000000000000 ) ) ;
#30385=VERTEX_POINT ( 'NONE', #21007 ) ;
#30388=ORIENTED_EDGE ( 'NONE', *, *, #42273, .T. ) ;
#30389=CARTESIAN_POINT ( 'NONE',  ( 0.000000000000000000, 12.24744871391589207, 2.500000000000000000 ) ) ;
#30391=ORIENTED_EDGE ( 'NONE', *, *, #6303, .T. ) ;
#30399=EDGE_CURVE ( 'NONE', #30212, #30126, #27649, .T. ) ;
#30401=CARTESIAN_POINT ( 'NONE',  ( 10.00000000000000000, 0.000000000000000000, 0.000000000000000000 ) ) ;
#30405=DIRECTION ( 'NONE',  ( -1.000000000000000000, -0.000000000000000000, -0.000000000000000000 ) ) ;
#30407=DIRECTION ( 'NONE',  ( -1.000000000000000000, -0.000000000000000000, -0.000000000000000000 ) ) ;
#30410=DIRECTION ( 'NONE',  ( -1.000000000000000000, -0.000000000000000000, -0.000000000000000000 ) ) ;
#30413=ORIENTED_EDGE ( 'NONE', *, *, #14596, .T. ) ;
#30416=DIRECTION ( 'NONE',  ( -1.000000000000000000, 0.000000000000000000, 0.000000000000000000 ) ) ;
#30420=AXIS2_PLACEMENT_3D ( 'NONE', #8494, #18780, #44992 ) ;
#30423=ORIENTED_EDGE ( 'NONE', *, *, #48138, .F. ) ;
#30428=EDGE_LOOP ( 'NONE', ( #43842, #41394, #38198, #30868 ) ) ;
#30430=DIRECTION ( 'NONE',  ( -1.000000000000000000, 0.000000000000000000, -0.000000000000000000 ) ) ;
#30437=ORIENTED_EDGE ( 'NONE', *, *, #29147, .T. ) ;
#30441=CARTESIAN_POINT ( 'NONE',  ( 0.000000000000000000, -14.66109333815410487, -73.73191006444587003 ) ) ;
#30442=ADVANCED_FACE ( 'NONE', ( #16868 ), #24920, .T. ) ;
#30454=AXIS2_PLACEMENT_3D ( 'NONE', #24642, #20239, #39590 ) ;
#30469=ORIENTED_EDGE ( 'NONE', *, *, #22006, .T. ) ;
#30470=DIRECTION ( 'NONE',  ( 0.000000000000000000, 0.000000000000000000, 1.000000000000000000 ) ) ;
#30479=LINE ( 'NONE', #33428, #21845 ) ;
#30484=ORIENTED_EDGE ( 'NONE', *, *, #25614, .T. ) ;
#30491=CARTESIAN_POINT ( 'NONE',  ( 10.00000000000000000, 0.000000000000000000, 0.000000000000000000 ) ) ;
#30494=ADVANCED_FACE ( 'NONE', ( #16614 ), #39135, .T. ) ;
#30508=ORIENTED_EDGE ( 'NONE', *, *, #17706, .T. ) ;
#30509=VERTEX_POINT ( 'NONE', #39634 ) ;
#30513=CARTESIAN_POINT ( 'NONE',  ( 10.00000000000000000, 0.000000000000000000, 0.000000000000000000 ) ) ;
#30517=DIRECTION ( 'NONE',  ( -1.000000000000000000, 0.000000000000000000, -0.000000000000000000 ) ) ;
#30520=CARTESIAN_POINT ( 'NONE',  ( 10.00000000000000000, -46.21855187248673502, 62.20884554314003623 ) ) ;
#30526=VECTOR ( 'NONE', #43374, 1000.000000000000000 ) ;
#30529=AXIS2_PLACEMENT_3D ( 'NONE', #46272, #20306, #12742 ) ;
#30534=ORIENTED_EDGE ( 'NONE', *, *, #37365, .T. ) ;
#30552=DIRECTION ( 'NONE',  ( -1.000000000000000000, -0.000000000000000000, 0.000000000000000000 ) ) ;
#30559=DIRECTION ( 'NONE',  ( -1.000000000000000000, -0.000000000000000000, 0.000000000000000000 ) ) ;
#30560=VERTEX_POINT ( 'NONE', #36883 ) ;
#30569=DIRECTION ( 'NONE',  ( 0.000000000000000000, 0.000000000000000000, -1.000000000000000000 ) ) ;
#30571=CARTESIAN_POINT ( 'NONE',  ( 10.00000000000000000, -41.19522573413780009, 65.64334221924896440 ) ) ;
#30576=DIRECTION ( 'NONE',  ( 0.000000000000000000, 0.000000000000000000, 1.000000000000000000 ) ) ;
#30580=EDGE_CURVE ( 'NONE', #8066, #28131, #46443, .T. ) ;
#30582=UNCERTAINTY_MEASURE_WITH_UNIT (LENGTH_MEASURE( 1.000000000000000082E-05 ), #38116, 'distance_accuracy_value', 'NONE');
#30589=ORIENTED_EDGE ( 'NONE', *, *, #32861, .F. ) ;
#30592=EDGE_LOOP ( 'NONE', ( #38946, #13832, #13947, #4618 ) ) ;
#30597=ORIENTED_EDGE ( 'NONE', *, *, #14653, .F. ) ;
#30598=ORIENTED_EDGE ( 'NONE', *, *, #32493, .T. ) ;
#30601=DIRECTION ( 'NONE',  ( 0.000000000000000000, -0.4539904997395542430, 0.8910065241883641241 ) ) ;
#30606=CARTESIAN_POINT ( 'NONE',  ( 10.00000000000000000, 63.97538442413500093, -51.29473840253157135 ) ) ;
#30609=EDGE_CURVE ( 'NONE', #20108, #6477, #7338, .T. ) ;
#30610=DIRECTION ( 'NONE',  ( -1.000000000000000000, -0.000000000000000000, -0.000000000000000000 ) ) ;
#30613=ORIENTED_EDGE ( 'NONE', *, *, #12520, .T. ) ;
#30626=DIRECTION ( 'NONE',  ( -1.000000000000000000, 0.000000000000000000, 0.000000000000000000 ) ) ;
#30636=DIRECTION ( 'NONE',  ( 0.000000000000000000, 0.000000000000000000, 1.000000000000000000 ) ) ;
#30644=DIRECTION ( 'NONE',  ( -1.000000000000000000, -0.000000000000000000, 0.000000000000000000 ) ) ;
#30646=ORIENTED_EDGE ( 'NONE', *, *, #19269, .T. ) ;
#30649=DIRECTION ( 'NONE',  ( -1.000000000000000000, 0.000000000000000000, 0.000000000000000000 ) ) ;
#30654=AXIS2_PLACEMENT_3D ( 'NONE', #31844, #32072, #42603 ) ;
#30656=DIRECTION ( 'NONE',  ( 1.000000000000000000, 0.000000000000000000, -0.000000000000000000 ) ) ;
#30661=DIRECTION ( 'NONE',  ( 0.000000000000000000, -0.8910065241883722287, 0.4539904997395383113 ) ) ;
#30667=EDGE_CURVE ( 'NONE', #37239, #46298, #25322, .T. ) ;
#30668=DIRECTION ( 'NONE',  ( -1.000000000000000000, -0.000000000000000000, 0.000000000000000000 ) ) ;
#30669=DIRECTION ( 'NONE',  ( -1.000000000000000000, -0.000000000000000000, 0.000000000000000000 ) ) ;
#30674=VERTEX_POINT ( 'NONE', #46355 ) ;
#30684=ORIENTED_EDGE ( 'NONE', *, *, #19235, .F. ) ;
#30686=LINE ( 'NONE', #1319, #34625 ) ;
#30687=CARTESIAN_POINT ( 'NONE',  ( 0.000000000000000000, 23.16143007188532366, -73.95703589263949596 ) ) ;
#30692=CARTESIAN_POINT ( 'NONE',  ( 10.00000000000000000, 0.000000000000000000, 0.000000000000000000 ) ) ;
#30695=AXIS2_PLACEMENT_3D ( 'NONE', #1918, #24410, #12934 ) ;
#30705=ORIENTED_EDGE ( 'NONE', *, *, #949, .F. ) ;
#30708=CARTESIAN_POINT ( 'NONE',  ( 10.00000000000000000, 0.000000000000000000, 0.000000000000000000 ) ) ;
#30710=EDGE_CURVE ( 'NONE', #30299, #10059, #28010, .T. ) ;
#30717=ORIENTED_EDGE ( 'NONE', *, *, #41853, .F. ) ;
#30721=AXIS2_PLACEMENT_3D ( 'NONE', #17132, #42616, #24481 ) ;
#30722=DIRECTION ( 'NONE',  ( -1.000000000000000000, 0.000000000000000000, 0.000000000000000000 ) ) ;
#30724=DIRECTION ( 'NONE',  ( -1.000000000000000000, -0.000000000000000000, 0.000000000000000000 ) ) ;
#30727=DIRECTION ( 'NONE',  ( -1.000000000000000000, -0.000000000000000000, -0.000000000000000000 ) ) ;
#30734=ORIENTED_EDGE ( 'NONE', *, *, #12362, .T. ) ;
#30735=ADVANCED_FACE ( 'NONE', ( #13313 ), #43173, .T. ) ;
#30737=LINE ( 'NONE', #38082, #35033 ) ;
#30738=CARTESIAN_POINT ( 'NONE',  ( 0.000000000000000000, 0.000000000000000000, 0.000000000000000000 ) ) ;
#30744=CYLINDRICAL_SURFACE ( 'NONE', #36364, 31.99999999999998579 ) ;
#30751=ORIENTED_EDGE ( 'NONE', *, *, #10008, .T. ) ;
#30752=DIRECTION ( 'NONE',  ( 0.000000000000000000, 0.000000000000000000, 1.000000000000000000 ) ) ;
#30754=DIRECTION ( 'NONE',  ( -1.000000000000000000, 0.000000000000000000, 0.000000000000000000 ) ) ;
#30755=DIRECTION ( 'NONE',  ( -1.000000000000000000, 0.000000000000000000, 0.000000000000000000 ) ) ;
#30758=CARTESIAN_POINT ( 'NONE',  ( 10.00000000000000000, 0.000000000000000000, 0.000000000000000000 ) ) ;
#30761=CARTESIAN_POINT ( 'NONE',  ( 5.000000000000000000, 27.74655509720669500, 77.16300072079670258 ) ) ;
#30762=DIRECTION ( 'NONE',  ( -1.000000000000000000, -0.000000000000000000, -0.000000000000000000 ) ) ;
#30779=CIRCLE ( 'NONE', #9657, 31.99999999999998934 ) ;
#30781=EDGE_CURVE ( 'NONE', #9766, #12926, #18267, .T. ) ;
#30782=ORIENTED_EDGE ( 'NONE', *, *, #13321, .T. ) ;
#30790=ORIENTED_EDGE ( 'NONE', *, *, #17789, .F. ) ;
#30791=VERTEX_POINT ( 'NONE', #5984 ) ;
#30795=FACE_OUTER_BOUND ( 'NONE', #20461, .T. ) ;
#30796=DIRECTION ( 'NONE',  ( 0.000000000000000000, 0.9238795325112851842, 0.3826834323650937786 ) ) ;
#30798=AXIS2_PLACEMENT_3D ( 'NONE', #25978, #25497, #44584 ) ;
#30799=DIRECTION ( 'NONE',  ( -1.000000000000000000, -0.000000000000000000, -0.000000000000000000 ) ) ;
#30800=ORIENTED_EDGE ( 'NONE', *, *, #1583, .F. ) ;
#30807=AXIS2_PLACEMENT_3D ( 'NONE', #15567, #11901, #27081 ) ;
#30808=DIRECTION ( 'NONE',  ( -1.000000000000000000, -0.000000000000000000, 0.000000000000000000 ) ) ;
#30810=ORIENTED_EDGE ( 'NONE', *, *, #27463, .F. ) ;
#30811=CARTESIAN_POINT ( 'NONE',  ( 0.000000000000000000, 81.96053171279902472, 2.543863470248670211 ) ) ;
#30812=LINE ( 'NONE', #23689, #40857 ) ;
#30814=VERTEX_POINT ( 'NONE', #20903 ) ;
#30816=ADVANCED_FACE ( 'NONE', ( #2770 ), #28953, .T. ) ;
#30827=DIRECTION ( 'NONE',  ( 1.000000000000000000, 0.000000000000000000, 0.000000000000000000 ) ) ;
#30828=CARTESIAN_POINT ( 'NONE',  ( 10.00000000000000000, 0.000000000000000000, 0.000000000000000000 ) ) ;
#30830=FACE_OUTER_BOUND ( 'NONE', #21735, .T. ) ;
#30833=DIRECTION ( 'NONE',  ( -1.000000000000000000, -0.000000000000000000, -0.000000000000000000 ) ) ;
#30841=DIRECTION ( 'NONE',  ( -1.000000000000000000, -0.000000000000000000, -0.000000000000000000 ) ) ;
#30853=VERTEX_POINT ( 'NONE', #24810 ) ;
#30861=CARTESIAN_POINT ( 'NONE',  ( 0.000000000000000000, 65.64334221924966073, -41.19522573413664190 ) ) ;
#30862=EDGE_CURVE ( 'NONE', #26881, #42399, #23688, .T. ) ;
#30866=DIRECTION ( 'NONE',  ( 0.000000000000000000, -0.9238795325112906243, 0.3826834323650805114 ) ) ;
#30868=ORIENTED_EDGE ( 'NONE', *, *, #5158, .T. ) ;
#30872=ORIENTED_EDGE ( 'NONE', *, *, #32639, .F. ) ;
#30873=EDGE_CURVE ( 'NONE', #32923, #45066, #18185, .T. ) ;
#30881=CARTESIAN_POINT ( 'NONE',  ( 10.00000000000000000, -75.16055320797043748, 18.89407956138229494 ) ) ;
#30885=DIRECTION ( 'NONE',  ( -1.000000000000000000, 0.000000000000000000, 0.000000000000000000 ) ) ;
#30890=EDGE_CURVE ( 'NONE', #23694, #46638, #1794, .T. ) ;
#30896=AXIS2_PLACEMENT_3D ( 'NONE', #19965, #8699, #31010 ) ;
#30898=DIRECTION ( 'NONE',  ( 0.000000000000000000, 0.000000000000000000, 1.000000000000000000 ) ) ;
#30901=CIRCLE ( 'NONE', #33224, 82.00000000000000000 ) ;
#30910=AXIS2_PLACEMENT_3D ( 'NONE', #20826, #17623, #29115 ) ;
#30916=AXIS2_PLACEMENT_3D ( 'NONE', #29164, #43628, #10324 ) ;
#30918=FACE_OUTER_BOUND ( 'NONE', #20127, .T. ) ;
#30921=CIRCLE ( 'NONE', #12169, 77.49900000000000944 ) ;
#30936=ORIENTED_EDGE ( 'NONE', *, *, #10049, .F. ) ;
#30939=ORIENTED_EDGE ( 'NONE', *, *, #16809, .T. ) ;
#30950=CARTESIAN_POINT ( 'NONE',  ( 10.00000000000000000, 51.02545421589402252, -55.20638768913705263 ) ) ;
#30952=CARTESIAN_POINT ( 'NONE',  ( 10.00000000000000000, 71.27951684758026829, 30.41916302227139113 ) ) ;
#30953=ADVANCED_FACE ( 'NONE', ( #45103 ), #34305, .T. ) ;
#30955=DIRECTION ( 'NONE',  ( -1.000000000000000000, 0.000000000000000000, -0.000000000000000000 ) ) ;
#30957=LINE ( 'NONE', #45883, #29097 ) ;
#30958=CARTESIAN_POINT ( 'NONE',  ( 10.00000000000000000, 22.90783923731741112, -78.73519480814930205 ) ) ;
#30966=EDGE_CURVE ( 'NONE', #41833, #15455, #8027, .T. ) ;
#30968=AXIS2_PLACEMENT_3D ( 'NONE', #47317, #28714, #13790 ) ;
#30981=AXIS2_PLACEMENT_3D ( 'NONE', #31618, #24742, #38722 ) ;
#30989=AXIS2_PLACEMENT_3D ( 'NONE', #41063, #26601, #7981 ) ;
#30991=CARTESIAN_POINT ( 'NONE',  ( 0.000000000000000000, 41.76937507738875155, -62.50329211542393892 ) ) ;
#30993=DIRECTION ( 'NONE',  ( -1.000000000000000000, 0.000000000000000000, 0.000000000000000000 ) ) ;
#30994=AXIS2_PLACEMENT_3D ( 'NONE', #15394, #37408, #7785 ) ;
#31006=LINE ( 'NONE', #4797, #47121 ) ;
#31010=DIRECTION ( 'NONE',  ( 0.000000000000000000, 0.000000000000000000, -1.000000000000000000 ) ) ;
#31014=EDGE_CURVE ( 'NONE', #40883, #43442, #4932, .T. ) ;
#31017=CARTESIAN_POINT ( 'NONE',  ( 10.00000000000000000, 2.946379043146343246, 75.11764819372150725 ) ) ;
#31026=ORIENTED_EDGE ( 'NONE', *, *, #34639, .T. ) ;
#31027=VERTEX_POINT ( 'NONE', #37508 ) ;
#31028=ADVANCED_FACE ( 'NONE', ( #37271 ), #48282, .T. ) ;
#31029=DIRECTION ( 'NONE',  ( 1.000000000000000000, 0.000000000000000000, 0.000000000000000000 ) ) ;
#31036=CARTESIAN_POINT ( 'NONE',  ( 10.00000000000000000, -74.65374052328654386, 8.840884882374837161 ) ) ;
#31038=EDGE_CURVE ( 'NONE', #40126, #38600, #3736, .T. ) ;
#31040=AXIS2_PLACEMENT_3D ( 'NONE', #20638, #31687, #13071 ) ;
#31042=CYLINDRICAL_SURFACE ( 'NONE', #14388, 82.00000000000000000 ) ;
#31045=CIRCLE ( 'NONE', #23980, 82.00000000000000000 ) ;
#31046=DIRECTION ( 'NONE',  ( 0.000000000000000000, 0.000000000000000000, 1.000000000000000000 ) ) ;
#31047=CYLINDRICAL_SURFACE ( 'NONE', #21906, 31.99999999999999289 ) ;
#31059=DIRECTION ( 'NONE',  ( 0.000000000000000000, 0.000000000000000000, 1.000000000000000000 ) ) ;
#31061=EDGE_LOOP ( 'NONE', ( #44769, #29982, #14015, #19486 ) ) ;
#31063=CIRCLE ( 'NONE', #27918, 31.99999999999999645 ) ;
#31068=ORIENTED_EDGE ( 'NONE', *, *, #31188, .F. ) ;
#31069=CARTESIAN_POINT ( 'NONE',  ( 10.00000000000000000, -51.03279382321048985, -55.19960302592120627 ) ) ;
#31070=ORIENTED_EDGE ( 'NONE', *, *, #40964, .F. ) ;
#31072=FACE_OUTER_BOUND ( 'NONE', #30050, .T. ) ;
#31080=DIRECTION ( 'NONE',  ( -1.000000000000000000, -0.000000000000000000, -0.000000000000000000 ) ) ;
#31088=VERTEX_POINT ( 'NONE', #42388 ) ;
#31092=EDGE_CURVE ( 'NONE', #44962, #18546, #15063, .T. ) ;
#31094=LINE ( 'NONE', #37945, #40641 ) ;
#31096=ORIENTED_EDGE ( 'NONE', *, *, #1083, .T. ) ;
#31101=ORIENTED_EDGE ( 'NONE', *, *, #33929, .F. ) ;
#31105=ORIENTED_EDGE ( 'NONE', *, *, #20999, .T. ) ;
#31107=DIRECTION ( 'NONE',  ( -1.000000000000000000, 0.000000000000000000, 0.000000000000000000 ) ) ;
#31108=FACE_OUTER_BOUND ( 'NONE', #856, .T. ) ;
#31114=DIRECTION ( 'NONE',  ( 0.000000000000000000, 0.000000000000000000, 1.000000000000000000 ) ) ;
#31116=CARTESIAN_POINT ( 'NONE',  ( 10.00000000000000000, 65.59268652807263322, -36.72794159290169347 ) ) ;
#31117=ORIENTED_EDGE ( 'NONE', *, *, #101, .T. ) ;
#31122=DIRECTION ( 'NONE',  ( 0.000000000000000000, 0.000000000000000000, 1.000000000000000000 ) ) ;
#31123=DIRECTION ( 'NONE',  ( -1.000000000000000000, -0.000000000000000000, -0.000000000000000000 ) ) ;
#31128=EDGE_CURVE ( 'NONE', #28820, #9321, #42146, .T. ) ;
#31130=AXIS2_PLACEMENT_3D ( 'NONE', #1728, #38944, #5397 ) ;
#31131=ORIENTED_EDGE ( 'NONE', *, *, #11842, .F. ) ;
#31132=CARTESIAN_POINT ( 'NONE',  ( 10.00000000000000000, 0.000000000000000000, 0.000000000000000000 ) ) ;
#31133=ADVANCED_FACE ( 'NONE', ( #27711 ), #35527, .T. ) ;
#31134=CARTESIAN_POINT ( 'NONE',  ( 10.00000000000000000, -31.47745569255092235, -68.26794271651296242 ) ) ;
#31139=CARTESIAN_POINT ( 'NONE',  ( 10.00000000000000000, 34.44570377933695227, -69.42325613327405165 ) ) ;
#31140=CIRCLE ( 'NONE', #7670, 32.00000000000000000 ) ;
#31142=ADVANCED_FACE ( 'NONE', ( #9102 ), #26994, .T. ) ;
#31143=ORIENTED_EDGE ( 'NONE', *, *, #2414, .T. ) ;
#31144=CARTESIAN_POINT ( 'NONE',  ( 10.00000000000000000, 28.89263327155746097, 71.91182617369197771 ) ) ;
#31149=CARTESIAN_POINT ( 'NONE',  ( 10.00000000000000000, 41.19522573413731692, 65.64334221924924861 ) ) ;
#31150=ORIENTED_EDGE ( 'NONE', *, *, #17228, .F. ) ;
#31157=EDGE_CURVE ( 'NONE', #31088, #25106, #47134, .T. ) ;
#31159=FACE_OUTER_BOUND ( 'NONE', #20369, .T. ) ;
#31160=ORIENTED_EDGE ( 'NONE', *, *, #561, .F. ) ;
#31167=DIRECTION ( 'NONE',  ( 0.000000000000000000, 0.000000000000000000, 1.000000000000000000 ) ) ;
#31174=DIRECTION ( 'NONE',  ( 1.000000000000000000, 0.000000000000000000, 0.000000000000000000 ) ) ;
#31179=ORIENTED_EDGE ( 'NONE', *, *, #6507, .F. ) ;
#31181=DIRECTION ( 'NONE',  ( -1.000000000000000000, -0.000000000000000000, 0.000000000000000000 ) ) ;
#31187=DIRECTION ( 'NONE',  ( 1.000000000000000000, -0.000000000000000000, -0.000000000000000000 ) ) ;
#31188=EDGE_CURVE ( 'NONE', #32575, #12049, #4939, .T. ) ;
#31193=DIRECTION ( 'NONE',  ( 0.000000000000000000, 0.000000000000000000, 1.000000000000000000 ) ) ;
#31195=FACE_OUTER_BOUND ( 'NONE', #18248, .T. ) ;
#31204=VECTOR ( 'NONE', #44963, 1000.000000000000000 ) ;
#31208=ADVANCED_FACE ( 'NONE', ( #27470 ), #40164, .T. ) ;
#31218=ORIENTED_EDGE ( 'NONE', *, *, #146, .T. ) ;
#31221=ORIENTED_EDGE ( 'NONE', *, *, #47902, .T. ) ;
#31222=ORIENTED_EDGE ( 'NONE', *, *, #29940, .T. ) ;
#31224=CYLINDRICAL_SURFACE ( 'NONE', #40341, 82.00000000000000000 ) ;
#31225=DIRECTION ( 'NONE',  ( -1.000000000000000000, 0.000000000000000000, -0.000000000000000000 ) ) ;
#31229=VECTOR ( 'NONE', #19443, 1000.000000000000000 ) ;
#31230=CARTESIAN_POINT ( 'NONE',  ( 5.000000000000002665, 81.34940948281337114, 10.30890764327411979 ) ) ;
#31231=ORIENTED_EDGE ( 'NONE', *, *, #37310, .F. ) ;
#31234=VECTOR ( 'NONE', #22699, 1000.000000000000000 ) ;
#31235=CARTESIAN_POINT ( 'NONE',  ( 0.000000000000000000, 77.16300072079700101, -27.74655509720590985 ) ) ;
#31238=DIRECTION ( 'NONE',  ( -1.000000000000000000, -0.000000000000000000, 0.000000000000000000 ) ) ;
#31251=DIRECTION ( 'NONE',  ( -1.000000000000000000, 0.000000000000000000, -0.000000000000000000 ) ) ;
#31252=EDGE_CURVE ( 'NONE', #31274, #9220, #10412, .T. ) ;
#31253=DIRECTION ( 'NONE',  ( 0.000000000000000000, 0.000000000000000000, 1.000000000000000000 ) ) ;
#31256=CARTESIAN_POINT ( 'NONE',  ( -10.00000000000000000, 0.000000000000000000, 0.000000000000000000 ) ) ;
#31257=DIRECTION ( 'NONE',  ( 0.000000000000000000, 0.000000000000000000, 1.000000000000000000 ) ) ;
#31260=SHAPE_REPRESENTATION ( 'big gear_ISO - Spur gear 2M 80T 20PA 10FW ---S80A75H50L20.0N', ( #11636 ), #725 ) ;
#31261=ORIENTED_EDGE ( 'NONE', *, *, #15276, .F. ) ;
#31269=ORIENTED_EDGE ( 'NONE', *, *, #2701, .T. ) ;
#31274=VERTEX_POINT ( 'NONE', #32573 ) ;
#31277=DIRECTION ( 'NONE',  ( 0.000000000000000000, 0.000000000000000000, 1.000000000000000000 ) ) ;
#31281=ADVANCED_FACE ( 'NONE', ( #47495 ), #28417, .T. ) ;
#31290=ORIENTED_EDGE ( 'NONE', *, *, #10842, .T. ) ;
#31298=ORIENTED_EDGE ( 'NONE', *, *, #47895, .T. ) ;
#31301=EDGE_LOOP ( 'NONE', ( #44161, #13692, #32698, #41799 ) ) ;
#31305=VERTEX_POINT ( 'NONE', #31879 ) ;
#31309=DIRECTION ( 'NONE',  ( -1.000000000000000000, 0.000000000000000000, 0.000000000000000000 ) ) ;
#31313=CARTESIAN_POINT ( 'NONE',  ( 0.000000000000000000, 46.54456581323888997, -59.03342792756214408 ) ) ;
#31317=DIRECTION ( 'NONE',  ( -1.000000000000000000, -0.000000000000000000, 0.000000000000000000 ) ) ;
#31318=DIRECTION ( 'NONE',  ( -1.000000000000000000, -0.000000000000000000, -0.000000000000000000 ) ) ;
#31320=DIRECTION ( 'NONE',  ( 0.000000000000000000, 0.000000000000000000, 1.000000000000000000 ) ) ;
#31324=ORIENTED_EDGE ( 'NONE', *, *, #27420, .T. ) ;
#31326=CARTESIAN_POINT ( 'NONE',  ( 0.000000000000000000, 69.42325613327489009, -34.44570377933524696 ) ) ;
#31338=ORIENTED_EDGE ( 'NONE', *, *, #31701, .T. ) ;
#31341=EDGE_LOOP ( 'NONE', ( #25606, #29039, #14759, #32111 ) ) ;
#31346=AXIS2_PLACEMENT_3D ( 'NONE', #12336, #12569, #46335 ) ;
#31353=CARTESIAN_POINT ( 'NONE',  ( 10.00000000000000000, 16.00000000000000000, 2.500000000000000000 ) ) ;
#31354=CARTESIAN_POINT ( 'NONE',  ( 0.000000000000000000, 0.000000000000000000, 0.000000000000000000 ) ) ;
#31361=ORIENTED_EDGE ( 'NONE', *, *, #23342, .T. ) ;
#31362=CARTESIAN_POINT ( 'NONE',  ( 10.00000000000000000, -2.946379043146863719, 75.11764819372146462 ) ) ;
#31367=CARTESIAN_POINT ( 'NONE',  ( 0.000000000000000000, -73.73191006444582740, 14.66109333815435889 ) ) ;
#31373=DIRECTION ( 'NONE',  ( -1.000000000000000000, 0.000000000000000000, 0.000000000000000000 ) ) ;
#31379=DIRECTION ( 'NONE',  ( -1.000000000000000000, 0.000000000000000000, -0.000000000000000000 ) ) ;
#31384=CARTESIAN_POINT ( 'NONE',  ( 10.00000000000000000, -77.16300072079680206, 27.74655509720639657 ) ) ;
#31387=AXIS2_PLACEMENT_3D ( 'NONE', #8033, #34456, #22968 ) ;
#31388=ORIENTED_EDGE ( 'NONE', *, *, #25984, .F. ) ;
#31391=DIRECTION ( 'NONE',  ( -1.000000000000000000, 0.000000000000000000, -0.000000000000000000 ) ) ;
#31394=CARTESIAN_POINT ( 'NONE',  ( 0.000000000000000000, 80.55351364060611274, -15.33399622253396544 ) ) ;
#31396=ADVANCED_FACE ( 'NONE', ( #7823 ), #29616, .T. ) ;
#31397=DIRECTION ( 'NONE',  ( -1.000000000000000000, 0.000000000000000000, 0.000000000000000000 ) ) ;
#31404=AXIS2_PLACEMENT_3D ( 'NONE', #27798, #5509, #42225 ) ;
#31410=ORIENTED_EDGE ( 'NONE', *, *, #13217, .T. ) ;
#31413=AXIS2_PLACEMENT_3D ( 'NONE', #8698, #37850, #12632 ) ;
#31417=EDGE_CURVE ( 'NONE', #15994, #2489, #44018, .T. ) ;
#31419=CYLINDRICAL_SURFACE ( 'NONE', #3904, 82.00000000000000000 ) ;
#31420=ORIENTED_EDGE ( 'NONE', *, *, #47557, .T. ) ;
#31426=VERTEX_POINT ( 'NONE', #226 ) ;
#31435=EDGE_CURVE ( 'NONE', #40433, #14416, #25247, .T. ) ;
#31437=DIRECTION ( 'NONE',  ( -1.000000000000000000, 0.000000000000000000, 0.000000000000000000 ) ) ;
#31438=CARTESIAN_POINT ( 'NONE',  ( 5.000000000000002665, 81.50828551894240093, -8.966570791699803422 ) ) ;
#31441=DIRECTION ( 'NONE',  ( 0.000000000000000000, 0.9723699203976773342, -0.2334453638559023381 ) ) ;
#31445=DIRECTION ( 'NONE',  ( 1.000000000000000000, 0.000000000000000000, 0.000000000000000000 ) ) ;
#31447=CARTESIAN_POINT ( 'NONE',  ( 10.00000000000000000, 0.000000000000000000, 0.000000000000000000 ) ) ;
#31448=CIRCLE ( 'NONE', #14231, 77.49899999999999523 ) ;
#31453=EDGE_LOOP ( 'NONE', ( #10056, #22846, #7248, #34951 ) ) ;
#31460=DIRECTION ( 'NONE',  ( -1.000000000000000000, -0.000000000000000000, -0.000000000000000000 ) ) ;
#31481=CARTESIAN_POINT ( 'NONE',  ( 0.000000000000000000, 0.000000000000000000, 0.000000000000000000 ) ) ;
#31488=EDGE_CURVE ( 'NONE', #5219, #5603, #1937, .T. ) ;
#31491=ORIENTED_EDGE ( 'NONE', *, *, #29576, .T. ) ;
#31492=AXIS2_PLACEMENT_3D ( 'NONE', #9667, #24611, #14796 ) ;
#31513=VERTEX_POINT ( 'NONE', #23976 ) ;
#31514=AXIS2_PLACEMENT_3D ( 'NONE', #22251, #37656, #18571 ) ;
#31518=ORIENTED_EDGE ( 'NONE', *, *, #38914, .T. ) ;
#31522=EDGE_CURVE ( 'NONE', #28423, #32581, #42323, .T. ) ;
#31527=ORIENTED_EDGE ( 'NONE', *, *, #44216, .T. ) ;
#31528=FACE_OUTER_BOUND ( 'NONE', #32782, .T. ) ;
#31531=DIRECTION ( 'NONE',  ( -1.000000000000000000, -0.000000000000000000, -0.000000000000000000 ) ) ;
#31534=VERTEX_POINT ( 'NONE', #31326 ) ;
#31541=VECTOR ( 'NONE', #34794, 1000.000000000000000 ) ;
#31543=ORIENTED_EDGE ( 'NONE', *, *, #20532, .T. ) ;
#31550=ORIENTED_EDGE ( 'NONE', *, *, #11344, .T. ) ;
#31556=CYLINDRICAL_SURFACE ( 'NONE', #42442, 31.99999999999999289 ) ;
#31569=EDGE_CURVE ( 'NONE', #17592, #33075, #42580, .T. ) ;
#31571=ADVANCED_BREP_SHAPE_REPRESENTATION ( '', ( #19734, #11636 ), #725 ) ;
#31574=CARTESIAN_POINT ( 'NONE',  ( 10.00000000000000000, 62.50884508063427347, 41.76106447765511831 ) ) ;
#31577=EDGE_CURVE ( 'NONE', #6991, #17121, #26134, .T. ) ;
#31581=AXIS2_PLACEMENT_3D ( 'NONE', #3856, #30047, #44979 ) ;
#31582=ORIENTED_EDGE ( 'NONE', *, *, #3030, .T. ) ;
#31584=EDGE_CURVE ( 'NONE', #11671, #45038, #22673, .T. ) ;
#31586=DIRECTION ( 'NONE',  ( -1.000000000000000000, 0.000000000000000000, 0.000000000000000000 ) ) ;
#31589=CIRCLE ( 'NONE', #29228, 31.99999999999999289 ) ;
#31591=CYLINDRICAL_SURFACE ( 'NONE', #5168, 31.99999999999999289 ) ;
#31597=DIRECTION ( 'NONE',  ( -1.000000000000000000, -0.000000000000000000, 0.000000000000000000 ) ) ;
#31600=DIRECTION ( 'NONE',  ( 0.000000000000000000, 0.000000000000000000, 1.000000000000000000 ) ) ;
#31610=CARTESIAN_POINT ( 'NONE',  ( 0.000000000000000000, 0.000000000000000000, 0.000000000000000000 ) ) ;
#31618=CARTESIAN_POINT ( 'NONE',  ( -10.00000000000000000, 0.000000000000000000, 0.000000000000000000 ) ) ;
#31624=CARTESIAN_POINT ( 'NONE',  ( 10.00000000000000000, -68.27212725128254078, -31.46837873495049465 ) ) ;
#31630=ORIENTED_EDGE ( 'NONE', *, *, #13965, .T. ) ;
#31633=CARTESIAN_POINT ( 'NONE',  ( 0.000000000000000000, -76.69515212745996280, -29.01471420065644580 ) ) ;
#31634=CIRCLE ( 'NONE', #10503, 31.99999999999999645 ) ;
#31642=EDGE_CURVE ( 'NONE', #26337, #45282, #33452, .T. ) ;
#31643=ORIENTED_EDGE ( 'NONE', *, *, #29405, .T. ) ;
#31645=ORIENTED_EDGE ( 'NONE', *, *, #31577, .F. ) ;
#31648=CARTESIAN_POINT ( 'NONE',  ( 0.000000000000000000, 0.000000000000000000, 0.000000000000000000 ) ) ;
#31653=VERTEX_POINT ( 'NONE', #44957 ) ;
#31659=CYLINDRICAL_SURFACE ( 'NONE', #24465, 31.99999999999999289 ) ;
#31662=DIRECTION ( 'NONE',  ( 0.000000000000000000, 0.000000000000000000, 1.000000000000000000 ) ) ;
#31664=AXIS2_PLACEMENT_3D ( 'NONE', #43942, #28777, #39310 ) ;
#31667=ORIENTED_EDGE ( 'NONE', *, *, #45172, .F. ) ;
#31672=CARTESIAN_POINT ( 'NONE',  ( 10.00000000000000000, 81.34940948281349904, -10.30890764327296871 ) ) ;
#31673=VECTOR ( 'NONE', #18635, 1000.000000000000000 ) ;
#31680=DIRECTION ( 'NONE',  ( 1.000000000000000000, -0.000000000000000000, 0.000000000000000000 ) ) ;
#31683=ADVANCED_FACE ( 'NONE', ( #22911 ), #4334, .T. ) ;
#31687=DIRECTION ( 'NONE',  ( -1.000000000000000000, 0.000000000000000000, 0.000000000000000000 ) ) ;
#31693=CIRCLE ( 'NONE', #10560, 31.99999999999999645 ) ;
#31701=EDGE_CURVE ( 'NONE', #29354, #15461, #4275, .T. ) ;
#31706=ORIENTED_EDGE ( 'NONE', *, *, #39463, .F. ) ;
#31709=CIRCLE ( 'NONE', #37941, 82.00000000000000000 ) ;
#31717=ORIENTED_EDGE ( 'NONE', *, *, #15355, .T. ) ;
#31720=ORIENTED_EDGE ( 'NONE', *, *, #47895, .F. ) ;
#31722=DIRECTION ( 'NONE',  ( 0.000000000000000000, 0.000000000000000000, 1.000000000000000000 ) ) ;
#31723=DIRECTION ( 'NONE',  ( -1.000000000000000000, -0.000000000000000000, 0.000000000000000000 ) ) ;
#31726=ORIENTED_EDGE ( 'NONE', *, *, #4368, .F. ) ;
#31737=VERTEX_POINT ( 'NONE', #41292 ) ;
#31742=AXIS2_PLACEMENT_3D ( 'NONE', #11225, #189, #15145 ) ;
#31745=EDGE_CURVE ( 'NONE', #26295, #43969, #22447, .T. ) ;
#31746=AXIS2_PLACEMENT_3D ( 'NONE', #24615, #6257, #13847 ) ;
#31750=EDGE_CURVE ( 'NONE', #8929, #29160, #5026, .T. ) ;
#31753=DIRECTION ( 'NONE',  ( 1.000000000000000000, 0.000000000000000000, 0.000000000000000000 ) ) ;
#31754=CARTESIAN_POINT ( 'NONE',  ( 10.00000000000000000, 31.47745569255140552, 68.26794271651274926 ) ) ;
#31757=DIRECTION ( 'NONE',  ( -1.000000000000000000, 0.000000000000000000, 0.000000000000000000 ) ) ;
#31758=VERTEX_POINT ( 'NONE', #34393 ) ;
#31761=DIRECTION ( 'NONE',  ( 0.000000000000000000, -0.9510565162951500895, -0.3090169943749581649 ) ) ;
#31766=EDGE_CURVE ( 'NONE', #25818, #26295, #16789, .T. ) ;
#31768=CARTESIAN_POINT ( 'NONE',  ( 10.00000000000000000, 10.30890764327502573, -81.34940948281324324 ) ) ;
#31772=ADVANCED_FACE ( 'NONE', ( #20207 ), #870, .T. ) ;
#31773=CIRCLE ( 'NONE', #34116, 31.99999999999998934 ) ;
#31778=ORIENTED_EDGE ( 'NONE', *, *, #826, .F. ) ;
#31779=CARTESIAN_POINT ( 'NONE',  ( 10.00000000000000000, 0.000000000000000000, 0.000000000000000000 ) ) ;
#31791=DIRECTION ( 'NONE',  ( -1.000000000000000000, -0.000000000000000000, 0.000000000000000000 ) ) ;
#31795=VERTEX_POINT ( 'NONE', #46404 ) ;
#31798=VECTOR ( 'NONE', #33749, 1000.000000000000000 ) ;
#31802=DIRECTION ( 'NONE',  ( 0.000000000000000000, -0.8090169943749402348, -0.5877852522924830181 ) ) ;
#31806=DIRECTION ( 'NONE',  ( 0.000000000000000000, 0.9969173337331276308, 0.07845909572784873220 ) ) ;
#31808=ORIENTED_EDGE ( 'NONE', *, *, #7633, .F. ) ;
#31810=EDGE_CURVE ( 'NONE', #42670, #46575, #12630, .T. ) ;
#31813=AXIS2_PLACEMENT_3D ( 'NONE', #4068, #34160, #15340 ) ;
#31820=DIRECTION ( 'NONE',  ( -1.000000000000000000, 0.000000000000000000, 0.000000000000000000 ) ) ;
#31821=ORIENTED_EDGE ( 'NONE', *, *, #2976, .F. ) ;
#31825=CARTESIAN_POINT ( 'NONE',  ( 0.000000000000000000, -46.21855187248583974, -62.20884554314070414 ) ) ;
#31833=VERTEX_POINT ( 'NONE', #42976 ) ;
#31836=AXIS2_PLACEMENT_3D ( 'NONE', #42230, #8685, #19233 ) ;
#31844=CARTESIAN_POINT ( 'NONE',  ( 10.00000000000000000, 0.000000000000000000, 0.000000000000000000 ) ) ;
#31846=CARTESIAN_POINT ( 'NONE',  ( 10.00000000000000000, 0.000000000000000000, 0.000000000000000000 ) ) ;
#31856=CYLINDRICAL_SURFACE ( 'NONE', #38725, 82.00000000000000000 ) ;
#31865=CYLINDRICAL_SURFACE ( 'NONE', #1234, 31.99999999999998579 ) ;
#31866=DIRECTION ( 'NONE',  ( -1.000000000000000000, 0.000000000000000000, 0.000000000000000000 ) ) ;
#31867=EDGE_CURVE ( 'NONE', #21020, #23818, #23059, .T. ) ;
#31869=EDGE_CURVE ( 'NONE', #12683, #27602, #1122, .T. ) ;
#31871=CARTESIAN_POINT ( 'NONE',  ( 10.00000000000000000, -12.93880638057259169, -76.41127070299286572 ) ) ;
#31875=ORIENTED_EDGE ( 'NONE', *, *, #8554, .F. ) ;
#31878=DIRECTION ( 'NONE',  ( -1.000000000000000000, -0.000000000000000000, -0.000000000000000000 ) ) ;
#31879=CARTESIAN_POINT ( 'NONE',  ( 0.000000000000000000, -27.74655509720725988, 77.16300072079653205 ) ) ;
#31883=ORIENTED_EDGE ( 'NONE', *, *, #14237, .T. ) ;
#31886=AXIS2_PLACEMENT_3D ( 'NONE', #32154, #25026, #36047 ) ;
#31891=SURFACE_STYLE_FILL_AREA ( #12786 ) ;
#31893=EDGE_CURVE ( 'NONE', #24345, #27291, #17564, .T. ) ;
#31896=ORIENTED_EDGE ( 'NONE', *, *, #4269, .T. ) ;
#31901=ORIENTED_EDGE ( 'NONE', *, *, #20784, .T. ) ;
#31904=CARTESIAN_POINT ( 'NONE',  ( 10.00000000000000000, 0.000000000000000000, 0.000000000000000000 ) ) ;
#31905=CARTESIAN_POINT ( 'NONE',  ( 10.00000000000000000, 17.28742895386191236, -75.54627589209927407 ) ) ;
#31914=CARTESIAN_POINT ( 'NONE',  ( 0.000000000000000000, 51.29473840253317718, -63.97538442413369353 ) ) ;
#31918=EDGE_CURVE ( 'NONE', #40043, #47056, #1966, .T. ) ;
#31919=AXIS2_PLACEMENT_3D ( 'NONE', #35668, #39095, #2140 ) ;
#31929=EDGE_CURVE ( 'NONE', #371, #13186, #3513, .T. ) ;
#31933=DIRECTION ( 'NONE',  ( -1.000000000000000000, 0.000000000000000000, 0.000000000000000000 ) ) ;
#31960=ORIENTED_EDGE ( 'NONE', *, *, #28296, .T. ) ;
#31962=VERTEX_POINT ( 'NONE', #2101 ) ;
#31964=DIRECTION ( 'NONE',  ( -1.000000000000000000, -0.000000000000000000, 0.000000000000000000 ) ) ;
#31965=LINE ( 'NONE', #42236, #26888 ) ;
#31966=LINE ( 'NONE', #13349, #38349 ) ;
#31969=EDGE_CURVE ( 'NONE', #10316, #40419, #30901, .T. ) ;
#31972=DIRECTION ( 'NONE',  ( 0.000000000000000000, 0.000000000000000000, 1.000000000000000000 ) ) ;
#31979=CIRCLE ( 'NONE', #38219, 77.49899999999999523 ) ;
#31986=ORIENTED_EDGE ( 'NONE', *, *, #13723, .T. ) ;
#31991=ORIENTED_EDGE ( 'NONE', *, *, #28713, .F. ) ;
#31992=FACE_OUTER_BOUND ( 'NONE', #33853, .T. ) ;
#31998=VERTEX_POINT ( 'NONE', #32201 ) ;
#32000=CARTESIAN_POINT ( 'NONE',  ( 10.00000000000000000, 0.000000000000000000, 0.000000000000000000 ) ) ;
#32002=AXIS2_PLACEMENT_3D ( 'NONE', #35657, #16564, #42768 ) ;
#32006=ORIENTED_EDGE ( 'NONE', *, *, #47799, .T. ) ;
#32007=AXIS2_PLACEMENT_3D ( 'NONE', #16826, #1905, #46694 ) ;
#32008=EDGE_CURVE ( 'NONE', #42227, #26870, #39493, .T. ) ;
#32009=CARTESIAN_POINT ( 'NONE',  ( 10.00000000000000000, -2.946379043146863719, 75.11764819372146462 ) ) ;
#32013=ORIENTED_EDGE ( 'NONE', *, *, #35655, .T. ) ;
#32019=CARTESIAN_POINT ( 'NONE',  ( 10.00000000000000000, -59.75363087400112505, 56.15606465354937882 ) ) ;
#32020=DIRECTION ( 'NONE',  ( -1.000000000000000000, 0.000000000000000000, 0.000000000000000000 ) ) ;
#32021=DIRECTION ( 'NONE',  ( 0.000000000000000000, 0.000000000000000000, 1.000000000000000000 ) ) ;
#32022=ORIENTED_EDGE ( 'NONE', *, *, #3235, .F. ) ;
#32025=CYLINDRICAL_SURFACE ( 'NONE', #5550, 82.00000000000000000 ) ;
#32028=EDGE_CURVE ( 'NONE', #13467, #23694, #26347, .T. ) ;
#32029=DIRECTION ( 'NONE',  ( -1.000000000000000000, -0.000000000000000000, 0.000000000000000000 ) ) ;
#32044=CIRCLE ( 'NONE', #8562, 77.49899999999999523 ) ;
#32047=VERTEX_POINT ( 'NONE', #41048 ) ;
#32048=AXIS2_PLACEMENT_3D ( 'NONE', #24661, #32248, #40978 ) ;
#32054=DIRECTION ( 'NONE',  ( 1.000000000000000000, -0.000000000000000000, -0.000000000000000000 ) ) ;
#32058=ORIENTED_EDGE ( 'NONE', *, *, #1959, .F. ) ;
#32072=DIRECTION ( 'NONE',  ( -1.000000000000000000, -0.000000000000000000, -0.000000000000000000 ) ) ;
#32078=ORIENTED_EDGE ( 'NONE', *, *, #12186, .T. ) ;
#32092=DIRECTION ( 'NONE',  ( 0.000000000000000000, 0.000000000000000000, 1.000000000000000000 ) ) ;
#32094=DIRECTION ( 'NONE',  ( 1.000000000000000000, -0.000000000000000000, -0.000000000000000000 ) ) ;
#32102=CARTESIAN_POINT ( 'NONE',  ( 0.000000000000000000, -31.47745569255092235, -68.26794271651296242 ) ) ;
#32108=CIRCLE ( 'NONE', #35999, 82.00000000000000000 ) ;
#32111=ORIENTED_EDGE ( 'NONE', *, *, #19618, .T. ) ;
#32116=CARTESIAN_POINT ( 'NONE',  ( 10.00000000000000000, 0.000000000000000000, 0.000000000000000000 ) ) ;
#32118=DIRECTION ( 'NONE',  ( 0.000000000000000000, -0.3826834323650772363, -0.9238795325112919565 ) ) ;
#32126=ORIENTED_EDGE ( 'NONE', *, *, #48444, .F. ) ;
#32133=ORIENTED_EDGE ( 'NONE', *, *, #40462, .T. ) ;
#32137=ORIENTED_EDGE ( 'NONE', *, *, #11163, .F. ) ;
#32143=ORIENTED_EDGE ( 'NONE', *, *, #44024, .F. ) ;
#32145=CARTESIAN_POINT ( 'NONE',  ( 10.00000000000000000, 0.000000000000000000, 0.000000000000000000 ) ) ;
#32149=DIRECTION ( 'NONE',  ( -1.000000000000000000, 0.000000000000000000, 0.000000000000000000 ) ) ;
#32150=CARTESIAN_POINT ( 'NONE',  ( 5.000000000000002665, -15.33399622253423722, -80.55351364060604169 ) ) ;
#32152=DIRECTION ( 'NONE',  ( 1.000000000000000000, -0.000000000000000000, 0.000000000000000000 ) ) ;
#32154=CARTESIAN_POINT ( 'NONE',  ( 10.00000000000000000, 0.000000000000000000, 0.000000000000000000 ) ) ;
#32159=CARTESIAN_POINT ( 'NONE',  ( 10.00000000000000000, -20.40083707022935400, 72.35432306680478121 ) ) ;
#32167=DIRECTION ( 'NONE',  ( -1.000000000000000000, -0.000000000000000000, -0.000000000000000000 ) ) ;
#32169=ORIENTED_EDGE ( 'NONE', *, *, #19388, .F. ) ;
#32177=AXIS2_PLACEMENT_3D ( 'NONE', #15287, #18458, #44890 ) ;
#32184=EDGE_CURVE ( 'NONE', #2237, #26319, #1112, .T. ) ;
#32190=CARTESIAN_POINT ( 'NONE',  ( 10.00000000000000000, -54.21277698773636899, -55.38113227695839669 ) ) ;
#32192=DIRECTION ( 'NONE',  ( 0.000000000000000000, 0.9723699203976773342, -0.2334453638559024213 ) ) ;
#32194=DIRECTION ( 'NONE',  ( -1.000000000000000000, -0.000000000000000000, -0.000000000000000000 ) ) ;
#32199=EDGE_CURVE ( 'NONE', #33470, #33708, #9187, .T. ) ;
#32201=CARTESIAN_POINT ( 'NONE',  ( 10.00000000000000000, -71.91182617369167929, -28.89263327155822481 ) ) ;
#32203=CARTESIAN_POINT ( 'NONE',  ( 5.000000000000002665, 16.65972982744934683, 80.28980883073764119 ) ) ;
#32204=CARTESIAN_POINT ( 'NONE',  ( 0.000000000000000000, 0.000000000000000000, 0.000000000000000000 ) ) ;
#32216=DIRECTION ( 'NONE',  ( -1.000000000000000000, 0.000000000000000000, -0.000000000000000000 ) ) ;
#32217=ORIENTED_EDGE ( 'NONE', *, *, #5083, .T. ) ;
#32219=AXIS2_PLACEMENT_3D ( 'NONE', #20014, #28092, #35677 ) ;
#32222=ADVANCED_FACE ( 'NONE', ( #27315 ), #30744, .T. ) ;
#32223=DIRECTION ( 'NONE',  ( -1.000000000000000000, 0.000000000000000000, 0.000000000000000000 ) ) ;
#32224=ORIENTED_EDGE ( 'NONE', *, *, #7893, .F. ) ;
#32226=ORIENTED_EDGE ( 'NONE', *, *, #46970, .T. ) ;
#32227=CIRCLE ( 'NONE', #27536, 77.49899999999999523 ) ;
#32228=DIRECTION ( 'NONE',  ( 0.000000000000000000, 0.000000000000000000, 1.000000000000000000 ) ) ;
#32229=ORIENTED_EDGE ( 'NONE', *, *, #11804, .T. ) ;
#32230=EDGE_CURVE ( 'NONE', #15196, #41616, #8242, .T. ) ;
#32232=AXIS2_PLACEMENT_3D ( 'NONE', #39564, #47125, #14077 ) ;
#32235=ORIENTED_EDGE ( 'NONE', *, *, #36679, .F. ) ;
#32236=VERTEX_POINT ( 'NONE', #38824 ) ;
#32237=ORIENTED_EDGE ( 'NONE', *, *, #12606, .T. ) ;
#32238=CIRCLE ( 'NONE', #3319, 31.99999999999998934 ) ;
#32248=DIRECTION ( 'NONE',  ( -1.000000000000000000, -0.000000000000000000, 0.000000000000000000 ) ) ;
#32252=CARTESIAN_POINT ( 'NONE',  ( 0.000000000000000000, 70.53064760720316428, -26.01480285779861035 ) ) ;
#32254=CARTESIAN_POINT ( 'NONE',  ( 10.00000000000000000, 0.000000000000000000, 0.000000000000000000 ) ) ;
#32257=CARTESIAN_POINT ( 'NONE',  ( 10.00000000000000000, 76.41127070299273782, 12.93880638057342836 ) ) ;
#32258=VERTEX_POINT ( 'NONE', #5284 ) ;
#32259=AXIS2_PLACEMENT_3D ( 'NONE', #14912, #18334, #25664 ) ;
#32278=VERTEX_POINT ( 'NONE', #21649 ) ;
#32284=EDGE_CURVE ( 'NONE', #7344, #7731, #31709, .T. ) ;
#32287=CARTESIAN_POINT ( 'NONE',  ( 5.000000000000000000, 51.29473840253223926, 63.97538442413444670 ) ) ;
#32302=CYLINDRICAL_SURFACE ( 'NONE', #46310, 32.00000000000000000 ) ;
#32305=DIRECTION ( 'NONE',  ( -1.000000000000000000, -0.000000000000000000, 0.000000000000000000 ) ) ;
#32308=CARTESIAN_POINT ( 'NONE',  ( 10.00000000000000000, 70.52718814184260054, 26.02418014898334420 ) ) ;
#32311=ORIENTED_EDGE ( 'NONE', *, *, #5083, .F. ) ;
#32315=ORIENTED_EDGE ( 'NONE', *, *, #2477, .T. ) ;
#32316=AXIS2_PLACEMENT_3D ( 'NONE', #23306, #11578, #26502 ) ;
#32324=CARTESIAN_POINT ( 'NONE',  ( 10.00000000000000000, 70.52718814184294160, -26.02418014898236720 ) ) ;
#32326=LINE ( 'NONE', #36471, #24456 ) ;
#32327=DIRECTION ( 'NONE',  ( -1.000000000000000000, -0.000000000000000000, -0.000000000000000000 ) ) ;
#32335=ORIENTED_EDGE ( 'NONE', *, *, #33559, .F. ) ;
#32336=ORIENTED_EDGE ( 'NONE', *, *, #31918, .F. ) ;
#32337=EDGE_CURVE ( 'NONE', #40687, #23501, #43434, .T. ) ;
#32339=CARTESIAN_POINT ( 'NONE',  ( 10.00000000000000000, 68.26794271651307611, -31.47745569255064169 ) ) ;
#32340=CIRCLE ( 'NONE', #36236, 31.99999999999999645 ) ;
#32349=AXIS2_PLACEMENT_3D ( 'NONE', #1498, #30885, #24243 ) ;
#32350=DIRECTION ( 'NONE',  ( -1.000000000000000000, -0.000000000000000000, -0.000000000000000000 ) ) ;
#32358=DIRECTION ( 'NONE',  ( 0.000000000000000000, -1.000000000000000000, -1.040834085586084414E-14 ) ) ;
#32366=AXIS2_PLACEMENT_3D ( 'NONE', #25393, #40351, #6809 ) ;
#32368=LINE ( 'NONE', #13516, #14846 ) ;
#32370=CARTESIAN_POINT ( 'NONE',  ( 10.00000000000000000, -21.60688246758641995, 79.10210256391358996 ) ) ;
#32377=ORIENTED_EDGE ( 'NONE', *, *, #13830, .F. ) ;
#32378=AXIS2_PLACEMENT_3D ( 'NONE', #25091, #14081, #21421 ) ;
#32391=DIRECTION ( 'NONE',  ( 0.000000000000000000, 0.000000000000000000, -1.000000000000000000 ) ) ;
#32394=ADVANCED_FACE ( 'NONE', ( #48074 ), #40498, .T. ) ;
#32396=DIRECTION ( 'NONE',  ( -1.000000000000000000, -0.000000000000000000, -0.000000000000000000 ) ) ;
#32409=AXIS2_PLACEMENT_3D ( 'NONE', #14829, #9515, #37095 ) ;
#32412=ORIENTED_EDGE ( 'NONE', *, *, #37693, .F. ) ;
#32415=EDGE_LOOP ( 'NONE', ( #9406, #6226, #28546, #27923 ) ) ;
#32425=VERTEX_POINT ( 'NONE', #41457 ) ;
#32426=AXIS2_PLACEMENT_3D ( 'NONE', #21657, #21165, #40024 ) ;
#32436=DIRECTION ( 'NONE',  ( -1.000000000000000000, -0.000000000000000000, -0.000000000000000000 ) ) ;
#32438=CARTESIAN_POINT ( 'NONE',  ( 10.00000000000000000, 0.000000000000000000, 0.000000000000000000 ) ) ;
#32441=CARTESIAN_POINT ( 'NONE',  ( 10.00000000000000000, -2.956366410621191765, 75.11725578898467859 ) ) ;
#32447=FACE_OUTER_BOUND ( 'NONE', #7765, .T. ) ;
#32450=CARTESIAN_POINT ( 'NONE',  ( 0.000000000000000000, 76.41127070299273782, 12.93880638057342836 ) ) ;
#32455=VECTOR ( 'NONE', #31757, 1000.000000000000000 ) ;
#32456=CARTESIAN_POINT ( 'NONE',  ( 10.00000000000000000, 58.39081064771751528, 50.95692526931350841 ) ) ;
#32459=EDGE_CURVE ( 'NONE', #13395, #7073, #19164, .T. ) ;
#32465=ORIENTED_EDGE ( 'NONE', *, *, #8180, .T. ) ;
#32473=FACE_OUTER_BOUND ( 'NONE', #20959, .T. ) ;
#32476=CARTESIAN_POINT ( 'NONE',  ( 10.00000000000000000, 46.53671651293948486, 59.03961581697416250 ) ) ;
#32477=DIRECTION ( 'NONE',  ( -1.000000000000000000, 0.000000000000000000, -0.000000000000000000 ) ) ;
#32481=CIRCLE ( 'NONE', #24654, 77.49899999999999523 ) ;
#32482=AXIS2_PLACEMENT_3D ( 'NONE', #47053, #13517, #2971 ) ;
#32488=EDGE_CURVE ( 'NONE', #9223, #26325, #13765, .T. ) ;
#32489=AXIS2_PLACEMENT_3D ( 'NONE', #8416, #19906, #4986 ) ;
#32492=FACE_OUTER_BOUND ( 'NONE', #8629, .T. ) ;
#32493=EDGE_CURVE ( 'NONE', #43938, #21525, #45813, .T. ) ;
#32495=CIRCLE ( 'NONE', #23084, 77.49899999999999523 ) ;
#32503=AXIS2_PLACEMENT_3D ( 'NONE', #9749, #24687, #28606 ) ;
#32504=CARTESIAN_POINT ( 'NONE',  ( 10.00000000000000000, 8.830959090343430518, -74.65491531819107252 ) ) ;
#32506=EDGE_CURVE ( 'NONE', #7163, #43544, #7514, .T. ) ;
#32513=VERTEX_POINT ( 'NONE', #44405 ) ;
#32517=VERTEX_POINT ( 'NONE', #10874 ) ;
#32522=CARTESIAN_POINT ( 'NONE',  ( 10.00000000000000000, 23.16143007188426850, 73.95703589263983702 ) ) ;
#32525=AXIS2_PLACEMENT_3D ( 'NONE', #26315, #26787, #11396 ) ;
#32527=VERTEX_POINT ( 'NONE', #26036 ) ;
#32528=ORIENTED_EDGE ( 'NONE', *, *, #32184, .T. ) ;
#32530=VERTEX_POINT ( 'NONE', #18919 ) ;
#32533=DIRECTION ( 'NONE',  ( -1.000000000000000000, 0.000000000000000000, 0.000000000000000000 ) ) ;
#32535=ORIENTED_EDGE ( 'NONE', *, *, #45625, .F. ) ;
#32537=ORIENTED_EDGE ( 'NONE', *, *, #24502, .F. ) ;
#32538=FACE_OUTER_BOUND ( 'NONE', #20529, .T. ) ;
#32541=LINE ( 'NONE', #6357, #18934 ) ;
#32544=CARTESIAN_POINT ( 'NONE',  ( 5.000000000000002665, -80.28980883073747066, -16.65972982745018172 ) ) ;
#32545=EDGE_LOOP ( 'NONE', ( #8023, #43623, #9743, #13142 ) ) ;
#32546=DIRECTION ( 'NONE',  ( -1.000000000000000000, 0.000000000000000000, 0.000000000000000000 ) ) ;
#32554=VERTEX_POINT ( 'NONE', #27258 ) ;
#32559=DIRECTION ( 'NONE',  ( 0.000000000000000000, 0.000000000000000000, -1.000000000000000000 ) ) ;
#32561=EDGE_CURVE ( 'NONE', #6408, #48250, #38767, .T. ) ;
#32564=LINE ( 'NONE', #47485, #22371 ) ;
#32569=AXIS2_PLACEMENT_3D ( 'NONE', #46413, #19977, #27829 ) ;
#32573=CARTESIAN_POINT ( 'NONE',  ( 0.000000000000000000, -39.78640506895559525, -66.50666863322042843 ) ) ;
#32574=CARTESIAN_POINT ( 'NONE',  ( 10.00000000000000000, 67.80270845531956070, -46.11716303203112943 ) ) ;
#32575=VERTEX_POINT ( 'NONE', #42419 ) ;
#32578=DIRECTION ( 'NONE',  ( 0.000000000000000000, 0.000000000000000000, 1.000000000000000000 ) ) ;
#32581=VERTEX_POINT ( 'NONE', #27021 ) ;
#32584=CARTESIAN_POINT ( 'NONE',  ( 10.00000000000000000, 70.53064760720316428, -26.01480285779861035 ) ) ;
#32585=DIRECTION ( 'NONE',  ( -1.000000000000000000, -0.000000000000000000, -0.000000000000000000 ) ) ;
#32590=AXIS2_PLACEMENT_3D ( 'NONE', #5532, #13126, #20454 ) ;
#32591=LINE ( 'NONE', #21581, #36862 ) ;
#32601=ORIENTED_EDGE ( 'NONE', *, *, #37761, .F. ) ;
#32603=EDGE_CURVE ( 'NONE', #33968, #22554, #48136, .T. ) ;
#32604=CARTESIAN_POINT ( 'NONE',  ( 10.00000000000000000, 18.89407956138256139, 75.16055320797038064 ) ) ;
#32605=DIRECTION ( 'NONE',  ( 0.000000000000000000, 0.000000000000000000, 1.000000000000000000 ) ) ;
#32606=CARTESIAN_POINT ( 'NONE',  ( 10.00000000000000000, 79.10210256391397365, -21.60688246758502373 ) ) ;
#32607=CARTESIAN_POINT ( 'NONE',  ( 0.000000000000000000, 51.29473840253223926, 63.97538442413444670 ) ) ;
#32612=AXIS2_PLACEMENT_3D ( 'NONE', #29249, #21413, #32671 ) ;
#32618=DIRECTION ( 'NONE',  ( -1.000000000000000000, -0.000000000000000000, -0.000000000000000000 ) ) ;
#32625=ORIENTED_EDGE ( 'NONE', *, *, #22763, .F. ) ;
#32629=VECTOR ( 'NONE', #16319, 1000.000000000000000 ) ;
#32631=CARTESIAN_POINT ( 'NONE',  ( 10.00000000000000000, 0.000000000000000000, 0.000000000000000000 ) ) ;
#32638=DIRECTION ( 'NONE',  ( 0.000000000000000000, 0.000000000000000000, -1.000000000000000000 ) ) ;
#32639=EDGE_CURVE ( 'NONE', #20444, #32581, #23898, .T. ) ;
#32645=CARTESIAN_POINT ( 'NONE',  ( 10.00000000000000000, 46.54456581323805153, 59.03342792756280488 ) ) ;
#32661=ORIENTED_EDGE ( 'NONE', *, *, #27119, .F. ) ;
#32668=CARTESIAN_POINT ( 'NONE',  ( 10.00000000000000000, -59.03961581697432592, 46.53671651293927880 ) ) ;
#32669=ORIENTED_EDGE ( 'NONE', *, *, #37699, .F. ) ;
#32671=DIRECTION ( 'NONE',  ( 0.000000000000000000, 0.000000000000000000, 1.000000000000000000 ) ) ;
#32673=FACE_OUTER_BOUND ( 'NONE', #1859, .T. ) ;
#32675=CIRCLE ( 'NONE', #48291, 31.99999999999999289 ) ;
#32676=ADVANCED_FACE ( 'NONE', ( #39960 ), #43148, .T. ) ;
#32684=CARTESIAN_POINT ( 'NONE',  ( 10.00000000000000000, 60.67117009219136037, 55.16347631943062879 ) ) ;
#32689=CARTESIAN_POINT ( 'NONE',  ( 10.00000000000000000, 77.16300072079661732, 27.74655509720697921 ) ) ;
#32691=VERTEX_POINT ( 'NONE', #5457 ) ;
#32693=ORIENTED_EDGE ( 'NONE', *, *, #40511, .T. ) ;
#32697=DIRECTION ( 'NONE',  ( -1.000000000000000000, 0.000000000000000000, 0.000000000000000000 ) ) ;
#32698=ORIENTED_EDGE ( 'NONE', *, *, #27583, .F. ) ;
#32702=ORIENTED_EDGE ( 'NONE', *, *, #9445, .F. ) ;
#32703=VERTEX_POINT ( 'NONE', #17419 ) ;
#32711=ADVANCED_FACE ( 'NONE', ( #21092 ), #20876, .T. ) ;
#32717=DIRECTION ( 'NONE',  ( -1.000000000000000000, -0.000000000000000000, 0.000000000000000000 ) ) ;
#32727=DIRECTION ( 'NONE',  ( -1.000000000000000000, 0.000000000000000000, 0.000000000000000000 ) ) ;
#32738=ORIENTED_EDGE ( 'NONE', *, *, #38689, .F. ) ;
#32739=EDGE_LOOP ( 'NONE', ( #43132, #4552, #694, #38813 ) ) ;
#32755=ORIENTED_EDGE ( 'NONE', *, *, #27705, .T. ) ;
#32762=CARTESIAN_POINT ( 'NONE',  ( 5.000000000000002665, -81.96053171279903893, 2.543863470248101333 ) ) ;
#32763=ORIENTED_EDGE ( 'NONE', *, *, #25130, .T. ) ;
#32767=CARTESIAN_POINT ( 'NONE',  ( 10.00000000000000000, -55.19960302592029677, -51.03279382321147750 ) ) ;
#32769=AXIS2_PLACEMENT_3D ( 'NONE', #3069, #29517, #36606 ) ;
#32770=EDGE_LOOP ( 'NONE', ( #3187, #1231, #5453, #33328 ) ) ;
#32782=EDGE_LOOP ( 'NONE', ( #45572, #19574, #25869, #34744 ) ) ;
#32785=FACE_OUTER_BOUND ( 'NONE', #42042, .T. ) ;
#32797=EDGE_CURVE ( 'NONE', #40433, #2363, #2818, .T. ) ;
#32799=AXIS2_PLACEMENT_3D ( 'NONE', #45491, #11977, #26908 ) ;
#32803=CARTESIAN_POINT ( 'NONE',  ( 10.00000000000000000, -41.76106447765443619, -62.50884508063471401 ) ) ;
#32807=EDGE_CURVE ( 'NONE', #35473, #40588, #21821, .T. ) ;
#32808=EDGE_CURVE ( 'NONE', #10070, #39605, #6668, .T. ) ;
#32811=CIRCLE ( 'NONE', #20310, 12.50000000000000000 ) ;
#32813=ORIENTED_EDGE ( 'NONE', *, *, #28792, .F. ) ;
#32820=CARTESIAN_POINT ( 'NONE',  ( 10.00000000000000000, 0.000000000000000000, 0.000000000000000000 ) ) ;
#32833=CARTESIAN_POINT ( 'NONE',  ( 10.00000000000000000, -26.01480285779785362, -70.53064760720343429 ) ) ;
#32835=DIRECTION ( 'NONE',  ( 0.000000000000000000, 0.9969173337331281859, -0.07845909572784168229 ) ) ;
#32844=CARTESIAN_POINT ( 'NONE',  ( 0.000000000000000000, -68.26794271651239399, -31.47745569255214093 ) ) ;
#32848=CARTESIAN_POINT ( 'NONE',  ( 0.000000000000000000, 55.20638768913831029, -51.02545421589267960 ) ) ;
#32849=CARTESIAN_POINT ( 'NONE',  ( 0.000000000000000000, 0.000000000000000000, 0.000000000000000000 ) ) ;
#32852=AXIS2_PLACEMENT_3D ( 'NONE', #43463, #9668, #21407 ) ;
#32858=CIRCLE ( 'NONE', #16448, 77.49899999999999523 ) ;
#32861=EDGE_CURVE ( 'NONE', #30212, #16459, #18136, .T. ) ;
#32878=AXIS2_PLACEMENT_3D ( 'NONE', #33723, #41097, #41331 ) ;
#32879=ORIENTED_EDGE ( 'NONE', *, *, #15832, .T. ) ;
#32883=CARTESIAN_POINT ( 'NONE',  ( 10.00000000000000000, -74.65491531819111515, -8.830959090343204920 ) ) ;
#32886=CARTESIAN_POINT ( 'NONE',  ( 10.00000000000000000, 17.28742895386191236, -75.54627589209927407 ) ) ;
#32887=EDGE_CURVE ( 'NONE', #18371, #7999, #11330, .T. ) ;
#32889=AXIS2_PLACEMENT_3D ( 'NONE', #5111, #20023, #16594 ) ;
#32890=DIRECTION ( 'NONE',  ( -1.000000000000000000, -0.000000000000000000, 0.000000000000000000 ) ) ;
#32895=DIRECTION ( 'NONE',  ( 0.000000000000000000, 0.000000000000000000, 1.000000000000000000 ) ) ;
#32896=FACE_OUTER_BOUND ( 'NONE', #2182, .T. ) ;
#32906=DIRECTION ( 'NONE',  ( -1.000000000000000000, -0.000000000000000000, 0.000000000000000000 ) ) ;
#32907=CARTESIAN_POINT ( 'NONE',  ( 10.00000000000000000, 0.000000000000000000, 0.000000000000000000 ) ) ;
#32910=ORIENTED_EDGE ( 'NONE', *, *, #13381, .F. ) ;
#32915=CARTESIAN_POINT ( 'NONE',  ( 5.000000000000002665, 78.73519480814955784, 22.90783923731657268 ) ) ;
#32918=ADVANCED_FACE ( 'NONE', ( #18864 ), #25241, .T. ) ;
#32922=ORIENTED_EDGE ( 'NONE', *, *, #8156, .T. ) ;
#32923=VERTEX_POINT ( 'NONE', #34047 ) ;
#32924=VECTOR ( 'NONE', #37429, 1000.000000000000000 ) ;
#32927=EDGE_CURVE ( 'NONE', #28709, #10878, #15243, .T. ) ;
#32929=CARTESIAN_POINT ( 'NONE',  ( 10.00000000000000000, 0.000000000000000000, 0.000000000000000000 ) ) ;
#32930=ORIENTED_EDGE ( 'NONE', *, *, #9427, .F. ) ;
#32932=CYLINDRICAL_SURFACE ( 'NONE', #5862, 32.00000000000000000 ) ;
#32933=ADVANCED_FACE ( 'NONE', ( #16190 ), #4914, .T. ) ;
#32935=CARTESIAN_POINT ( 'NONE',  ( 10.00000000000000000, 0.000000000000000000, 0.000000000000000000 ) ) ;
#32945=DIRECTION ( 'NONE',  ( -1.000000000000000000, 0.000000000000000000, 0.000000000000000000 ) ) ;
#32947=ORIENTED_EDGE ( 'NONE', *, *, #21841, .T. ) ;
#32949=CARTESIAN_POINT ( 'NONE',  ( 10.00000000000000000, 0.000000000000000000, 0.000000000000000000 ) ) ;
#32952=DIRECTION ( 'NONE',  ( 0.000000000000000000, -0.3090169943749548898, 0.9510565162951511997 ) ) ;
#32953=CARTESIAN_POINT ( 'NONE',  ( 10.00000000000000000, -54.21277698773715059, 55.38113227695762930 ) ) ;
#32954=LINE ( 'NONE', #47880, #24467 ) ;
#32961=DIRECTION ( 'NONE',  ( -1.000000000000000000, 0.000000000000000000, -0.000000000000000000 ) ) ;
#32964=VERTEX_POINT ( 'NONE', #30881 ) ;
#32971=FACE_OUTER_BOUND ( 'NONE', #19104, .T. ) ;
#32975=EDGE_LOOP ( 'NONE', ( #35232, #21577, #11205, #18299 ) ) ;
#32982=EDGE_CURVE ( 'NONE', #12875, #28552, #23928, .T. ) ;
#32983=ORIENTED_EDGE ( 'NONE', *, *, #5599, .T. ) ;
#32990=LINE ( 'NONE', #9999, #34711 ) ;
#32991=VERTEX_POINT ( 'NONE', #26714 ) ;
#33001=ORIENTED_EDGE ( 'NONE', *, *, #30368, .F. ) ;
#33002=DIRECTION ( 'NONE',  ( -1.000000000000000000, 0.000000000000000000, -0.000000000000000000 ) ) ;
#33005=ORIENTED_EDGE ( 'NONE', *, *, #28283, .T. ) ;
#33008=DIRECTION ( 'NONE',  ( 0.000000000000000000, 0.000000000000000000, -1.000000000000000000 ) ) ;
#33013=CYLINDRICAL_SURFACE ( 'NONE', #22848, 77.49899999999999523 ) ;
#33019=CARTESIAN_POINT ( 'NONE',  ( 10.00000000000000000, -68.55367621811173251, 44.99326035066030016 ) ) ;
#33030=CIRCLE ( 'NONE', #36937, 77.49900000000000944 ) ;
#33042=DIRECTION ( 'NONE',  ( 0.000000000000000000, 0.3090169943749411785, 0.9510565162951556406 ) ) ;
#33043=ADVANCED_FACE ( 'NONE', ( #27443 ), #11550, .T. ) ;
#33053=CARTESIAN_POINT ( 'NONE',  ( 10.00000000000000000, 0.000000000000000000, 0.000000000000000000 ) ) ;
#33062=CARTESIAN_POINT ( 'NONE',  ( 10.00000000000000000, -35.91791733033426226, -68.67312586195033930 ) ) ;
#33070=DIRECTION ( 'NONE',  ( 0.000000000000000000, 0.000000000000000000, -1.000000000000000000 ) ) ;
#33072=DIRECTION ( 'NONE',  ( -1.000000000000000000, -0.000000000000000000, -0.000000000000000000 ) ) ;
#33075=VERTEX_POINT ( 'NONE', #38948 ) ;
#33081=CYLINDRICAL_SURFACE ( 'NONE', #17231, 32.00000000000000000 ) ;
#33087=DIRECTION ( 'NONE',  ( 0.000000000000000000, 0.9969173337331282969, -0.07845909572784179331 ) ) ;
#33089=CARTESIAN_POINT ( 'NONE',  ( 0.000000000000000000, -36.72794159290288718, 65.59268652807197952 ) ) ;
#33093=DIRECTION ( 'NONE',  ( -1.000000000000000000, -0.000000000000000000, 0.000000000000000000 ) ) ;
#33098=ORIENTED_EDGE ( 'NONE', *, *, #7656, .F. ) ;
#33100=DIRECTION ( 'NONE',  ( 1.000000000000000000, 0.000000000000000000, -0.000000000000000000 ) ) ;
#33105=EDGE_CURVE ( 'NONE', #12571, #38965, #27940, .T. ) ;
#33107=ORIENTED_EDGE ( 'NONE', *, *, #23640, .F. ) ;
#33111=VERTEX_POINT ( 'NONE', #13466 ) ;
#33120=ORIENTED_EDGE ( 'NONE', *, *, #30890, .T. ) ;
#33121=VECTOR ( 'NONE', #28236, 1000.000000000000000 ) ;
#33124=VERTEX_POINT ( 'NONE', #17133 ) ;
#33126=VECTOR ( 'NONE', #40991, 1000.000000000000000 ) ;
#33130=ORIENTED_EDGE ( 'NONE', *, *, #13550, .F. ) ;
#33136=DIRECTION ( 'NONE',  ( -1.000000000000000000, 0.000000000000000000, -0.000000000000000000 ) ) ;
#33143=ORIENTED_EDGE ( 'NONE', *, *, #29244, .F. ) ;
#33165=ADVANCED_FACE ( 'NONE', ( #24730 ), #31856, .T. ) ;
#33169=DIRECTION ( 'NONE',  ( -1.000000000000000000, 0.000000000000000000, -0.000000000000000000 ) ) ;
#33171=CIRCLE ( 'NONE', #12080, 77.49899999999999523 ) ;
#33179=AXIS2_PLACEMENT_3D ( 'NONE', #21951, #7022, #41299 ) ;
#33182=CYLINDRICAL_SURFACE ( 'NONE', #21848, 31.99999999999999289 ) ;
#33184=VECTOR ( 'NONE', #404, 1000.000000000000000 ) ;
#33200=EDGE_LOOP ( 'NONE', ( #6955, #18224, #25112, #15124 ) ) ;
#33215=AXIS2_PLACEMENT_3D ( 'NONE', #25050, #40002, #3257 ) ;
#33220=AXIS2_PLACEMENT_3D ( 'NONE', #12278, #23511, #38713 ) ;
#33224=AXIS2_PLACEMENT_3D ( 'NONE', #10651, #25558, #31972 ) ;
#33225=EDGE_CURVE ( 'NONE', #17540, #32047, #42633, .T. ) ;
#33226=DIRECTION ( 'NONE',  ( -1.000000000000000000, -0.000000000000000000, -0.000000000000000000 ) ) ;
#33235=CARTESIAN_POINT ( 'NONE',  ( 10.00000000000000000, -81.96053171279902472, 2.543863470248087566 ) ) ;
#33246=ORIENTED_EDGE ( 'NONE', *, *, #35460, .F. ) ;
#33254=ORIENTED_EDGE ( 'NONE', *, *, #45088, .T. ) ;
#33258=CIRCLE ( 'NONE', #30171, 31.99999999999999645 ) ;
#33261=EDGE_LOOP ( 'NONE', ( #40674, #11284, #8735, #12698 ) ) ;
#33262=EDGE_CURVE ( 'NONE', #45718, #6408, #27007, .T. ) ;
#33266=CARTESIAN_POINT ( 'NONE',  ( 10.00000000000000000, -22.90783923731575911, -78.73519480814978522 ) ) ;
#33269=EDGE_CURVE ( 'NONE', #5219, #7382, #3511, .T. ) ;
#33279=CIRCLE ( 'NONE', #3617, 82.00000000000000000 ) ;
#33284=CARTESIAN_POINT ( 'NONE',  ( 5.000000000000000000, -64.81221759200306565, -50.23322058963418613 ) ) ;
#33285=AXIS2_PLACEMENT_3D ( 'NONE', #47302, #14003, #2043 ) ;
#33293=AXIS2_PLACEMENT_3D ( 'NONE', #36589, #6265, #44661 ) ;
#33295=ORIENTED_EDGE ( 'NONE', *, *, #36616, .F. ) ;
#33302=VERTEX_POINT ( 'NONE', #33503 ) ;
#33305=ORIENTED_EDGE ( 'NONE', *, *, #36306, .F. ) ;
#33306=CYLINDRICAL_SURFACE ( 'NONE', #34378, 82.00000000000000000 ) ;
#33311=ORIENTED_EDGE ( 'NONE', *, *, #20374, .T. ) ;
#33313=CYLINDRICAL_SURFACE ( 'NONE', #37654, 31.99999999999999289 ) ;
#33319=ORIENTED_EDGE ( 'NONE', *, *, #45581, .T. ) ;
#33328=ORIENTED_EDGE ( 'NONE', *, *, #18616, .T. ) ;
#33332=VERTEX_POINT ( 'NONE', #43801 ) ;
#33334=AXIS2_PLACEMENT_3D ( 'NONE', #34531, #31379, #42868 ) ;
#33343=CARTESIAN_POINT ( 'NONE',  ( 10.00000000000000000, -8.830959090342926032, 74.65491531819115778 ) ) ;
#33344=LINE ( 'NONE', #35447, #5602 ) ;
#33353=AXIS2_PLACEMENT_3D ( 'NONE', #40785, #47875, #18259 ) ;
#33356=DIRECTION ( 'NONE',  ( 0.000000000000000000, 0.9723699203976756689, 0.2334453638559095268 ) ) ;
#33358=AXIS2_PLACEMENT_3D ( 'NONE', #8827, #20097, #16198 ) ;
#33362=AXIS2_PLACEMENT_3D ( 'NONE', #10833, #6438, #47070 ) ;
#33363=ORIENTED_EDGE ( 'NONE', *, *, #13836, .T. ) ;
#33364=EDGE_CURVE ( 'NONE', #30385, #37478, #39519, .T. ) ;
#33375=DIRECTION ( 'NONE',  ( 1.000000000000000000, -0.000000000000000000, -0.000000000000000000 ) ) ;
#33377=ORIENTED_EDGE ( 'NONE', *, *, #45379, .T. ) ;
#33379=EDGE_CURVE ( 'NONE', #23020, #35449, #8955, .T. ) ;
#33395=ORIENTED_EDGE ( 'NONE', *, *, #40882, .T. ) ;
#33401=AXIS2_PLACEMENT_3D ( 'NONE', #26847, #11683, #34187 ) ;
#33403=ORIENTED_EDGE ( 'NONE', *, *, #34271, .F. ) ;
#33413=DIRECTION ( 'NONE',  ( 0.000000000000000000, 0.000000000000000000, 1.000000000000000000 ) ) ;
#33415=DIRECTION ( 'NONE',  ( 0.000000000000000000, 0.000000000000000000, 1.000000000000000000 ) ) ;
#33417=EDGE_CURVE ( 'NONE', #28552, #18377, #19162, .T. ) ;
#33418=CIRCLE ( 'NONE', #44386, 77.49899999999999523 ) ;
#33419=EDGE_CURVE ( 'NONE', #34570, #12619, #42744, .T. ) ;
#33420=ORIENTED_EDGE ( 'NONE', *, *, #34778, .T. ) ;
#33422=AXIS2_PLACEMENT_3D ( 'NONE', #23405, #40225, #25261 ) ;
#33423=DIRECTION ( 'NONE',  ( 0.000000000000000000, -0.1564344650402170744, -0.9876883405951399908 ) ) ;
#33424=EDGE_LOOP ( 'NONE', ( #18549, #44045, #24187, #4117 ) ) ;
#33428=CARTESIAN_POINT ( 'NONE',  ( 10.00000000000000000, -17.28742895386031719, -75.54627589209962935 ) ) ;
#33452=LINE ( 'NONE', #14625, #33184 ) ;
#33453=EDGE_CURVE ( 'NONE', #9220, #24955, #9006, .T. ) ;
#33454=EDGE_LOOP ( 'NONE', ( #41062, #43082, #28381, #21242 ) ) ;
#33470=VERTEX_POINT ( 'NONE', #1380 ) ;
#33476=VERTEX_POINT ( 'NONE', #39060 ) ;
#33493=CARTESIAN_POINT ( 'NONE',  ( 0.000000000000000000, -70.53064760720297954, -26.01480285779911839 ) ) ;
#33494=ORIENTED_EDGE ( 'NONE', *, *, #39115, .F. ) ;
#33499=DIRECTION ( 'NONE',  ( -1.000000000000000000, 0.000000000000000000, 0.000000000000000000 ) ) ;
#33503=CARTESIAN_POINT ( 'NONE',  ( 0.000000000000000000, 63.97538442413426907, 51.29473840253247374 ) ) ;
#33511=CARTESIAN_POINT ( 'NONE',  ( 0.000000000000000000, 74.65374052328660071, -8.840884882374309583 ) ) ;
#33512=LINE ( 'NONE', #15891, #31798 ) ;
#33520=FACE_OUTER_BOUND ( 'NONE', #42093, .T. ) ;
#33526=EDGE_CURVE ( 'NONE', #24182, #20061, #18433, .T. ) ;
#33530=EDGE_LOOP ( 'NONE', ( #18846, #11054, #35409, #13052 ) ) ;
#33535=EDGE_CURVE ( 'NONE', #34289, #11599, #440, .T. ) ;
#33536=CARTESIAN_POINT ( 'NONE',  ( 0.000000000000000000, 0.000000000000000000, 0.000000000000000000 ) ) ;
#33544=AXIS2_PLACEMENT_3D ( 'NONE', #17107, #16388, #9049 ) ;
#33547=VERTEX_POINT ( 'NONE', #36583 ) ;
#33549=ORIENTED_EDGE ( 'NONE', *, *, #7008, .F. ) ;
#33555=DIRECTION ( 'NONE',  ( -1.000000000000000000, -0.000000000000000000, -0.000000000000000000 ) ) ;
#33556=ORIENTED_EDGE ( 'NONE', *, *, #23832, .T. ) ;
#33559=EDGE_CURVE ( 'NONE', #32964, #11808, #44226, .T. ) ;
#33570=CARTESIAN_POINT ( 'NONE',  ( 0.000000000000000000, 0.000000000000000000, 0.000000000000000000 ) ) ;
#33572=CARTESIAN_POINT ( 'NONE',  ( 10.00000000000000000, 0.000000000000000000, 0.000000000000000000 ) ) ;
#33577=DIRECTION ( 'NONE',  ( -1.000000000000000000, 0.000000000000000000, 0.000000000000000000 ) ) ;
#33587=CARTESIAN_POINT ( 'NONE',  ( 10.00000000000000000, -76.66974797899830207, -11.30684508768422170 ) ) ;
#33590=EDGE_CURVE ( 'NONE', #36506, #20061, #45810, .T. ) ;
#33591=DIRECTION ( 'NONE',  ( -1.000000000000000000, 0.000000000000000000, -0.000000000000000000 ) ) ;
#33594=ADVANCED_FACE ( 'NONE', ( #35630 ), #46891, .T. ) ;
#33607=CYLINDRICAL_SURFACE ( 'NONE', #26926, 77.49899999999999523 ) ;
#33608=CARTESIAN_POINT ( 'NONE',  ( 0.000000000000000000, 55.19960302592141232, -51.03279382321027668 ) ) ;
#33610=CIRCLE ( 'NONE', #12531, 82.00000000000000000 ) ;
#33611=FACE_OUTER_BOUND ( 'NONE', #43651, .T. ) ;
#33613=FACE_OUTER_BOUND ( 'NONE', #5078, .T. ) ;
#33614=VERTEX_POINT ( 'NONE', #36817 ) ;
#33615=EDGE_LOOP ( 'NONE', ( #29892, #31645, #13464, #7573 ) ) ;
#33617=CIRCLE ( 'NONE', #23353, 31.99999999999999645 ) ;
#33620=CARTESIAN_POINT ( 'NONE',  ( 10.00000000000000000, 75.11725578898467859, 2.956366410620910656 ) ) ;
#33624=MECHANICAL_DESIGN_GEOMETRIC_PRESENTATION_REPRESENTATION('',(#5505),#6282);
#33636=VERTEX_POINT ( 'NONE', #30222 ) ;
#33637=DIRECTION ( 'NONE',  ( -1.000000000000000000, -0.000000000000000000, 0.000000000000000000 ) ) ;
#33640=FACE_OUTER_BOUND ( 'NONE', #12433, .T. ) ;
#33643=ORIENTED_EDGE ( 'NONE', *, *, #44687, .F. ) ;
#33644=EDGE_CURVE ( 'NONE', #5621, #29354, #4370, .T. ) ;
#33651=DIRECTION ( 'NONE',  ( 0.000000000000000000, -0.3826834323650774028, -0.9238795325112919565 ) ) ;
#33653=AXIS2_PLACEMENT_3D ( 'NONE', #9301, #1485, #16412 ) ;
#33654=VECTOR ( 'NONE', #38771, 1000.000000000000000 ) ;
#33656=CIRCLE ( 'NONE', #39931, 82.00000000000000000 ) ;
#33658=CARTESIAN_POINT ( 'NONE',  ( 10.00000000000000000, 0.000000000000000000, 0.000000000000000000 ) ) ;
#33659=ORIENTED_EDGE ( 'NONE', *, *, #10799, .T. ) ;
#33661=ORIENTED_EDGE ( 'NONE', *, *, #34080, .T. ) ;
#33664=CYLINDRICAL_SURFACE ( 'NONE', #22564, 77.49899999999999523 ) ;
#33682=CARTESIAN_POINT ( 'NONE',  ( 0.000000000000000000, 16.00000000000000000, 2.500000000000000000 ) ) ;
#33688=AXIS2_PLACEMENT_3D ( 'NONE', #42282, #43251, #28316 ) ;
#33689=DIRECTION ( 'NONE',  ( 0.000000000000000000, 0.4539904997395477482, -0.8910065241883674547 ) ) ;
#33690=VECTOR ( 'NONE', #18744, 1000.000000000000000 ) ;
#33702=ORIENTED_EDGE ( 'NONE', *, *, #37418, .F. ) ;
#33703=DIRECTION ( 'NONE',  ( 0.000000000000000000, 0.000000000000000000, -1.000000000000000000 ) ) ;
#33704=CYLINDRICAL_SURFACE ( 'NONE', #19041, 82.00000000000000000 ) ;
#33708=VERTEX_POINT ( 'NONE', #3776 ) ;
#33715=CIRCLE ( 'NONE', #11819, 77.49899999999999523 ) ;
#33716=DIRECTION ( 'NONE',  ( 0.000000000000000000, 0.000000000000000000, -1.000000000000000000 ) ) ;
#33717=AXIS2_PLACEMENT_3D ( 'NONE', #27082, #11437, #38094 ) ;
#33718=AXIS2_PLACEMENT_3D ( 'NONE', #16578, #1909, #46697 ) ;
#33719=EDGE_LOOP ( 'NONE', ( #17415, #433, #47975, #43086 ) ) ;
#33722=DIRECTION ( 'NONE',  ( 0.000000000000000000, -0.1564344650402381132, 0.9876883405951365491 ) ) ;
#33723=CARTESIAN_POINT ( 'NONE',  ( 10.00000000000000000, -59.03342792756231461, -46.54456581323868392 ) ) ;
#33724=EDGE_LOOP ( 'NONE', ( #30391, #18714, #4608, #14602 ) ) ;
#33726=EDGE_LOOP ( 'NONE', ( #48190, #8423, #1477, #28910 ) ) ;
#33732=CARTESIAN_POINT ( 'NONE',  ( 5.000000000000000000, 63.97538442413498672, -51.29473840253155714 ) ) ;
#33734=EDGE_CURVE ( 'NONE', #39455, #3739, #37791, .T. ) ;
#33745=LINE ( 'NONE', #37671, #9372 ) ;
#33746=EDGE_CURVE ( 'NONE', #23138, #33708, #43431, .T. ) ;
#33748=CIRCLE ( 'NONE', #47037, 31.99999999999998934 ) ;
#33749=DIRECTION ( 'NONE',  ( -1.000000000000000000, 0.000000000000000000, 0.000000000000000000 ) ) ;
#33755=DIRECTION ( 'NONE',  ( 0.000000000000000000, 0.000000000000000000, 1.000000000000000000 ) ) ;
#33761=AXIS2_PLACEMENT_3D ( 'NONE', #34443, #26159, #25901 ) ;
#33767=DIRECTION ( 'NONE',  ( -1.000000000000000000, -0.000000000000000000, -0.000000000000000000 ) ) ;
#33768=AXIS2_PLACEMENT_3D ( 'NONE', #11725, #8292, #30091 ) ;
#33770=ORIENTED_EDGE ( 'NONE', *, *, #26562, .F. ) ;
#33772=ORIENTED_EDGE ( 'NONE', *, *, #4171, .F. ) ;
#33774=DIRECTION ( 'NONE',  ( -1.000000000000000000, 0.000000000000000000, 0.000000000000000000 ) ) ;
#33786=DIRECTION ( 'NONE',  ( -1.000000000000000000, -0.000000000000000000, 0.000000000000000000 ) ) ;
#33790=VERTEX_POINT ( 'NONE', #12578 ) ;
#33797=EDGE_CURVE ( 'NONE', #28683, #29530, #6703, .T. ) ;
#33798=CARTESIAN_POINT ( 'NONE',  ( 0.000000000000000000, -80.55351364060599906, 15.33399622253456585 ) ) ;
#33810=EDGE_CURVE ( 'NONE', #27708, #46337, #8894, .T. ) ;
#33814=DIRECTION ( 'NONE',  ( -1.000000000000000000, 0.000000000000000000, -0.000000000000000000 ) ) ;
#33821=VERTEX_POINT ( 'NONE', #16257 ) ;
#33834=CIRCLE ( 'NONE', #8813, 31.99999999999999645 ) ;
#33839=DIRECTION ( 'NONE',  ( 0.000000000000000000, 0.000000000000000000, 1.000000000000000000 ) ) ;
#33844=AXIS2_PLACEMENT_3D ( 'NONE', #32339, #13966, #43363 ) ;
#33845=DIRECTION ( 'NONE',  ( -1.000000000000000000, -0.000000000000000000, 0.000000000000000000 ) ) ;
#33852=VERTEX_POINT ( 'NONE', #30952 ) ;
#33853=EDGE_LOOP ( 'NONE', ( #673, #7827, #33494, #30263 ) ) ;
#33857=AXIS2_PLACEMENT_3D ( 'NONE', #32252, #28095, #20257 ) ;
#33870=AXIS2_PLACEMENT_3D ( 'NONE', #14885, #28493, #16985 ) ;
#33872=DIRECTION ( 'NONE',  ( -1.000000000000000000, 0.000000000000000000, 0.000000000000000000 ) ) ;
#33877=FACE_OUTER_BOUND ( 'NONE', #20007, .T. ) ;
#33890=AXIS2_PLACEMENT_3D ( 'NONE', #26350, #30273, #13348 ) ;
#33892=DIRECTION ( 'NONE',  ( 0.000000000000000000, 0.000000000000000000, 1.000000000000000000 ) ) ;
#33893=ORIENTED_EDGE ( 'NONE', *, *, #39198, .F. ) ;
#33895=AXIS2_PLACEMENT_3D ( 'NONE', #39012, #21116, #5476 ) ;
#33899=ORIENTED_EDGE ( 'NONE', *, *, #32603, .F. ) ;
#33902=ORIENTED_EDGE ( 'NONE', *, *, #32561, .F. ) ;
#33906=DIRECTION ( 'NONE',  ( -1.000000000000000000, 0.000000000000000000, -0.000000000000000000 ) ) ;
#33910=LINE ( 'NONE', #31230, #16170 ) ;
#33915=LINE ( 'NONE', #398, #8074 ) ;
#33928=CARTESIAN_POINT ( 'NONE',  ( 10.00000000000000000, 0.000000000000000000, 0.000000000000000000 ) ) ;
#33929=EDGE_CURVE ( 'NONE', #3743, #17460, #8176, .T. ) ;
#33937=ORIENTED_EDGE ( 'NONE', *, *, #25873, .T. ) ;
#33944=( NAMED_UNIT ( * ) PLANE_ANGLE_UNIT ( ) SI_UNIT ( $, .RADIAN. ) );
#33948=ORIENTED_EDGE ( 'NONE', *, *, #37455, .T. ) ;
#33951=CARTESIAN_POINT ( 'NONE',  ( 5.000000000000002665, 3.894527615419058009, -81.90746397400384637 ) ) ;
#33952=VERTEX_POINT ( 'NONE', #2505 ) ;
#33955=CYLINDRICAL_SURFACE ( 'NONE', #30420, 77.49899999999999523 ) ;
#33963=DIRECTION ( 'NONE',  ( 0.000000000000000000, 0.3826834323650907810, -0.9238795325112864054 ) ) ;
#33968=VERTEX_POINT ( 'NONE', #36287 ) ;
#33969=CARTESIAN_POINT ( 'NONE',  ( 10.00000000000000000, -12.93880638057259169, -76.41127070299286572 ) ) ;
#33971=ORIENTED_EDGE ( 'NONE', *, *, #18095, .T. ) ;
#33974=CIRCLE ( 'NONE', #1142, 31.99999999999998579 ) ;
#33976=DIRECTION ( 'NONE',  ( 0.000000000000000000, -0.8910065241883626808, -0.4539904997395568520 ) ) ;
#33982=EDGE_CURVE ( 'NONE', #16811, #37458, #3619, .T. ) ;
#33995=DIRECTION ( 'NONE',  ( -1.000000000000000000, 0.000000000000000000, 0.000000000000000000 ) ) ;
#33998=DIRECTION ( 'NONE',  ( -1.000000000000000000, -0.000000000000000000, 0.000000000000000000 ) ) ;
#34003=CARTESIAN_POINT ( 'NONE',  ( 0.000000000000000000, -77.49459641780886443, -0.8261519478439277586 ) ) ;
#34009=AXIS2_PLACEMENT_3D ( 'NONE', #11911, #25185, #47945 ) ;
#34013=ORIENTED_EDGE ( 'NONE', *, *, #27115, .F. ) ;
#34018=ORIENTED_EDGE ( 'NONE', *, *, #7174, .T. ) ;
#34020=EDGE_LOOP ( 'NONE', ( #12059, #45662, #47887, #40847 ) ) ;
#34021=VERTEX_POINT ( 'NONE', #9607 ) ;
#34022=AXIS2_PLACEMENT_3D ( 'NONE', #1691, #20039, #31320 ) ;
#34028=ORIENTED_EDGE ( 'NONE', *, *, #949, .T. ) ;
#34036=EDGE_CURVE ( 'NONE', #25837, #10624, #3583, .T. ) ;
#34038=CYLINDRICAL_SURFACE ( 'NONE', #36727, 77.49899999999999523 ) ;
#34047=CARTESIAN_POINT ( 'NONE',  ( 10.00000000000000000, 55.16347631943129670, -60.67117009219074220 ) ) ;
#34049=DIRECTION ( 'NONE',  ( 0.000000000000000000, 0.3090169943749410120, 0.9510565162951556406 ) ) ;
#34050=VECTOR ( 'NONE', #35322, 1000.000000000000000 ) ;
#34051=DIRECTION ( 'NONE',  ( -1.000000000000000000, -0.000000000000000000, 0.000000000000000000 ) ) ;
#34059=CARTESIAN_POINT ( 'NONE',  ( 10.00000000000000000, -6.903761155837252694, -77.19088730480530103 ) ) ;
#34061=AXIS2_PLACEMENT_3D ( 'NONE', #9409, #16288, #4785 ) ;
#34063=DIRECTION ( 'NONE',  ( 0.000000000000000000, -0.7071067811865389130, -0.7071067811865561215 ) ) ;
#34070=DIRECTION ( 'NONE',  ( -1.000000000000000000, 0.000000000000000000, -0.000000000000000000 ) ) ;
#34072=DIRECTION ( 'NONE',  ( -1.000000000000000000, 0.000000000000000000, -0.000000000000000000 ) ) ;
#34078=ORIENTED_EDGE ( 'NONE', *, *, #5885, .T. ) ;
#34080=EDGE_CURVE ( 'NONE', #45900, #24990, #17190, .T. ) ;
#34088=CARTESIAN_POINT ( 'NONE',  ( 10.00000000000000000, 0.000000000000000000, 0.000000000000000000 ) ) ;
#34098=CIRCLE ( 'NONE', #48155, 31.99999999999999289 ) ;
#34106=CARTESIAN_POINT ( 'NONE',  ( 10.00000000000000000, -71.21200624218766961, -40.65526001592689909 ) ) ;
#34116=AXIS2_PLACEMENT_3D ( 'NONE', #36906, #3375, #44506 ) ;
#34117=CARTESIAN_POINT ( 'NONE',  ( 5.000000000000002665, -81.90746397400386059, -3.894527615418773347 ) ) ;
#34118=DIRECTION ( 'NONE',  ( 0.000000000000000000, 0.07845909572784512398, -0.9969173337331279638 ) ) ;
#34122=DIRECTION ( 'NONE',  ( 0.000000000000000000, 0.000000000000000000, 1.000000000000000000 ) ) ;
#34124=EDGE_CURVE ( 'NONE', #30814, #39658, #23926, .T. ) ;
#34126=DIRECTION ( 'NONE',  ( -1.000000000000000000, 0.000000000000000000, 0.000000000000000000 ) ) ;
#34129=VERTEX_POINT ( 'NONE', #41186 ) ;
#34131=DIRECTION ( 'NONE',  ( 0.000000000000000000, 0.000000000000000000, -1.000000000000000000 ) ) ;
#34136=ORIENTED_EDGE ( 'NONE', *, *, #18721, .F. ) ;
#34139=FACE_OUTER_BOUND ( 'NONE', #10083, .T. ) ;
#34151=CIRCLE ( 'NONE', #20895, 31.99999999999999645 ) ;
#34153=ORIENTED_EDGE ( 'NONE', *, *, #34614, .T. ) ;
#34160=DIRECTION ( 'NONE',  ( -1.000000000000000000, -0.000000000000000000, -0.000000000000000000 ) ) ;
#34173=CYLINDRICAL_SURFACE ( 'NONE', #31413, 77.49899999999999523 ) ;
#34177=CARTESIAN_POINT ( 'NONE',  ( 10.00000000000000000, 6.903761155838878061, -77.19088730480517313 ) ) ;
#34178=DIRECTION ( 'NONE',  ( -1.000000000000000000, 0.000000000000000000, -0.000000000000000000 ) ) ;
#34179=CYLINDRICAL_SURFACE ( 'NONE', #42355, 31.99999999999999289 ) ;
#34180=CARTESIAN_POINT ( 'NONE',  ( 0.000000000000000000, 0.000000000000000000, 0.000000000000000000 ) ) ;
#34184=EDGE_CURVE ( 'NONE', #33636, #15030, #21830, .T. ) ;
#34187=DIRECTION ( 'NONE',  ( 0.000000000000000000, 0.000000000000000000, 1.000000000000000000 ) ) ;
#34188=DIRECTION ( 'NONE',  ( 0.000000000000000000, 0.000000000000000000, -1.000000000000000000 ) ) ;
#34189=ORIENTED_EDGE ( 'NONE', *, *, #4090, .T. ) ;
#34190=VERTEX_POINT ( 'NONE', #7395 ) ;
#34192=ADVANCED_FACE ( 'NONE', ( #22334 ), #29433, .T. ) ;
#34193=ORIENTED_EDGE ( 'NONE', *, *, #40462, .F. ) ;
#34203=ORIENTED_EDGE ( 'NONE', *, *, #23677, .T. ) ;
#34206=DIRECTION ( 'NONE',  ( -1.000000000000000000, -0.000000000000000000, -0.000000000000000000 ) ) ;
#34208=CIRCLE ( 'NONE', #16989, 31.99999999999998579 ) ;
#34215=AXIS2_PLACEMENT_3D ( 'NONE', #1871, #19978, #47779 ) ;
#34218=AXIS2_PLACEMENT_3D ( 'NONE', #16113, #34934, #31046 ) ;
#34223=ORIENTED_EDGE ( 'NONE', *, *, #41610, .T. ) ;
#34224=LINE ( 'NONE', #205, #44722 ) ;
#34227=CARTESIAN_POINT ( 'NONE',  ( 0.000000000000000000, 0.000000000000000000, 0.000000000000000000 ) ) ;
#34234=DIRECTION ( 'NONE',  ( 0.000000000000000000, 0.000000000000000000, 1.000000000000000000 ) ) ;
#34236=ORIENTED_EDGE ( 'NONE', *, *, #43394, .T. ) ;
#34245=CARTESIAN_POINT ( 'NONE',  ( 10.00000000000000000, -20.40083707022935400, 72.35432306680478121 ) ) ;
#34255=ORIENTED_EDGE ( 'NONE', *, *, #4595, .F. ) ;
#34262=DIRECTION ( 'NONE',  ( -1.000000000000000000, 0.000000000000000000, -0.000000000000000000 ) ) ;
#34267=CARTESIAN_POINT ( 'NONE',  ( 0.000000000000000000, 65.64334221924909230, 41.19522573413756561 ) ) ;
#34270=ORIENTED_EDGE ( 'NONE', *, *, #11939, .T. ) ;
#34271=EDGE_CURVE ( 'NONE', #46234, #29434, #44291, .T. ) ;
#34287=DIRECTION ( 'NONE',  ( 0.000000000000000000, 0.000000000000000000, -1.000000000000000000 ) ) ;
#34288=DIRECTION ( 'NONE',  ( -1.000000000000000000, 0.000000000000000000, -0.000000000000000000 ) ) ;
#34289=VERTEX_POINT ( 'NONE', #15947 ) ;
#34290=ADVANCED_FACE ( 'NONE', ( #1503 ), #23517, .T. ) ;
#34292=DIRECTION ( 'NONE',  ( 0.000000000000000000, 0.000000000000000000, 1.000000000000000000 ) ) ;
#34294=ORIENTED_EDGE ( 'NONE', *, *, #9279, .F. ) ;
#34297=FACE_OUTER_BOUND ( 'NONE', #7161, .T. ) ;
#34299=CARTESIAN_POINT ( 'NONE',  ( 10.00000000000000000, 8.840884882375075193, 74.65374052328651544 ) ) ;
#34300=CYLINDRICAL_SURFACE ( 'NONE', #10024, 31.99999999999999289 ) ;
#34305=CYLINDRICAL_SURFACE ( 'NONE', #22882, 77.49899999999999523 ) ;
#34312=VECTOR ( 'NONE', #21908, 1000.000000000000000 ) ;
#34317=CARTESIAN_POINT ( 'NONE',  ( 10.00000000000000000, -62.50329211542465657, 41.76937507738766442 ) ) ;
#34327=EDGE_LOOP ( 'NONE', ( #19198, #3434, #21854, #14352 ) ) ;
#34334=ORIENTED_EDGE ( 'NONE', *, *, #29933, .T. ) ;
#34338=EDGE_CURVE ( 'NONE', #10794, #2137, #16148, .T. ) ;
#34339=DIRECTION ( 'NONE',  ( 0.000000000000000000, 0.000000000000000000, 1.000000000000000000 ) ) ;
#34341=VECTOR ( 'NONE', #38221, 1000.000000000000000 ) ;
#34342=ADVANCED_FACE ( 'NONE', ( #19127 ), #23046, .T. ) ;
#34343=VECTOR ( 'NONE', #9459, 1000.000000000000000 ) ;
#34347=AXIS2_PLACEMENT_3D ( 'NONE', #3561, #7484, #7227 ) ;
#34350=DIRECTION ( 'NONE',  ( -1.000000000000000000, 0.000000000000000000, -0.000000000000000000 ) ) ;
#34353=ORIENTED_EDGE ( 'NONE', *, *, #38, .F. ) ;
#34354=DIRECTION ( 'NONE',  ( 0.000000000000000000, 0.000000000000000000, 1.000000000000000000 ) ) ;
#34355=DIRECTION ( 'NONE',  ( 0.000000000000000000, 0.000000000000000000, 1.000000000000000000 ) ) ;
#34361=EDGE_CURVE ( 'NONE', #22636, #4251, #41971, .T. ) ;
#34371=CARTESIAN_POINT ( 'NONE',  ( 0.000000000000000000, 54.21277698773675979, 55.38113227695801299 ) ) ;
#34378=AXIS2_PLACEMENT_3D ( 'NONE', #7114, #10557, #6399 ) ;
#34379=CARTESIAN_POINT ( 'NONE',  ( 10.00000000000000000, -36.73666225445940370, 65.58780272294062286 ) ) ;
#34381=ORIENTED_EDGE ( 'NONE', *, *, #13097, .F. ) ;
#34387=DIRECTION ( 'NONE',  ( -1.000000000000000000, -0.000000000000000000, -0.000000000000000000 ) ) ;
#34393=CARTESIAN_POINT ( 'NONE',  ( 10.00000000000000000, 44.88180994100468268, -63.18004540532978552 ) ) ;
#34401=CARTESIAN_POINT ( 'NONE',  ( 0.000000000000000000, 0.000000000000000000, 0.000000000000000000 ) ) ;
#34404=ADVANCED_FACE ( 'NONE', ( #24246 ), #47484, .T. ) ;
#34407=EDGE_CURVE ( 'NONE', #46450, #2889, #43346, .T. ) ;
#34409=CARTESIAN_POINT ( 'NONE',  ( 0.000000000000000000, -63.97538442413463855, 51.29473840253199768 ) ) ;
#34414=AXIS2_PLACEMENT_3D ( 'NONE', #1235, #4892, #8796 ) ;
#34415=SURFACE_STYLE_FILL_AREA ( #23412 ) ;
#34421=VERTEX_POINT ( 'NONE', #20322 ) ;
#34424=ORIENTED_EDGE ( 'NONE', *, *, #47846, .F. ) ;
#34425=ORIENTED_EDGE ( 'NONE', *, *, #25776, .T. ) ;
#34434=DIRECTION ( 'NONE',  ( -1.000000000000000000, 0.000000000000000000, 0.000000000000000000 ) ) ;
#34437=FACE_OUTER_BOUND ( 'NONE', #38802, .T. ) ;
#34441=ORIENTED_EDGE ( 'NONE', *, *, #7233, .F. ) ;
#34443=CARTESIAN_POINT ( 'NONE',  ( 10.00000000000000000, 0.000000000000000000, 0.000000000000000000 ) ) ;
#34445=CIRCLE ( 'NONE', #25859, 31.99999999999999289 ) ;
#34447=ORIENTED_EDGE ( 'NONE', *, *, #44024, .T. ) ;
#34451=AXIS2_PLACEMENT_3D ( 'NONE', #4858, #1436, #16134 ) ;
#34452=ORIENTED_EDGE ( 'NONE', *, *, #39558, .T. ) ;
#34454=DIRECTION ( 'NONE',  ( 0.000000000000000000, 0.000000000000000000, 1.000000000000000000 ) ) ;
#34455=EDGE_CURVE ( 'NONE', #919, #9826, #48202, .T. ) ;
#34456=DIRECTION ( 'NONE',  ( -1.000000000000000000, -0.000000000000000000, -0.000000000000000000 ) ) ;
#34463=CARTESIAN_POINT ( 'NONE',  ( 0.000000000000000000, -79.10210256391383155, 21.60688246758557796 ) ) ;
#34465=DIRECTION ( 'NONE',  ( 0.000000000000000000, 0.000000000000000000, -1.000000000000000000 ) ) ;
#34467=EDGE_CURVE ( 'NONE', #9308, #20063, #7543, .T. ) ;
#34469=LINE ( 'NONE', #217, #21605 ) ;
#34482=AXIS2_PLACEMENT_3D ( 'NONE', #31846, #13224, #13706 ) ;
#34483=CIRCLE ( 'NONE', #20403, 31.99999999999999645 ) ;
#34490=CARTESIAN_POINT ( 'NONE',  ( 10.00000000000000000, -17.28742895386139722, 75.54627589209937355 ) ) ;
#34506=VERTEX_POINT ( 'NONE', #48439 ) ;
#34507=AXIS2_PLACEMENT_3D ( 'NONE', #30513, #15107, #48385 ) ;
#34510=EDGE_LOOP ( 'NONE', ( #37391, #12992, #39523, #17946 ) ) ;
#34521=DIRECTION ( 'NONE',  ( -1.000000000000000000, -0.000000000000000000, -0.000000000000000000 ) ) ;
#34531=CARTESIAN_POINT ( 'NONE',  ( 0.000000000000000000, 73.72996012237440766, 14.67089635893739619 ) ) ;
#34532=EDGE_CURVE ( 'NONE', #15854, #12049, #514, .T. ) ;
#34535=EDGE_CURVE ( 'NONE', #27549, #38979, #34151, .T. ) ;
#34537=DIRECTION ( 'NONE',  ( -1.000000000000000000, -0.000000000000000000, -0.000000000000000000 ) ) ;
#34539=CARTESIAN_POINT ( 'NONE',  ( 10.00000000000000000, 0.000000000000000000, 0.000000000000000000 ) ) ;
#34544=FACE_OUTER_BOUND ( 'NONE', #41869, .T. ) ;
#34549=VERTEX_POINT ( 'NONE', #216 ) ;
#34551=ADVANCED_FACE ( 'NONE', ( #44296 ), #29113, .T. ) ;
#34552=CARTESIAN_POINT ( 'NONE',  ( 0.000000000000000000, -77.16300072079681627, 27.74655509720641078 ) ) ;
#34553=DIRECTION ( 'NONE',  ( 0.000000000000000000, 0.000000000000000000, 1.000000000000000000 ) ) ;
#34556=AXIS2_PLACEMENT_3D ( 'NONE', #24149, #32223, #20463 ) ;
#34568=ORIENTED_EDGE ( 'NONE', *, *, #2418, .F. ) ;
#34570=VERTEX_POINT ( 'NONE', #44533 ) ;
#34574=ORIENTED_EDGE ( 'NONE', *, *, #2769, .F. ) ;
#34580=CARTESIAN_POINT ( 'NONE',  ( 10.00000000000000000, 77.49459641780886443, 0.8261519478433866359 ) ) ;
#34581=AXIS2_PLACEMENT_3D ( 'NONE', #23583, #5720, #20642 ) ;
#34586=LINE ( 'NONE', #5471, #15780 ) ;
#34592=AXIS2_PLACEMENT_3D ( 'NONE', #4742, #32149, #43158 ) ;
#34598=EDGE_LOOP ( 'NONE', ( #21871, #16251, #46312, #26940 ) ) ;
#34599=CARTESIAN_POINT ( 'NONE',  ( 10.00000000000000000, -2.956366410620109519, -75.11725578898472122 ) ) ;
#34604=AXIS2_PLACEMENT_3D ( 'NONE', #38238, #30649, #38969 ) ;
#34605=ORIENTED_EDGE ( 'NONE', *, *, #505, .T. ) ;
#34606=VERTEX_POINT ( 'NONE', #21542 ) ;
#34611=AXIS2_PLACEMENT_3D ( 'NONE', #1373, #1857, #12392 ) ;
#34614=EDGE_CURVE ( 'NONE', #44761, #12437, #19302, .T. ) ;
#34625=VECTOR ( 'NONE', #31187, 1000.000000000000000 ) ;
#34627=VERTEX_POINT ( 'NONE', #23231 ) ;
#34629=ORIENTED_EDGE ( 'NONE', *, *, #39415, .T. ) ;
#34637=AXIS2_PLACEMENT_3D ( 'NONE', #29690, #6227, #44146 ) ;
#34639=EDGE_CURVE ( 'NONE', #9519, #6523, #2129, .T. ) ;
#34640=EDGE_CURVE ( 'NONE', #38187, #45729, #38163, .T. ) ;
#34641=CYLINDRICAL_SURFACE ( 'NONE', #44560, 31.99999999999999289 ) ;
#34643=CARTESIAN_POINT ( 'NONE',  ( 10.00000000000000000, 0.000000000000000000, 0.000000000000000000 ) ) ;
#34647=DIRECTION ( 'NONE',  ( -1.000000000000000000, 0.000000000000000000, 0.000000000000000000 ) ) ;
#34651=CARTESIAN_POINT ( 'NONE',  ( 0.000000000000000000, 71.27951684758026829, 30.41916302227139113 ) ) ;
#34655=EDGE_CURVE ( 'NONE', #14299, #32923, #20036, .T. ) ;
#34659=VERTEX_POINT ( 'NONE', #30571 ) ;
#34660=VECTOR ( 'NONE', #44893, 1000.000000000000000 ) ;
#34661=CIRCLE ( 'NONE', #35468, 31.99999999999998579 ) ;
#34662=CIRCLE ( 'NONE', #24507, 32.00000000000000000 ) ;
#34664=DIRECTION ( 'NONE',  ( 0.000000000000000000, 0.000000000000000000, -1.000000000000000000 ) ) ;
#34672=AXIS2_PLACEMENT_3D ( 'NONE', #17651, #9830, #10561 ) ;
#34676=ADVANCED_FACE ( 'NONE', ( #45492 ), #1201, .T. ) ;
#34684=AXIS2_PLACEMENT_3D ( 'NONE', #26236, #12281, #41178 ) ;
#34686=ORIENTED_EDGE ( 'NONE', *, *, #720, .F. ) ;
#34699=CARTESIAN_POINT ( 'NONE',  ( 10.00000000000000000, -70.53064760720336324, 26.01480285779810231 ) ) ;
#34703=DIRECTION ( 'NONE',  ( 0.000000000000000000, 0.000000000000000000, 1.000000000000000000 ) ) ;
#34705=CIRCLE ( 'NONE', #19085, 82.00000000000000000 ) ;
#34711=VECTOR ( 'NONE', #24931, 1000.000000000000000 ) ;
#34712=CARTESIAN_POINT ( 'NONE',  ( -10.00000000000000000, 0.000000000000000000, 0.000000000000000000 ) ) ;
#34718=DIRECTION ( 'NONE',  ( -1.000000000000000000, 0.000000000000000000, 0.000000000000000000 ) ) ;
#34721=CARTESIAN_POINT ( 'NONE',  ( 0.000000000000000000, -30.41916302227060598, -71.27951684758059514 ) ) ;
#34726=EDGE_CURVE ( 'NONE', #14894, #32964, #29476, .T. ) ;
#34728=CIRCLE ( 'NONE', #32409, 82.00000000000000000 ) ;
#34729=ORIENTED_EDGE ( 'NONE', *, *, #3350, .T. ) ;
#34730=CIRCLE ( 'NONE', #15228, 31.99999999999999645 ) ;
#34740=CARTESIAN_POINT ( 'NONE',  ( 10.00000000000000000, -10.30890764327441822, 81.34940948281332851 ) ) ;
#34744=ORIENTED_EDGE ( 'NONE', *, *, #34271, .T. ) ;
#34746=ORIENTED_EDGE ( 'NONE', *, *, #43121, .T. ) ;
#34748=ADVANCED_FACE ( 'NONE', ( #8303 ), #4625, .T. ) ;
#34749=DIRECTION ( 'NONE',  ( -1.000000000000000000, 0.000000000000000000, -0.000000000000000000 ) ) ;
#34751=ORIENTED_EDGE ( 'NONE', *, *, #18111, .F. ) ;
#34752=CARTESIAN_POINT ( 'NONE',  ( -10.00000000000000000, 0.000000000000000000, 0.000000000000000000 ) ) ;
#34757=CARTESIAN_POINT ( 'NONE',  ( 10.00000000000000000, -51.29473840253269401, 63.97538442413405591 ) ) ;
#34763=DIRECTION ( 'NONE',  ( -1.000000000000000000, -0.000000000000000000, -0.000000000000000000 ) ) ;
#34764=ORIENTED_EDGE ( 'NONE', *, *, #6268, .T. ) ;
#34766=ORIENTED_EDGE ( 'NONE', *, *, #43755, .T. ) ;
#34771=ORIENTED_EDGE ( 'NONE', *, *, #25776, .F. ) ;
#34778=EDGE_CURVE ( 'NONE', #24346, #46450, #40421, .T. ) ;
#34783=CARTESIAN_POINT ( 'NONE',  ( 0.000000000000000000, 12.93880638057313703, 76.41127070299276625 ) ) ;
#34785=DIRECTION ( 'NONE',  ( -1.000000000000000000, -0.000000000000000000, 0.000000000000000000 ) ) ;
#34787=CARTESIAN_POINT ( 'NONE',  ( 0.000000000000000000, -75.11764819372149304, 2.946379043146075905 ) ) ;
#34792=DIRECTION ( 'NONE',  ( 0.000000000000000000, 0.8910065241883691201, -0.4539904997395446951 ) ) ;
#34794=DIRECTION ( 'NONE',  ( 1.000000000000000000, -0.000000000000000000, -0.000000000000000000 ) ) ;
#34797=DIRECTION ( 'NONE',  ( 0.000000000000000000, 0.000000000000000000, 1.000000000000000000 ) ) ;
#34801=CIRCLE ( 'NONE', #30798, 31.99999999999998579 ) ;
#34802=CARTESIAN_POINT ( 'NONE',  ( 5.000000000000000000, -21.60688246758642705, 79.10210256391360417 ) ) ;
#34807=CIRCLE ( 'NONE', #41088, 31.99999999999999645 ) ;
#34825=ORIENTED_EDGE ( 'NONE', *, *, #21770, .T. ) ;
#34826=CARTESIAN_POINT ( 'NONE',  ( 10.00000000000000000, 14.67089635893819377, -73.72996012237423713 ) ) ;
#34830=EDGE_LOOP ( 'NONE', ( #24414, #25138, #43613, #19377 ) ) ;
#34832=AXIS2_PLACEMENT_3D ( 'NONE', #12614, #27306, #31722 ) ;
#34833=LINE ( 'NONE', #43152, #33654 ) ;
#34841=FACE_OUTER_BOUND ( 'NONE', #26097, .T. ) ;
#34847=DIRECTION ( 'NONE',  ( -1.000000000000000000, 0.000000000000000000, -0.000000000000000000 ) ) ;
#34854=EDGE_CURVE ( 'NONE', #15510, #18371, #35208, .T. ) ;
#34856=EDGE_CURVE ( 'NONE', #46126, #42000, #39626, .T. ) ;
#34862=CIRCLE ( 'NONE', #23944, 77.49900000000000944 ) ;
#34863=ORIENTED_EDGE ( 'NONE', *, *, #48180, .T. ) ;
#34874=DIRECTION ( 'NONE',  ( 0.000000000000000000, 0.8090169943749446757, 0.5877852522924769119 ) ) ;
#34878=LINE ( 'NONE', #16522, #45233 ) ;
#34887=AXIS2_PLACEMENT_3D ( 'NONE', #33511, #48207, #11008 ) ;
#34890=DIRECTION ( 'NONE',  ( 0.000000000000000000, 0.000000000000000000, 1.000000000000000000 ) ) ;
#34892=DIRECTION ( 'NONE',  ( -1.000000000000000000, -0.000000000000000000, -0.000000000000000000 ) ) ;
#34897=FACE_OUTER_BOUND ( 'NONE', #3368, .T. ) ;
#34914=ORIENTED_EDGE ( 'NONE', *, *, #46531, .T. ) ;
#34919=CARTESIAN_POINT ( 'NONE',  ( 10.00000000000000000, 75.54627589209970040, -17.28742895386005785 ) ) ;
#34921=ORIENTED_EDGE ( 'NONE', *, *, #8252, .T. ) ;
#34927=EDGE_CURVE ( 'NONE', #22527, #4758, #44719, .T. ) ;
#34928=ORIENTED_EDGE ( 'NONE', *, *, #4588, .T. ) ;
#34930=CARTESIAN_POINT ( 'NONE',  ( 5.000000000000002665, 71.87247863392471459, -39.47590169984770370 ) ) ;
#34931=CYLINDRICAL_SURFACE ( 'NONE', #5013, 12.50000000000000000 ) ;
#34933=EDGE_LOOP ( 'NONE', ( #13168, #23471, #24096, #28705 ) ) ;
#34934=DIRECTION ( 'NONE',  ( -1.000000000000000000, 0.000000000000000000, 0.000000000000000000 ) ) ;
#34945=DIRECTION ( 'NONE',  ( 0.000000000000000000, 0.000000000000000000, 1.000000000000000000 ) ) ;
#34949=CARTESIAN_POINT ( 'NONE',  ( 10.00000000000000000, 21.60688246758695641, -79.10210256391344785 ) ) ;
#34950=ORIENTED_EDGE ( 'NONE', *, *, #12065, .F. ) ;
#34951=ORIENTED_EDGE ( 'NONE', *, *, #19029, .T. ) ;
#34953=CYLINDRICAL_SURFACE ( 'NONE', #19629, 31.99999999999999289 ) ;
#34959=AXIS2_PLACEMENT_3D ( 'NONE', #27334, #30517, #19256 ) ;
#34961=CARTESIAN_POINT ( 'NONE',  ( -10.00000000000000000, 0.000000000000000000, 0.000000000000000000 ) ) ;
#34965=CARTESIAN_POINT ( 'NONE',  ( 5.000000000000000000, 55.16347631943131802, -60.67117009219075641 ) ) ;
#34967=CIRCLE ( 'NONE', #13872, 31.99999999999998934 ) ;
#34968=DIRECTION ( 'NONE',  ( -1.000000000000000000, -0.000000000000000000, -0.000000000000000000 ) ) ;
#34982=EDGE_CURVE ( 'NONE', #26337, #35099, #21680, .T. ) ;
#34984=ORIENTED_EDGE ( 'NONE', *, *, #7066, .T. ) ;
#34986=EDGE_CURVE ( 'NONE', #39534, #31305, #36533, .T. ) ;
#34987=DIRECTION ( 'NONE',  ( 0.000000000000000000, 0.000000000000000000, 1.000000000000000000 ) ) ;
#34988=VERTEX_POINT ( 'NONE', #6555 ) ;
#34995=CARTESIAN_POINT ( 'NONE',  ( 10.00000000000000000, -70.53064760720336324, 26.01480285779810231 ) ) ;
#35002=DIRECTION ( 'NONE',  ( -1.000000000000000000, -0.000000000000000000, -0.000000000000000000 ) ) ;
#35005=ORIENTED_EDGE ( 'NONE', *, *, #16423, .F. ) ;
#35006=AXIS2_PLACEMENT_3D ( 'NONE', #36864, #18262, #44459 ) ;
#35009=EDGE_LOOP ( 'NONE', ( #2515, #3623, #9780, #28029 ) ) ;
#35012=ORIENTED_EDGE ( 'NONE', *, *, #31642, .F. ) ;
#35015=DIRECTION ( 'NONE',  ( 0.000000000000000000, -0.2334453638559125521, 0.9723699203976750027 ) ) ;
#35018=CARTESIAN_POINT ( 'NONE',  ( 0.000000000000000000, 77.19088730480532945, -6.903761155836913410 ) ) ;
#35024=CARTESIAN_POINT ( 'NONE',  ( 0.000000000000000000, -72.35160999960801576, -20.41045688087902121 ) ) ;
#35025=EDGE_CURVE ( 'NONE', #44331, #42385, #11524, .T. ) ;
#35033=VECTOR ( 'NONE', #18732, 1000.000000000000000 ) ;
#35035=ORIENTED_EDGE ( 'NONE', *, *, #39198, .T. ) ;
#35040=ADVANCED_FACE ( 'NONE', ( #25629 ), #657, .T. ) ;
#35059=CIRCLE ( 'NONE', #47560, 82.00000000000000000 ) ;
#35063=DIRECTION ( 'NONE',  ( 1.000000000000000000, 0.000000000000000000, 0.000000000000000000 ) ) ;
#35072=DIRECTION ( 'NONE',  ( 0.000000000000000000, 0.000000000000000000, 1.000000000000000000 ) ) ;
#35077=CYLINDRICAL_SURFACE ( 'NONE', #2562, 31.99999999999999289 ) ;
#35078=DIRECTION ( 'NONE',  ( 0.000000000000000000, 0.000000000000000000, -1.000000000000000000 ) ) ;
#35087=DIRECTION ( 'NONE',  ( 1.000000000000000000, 0.000000000000000000, 0.000000000000000000 ) ) ;
#35090=ADVANCED_FACE ( 'NONE', ( #4349 ), #44972, .T. ) ;
#35092=VECTOR ( 'NONE', #43773, 1000.000000000000000 ) ;
#35094=EDGE_CURVE ( 'NONE', #8812, #13864, #9172, .T. ) ;
#35099=VERTEX_POINT ( 'NONE', #38594 ) ;
#35103=DIRECTION ( 'NONE',  ( 0.000000000000000000, -0.9723699203976789995, 0.2334453638558956767 ) ) ;
#35104=DIRECTION ( 'NONE',  ( 0.000000000000000000, 0.000000000000000000, 1.000000000000000000 ) ) ;
#35110=EDGE_LOOP ( 'NONE', ( #23611, #23430, #16387, #39219 ) ) ;
#35111=DIRECTION ( 'NONE',  ( -1.000000000000000000, 0.000000000000000000, 0.000000000000000000 ) ) ;
#35112=CYLINDRICAL_SURFACE ( 'NONE', #34061, 77.49899999999999523 ) ;
#35117=CIRCLE ( 'NONE', #30454, 31.99999999999999289 ) ;
#35123=LINE ( 'NONE', #32604, #1758 ) ;
#35125=CARTESIAN_POINT ( 'NONE',  ( 10.00000000000000000, -77.19088730480518734, -6.903761155838607166 ) ) ;
#35134=CIRCLE ( 'NONE', #32048, 77.49899999999999523 ) ;
#35142=EDGE_CURVE ( 'NONE', #4911, #6805, #26843, .T. ) ;
#35151=DIRECTION ( 'NONE',  ( 1.000000000000000000, 0.000000000000000000, 0.000000000000000000 ) ) ;
#35153=AXIS2_PLACEMENT_3D ( 'NONE', #47248, #7326, #44531 ) ;
#35167=ORIENTED_EDGE ( 'NONE', *, *, #24862, .F. ) ;
#35168=CARTESIAN_POINT ( 'NONE',  ( 10.00000000000000000, -35.91791733033525702, 68.67312586194982771 ) ) ;
#35174=ORIENTED_EDGE ( 'NONE', *, *, #10407, .T. ) ;
#35177=ORIENTED_EDGE ( 'NONE', *, *, #31252, .T. ) ;
#35180=ADVANCED_FACE ( 'NONE', ( #12180 ), #42028, .T. ) ;
#35183=CARTESIAN_POINT ( 'NONE',  ( 10.00000000000000000, -76.66974797899830207, -11.30684508768422170 ) ) ;
#35184=DIRECTION ( 'NONE',  ( 0.000000000000000000, -0.07845909572785220165, 0.9969173337331274087 ) ) ;
#35185=ADVANCED_FACE ( 'NONE', ( #36536 ), #42752, .T. ) ;
#35188=DIRECTION ( 'NONE',  ( 0.000000000000000000, 0.000000000000000000, 1.000000000000000000 ) ) ;
#35192=CIRCLE ( 'NONE', #14093, 31.99999999999998224 ) ;
#35198=DIRECTION ( 'NONE',  ( -1.000000000000000000, -0.000000000000000000, -0.000000000000000000 ) ) ;
#35199=CARTESIAN_POINT ( 'NONE',  ( 10.00000000000000000, 74.65491531819105830, 8.830959090343693418 ) ) ;
#35201=FACE_OUTER_BOUND ( 'NONE', #21763, .T. ) ;
#35202=EDGE_CURVE ( 'NONE', #32964, #13148, #28944, .T. ) ;
#35205=EDGE_CURVE ( 'NONE', #708, #21020, #10005, .T. ) ;
#35208=LINE ( 'NONE', #36163, #28679 ) ;
#35210=CIRCLE ( 'NONE', #30529, 82.00000000000000000 ) ;
#35219=ORIENTED_EDGE ( 'NONE', *, *, #1776, .T. ) ;
#35220=VECTOR ( 'NONE', #38273, 1000.000000000000000 ) ;
#35222=CARTESIAN_POINT ( 'NONE',  ( 10.00000000000000000, -55.19960302592029677, -51.03279382321147750 ) ) ;
#35223=VECTOR ( 'NONE', #24548, 1000.000000000000000 ) ;
#35232=ORIENTED_EDGE ( 'NONE', *, *, #28789, .F. ) ;
#35241=ADVANCED_FACE ( 'NONE', ( #23901 ), #10605, .T. ) ;
#35247=DIRECTION ( 'NONE',  ( 0.000000000000000000, 0.000000000000000000, 1.000000000000000000 ) ) ;
#35254=DIRECTION ( 'NONE',  ( 0.000000000000000000, 0.000000000000000000, -1.000000000000000000 ) ) ;
#35258=CARTESIAN_POINT ( 'NONE',  ( 0.000000000000000000, 55.19960302592066625, 51.03279382321107249 ) ) ;
#35278=CARTESIAN_POINT ( 'NONE',  ( 10.00000000000000000, -75.11764819372145041, -2.946379043147127064 ) ) ;
#35290=VERTEX_POINT ( 'NONE', #39306 ) ;
#35292=AXIS2_PLACEMENT_3D ( 'NONE', #37591, #18509, #26341 ) ;
#35295=VECTOR ( 'NONE', #14306, 1000.000000000000000 ) ;
#35299=CARTESIAN_POINT ( 'NONE',  ( 0.000000000000000000, 51.02545421589402252, -55.20638768913705263 ) ) ;
#35305=CARTESIAN_POINT ( 'NONE',  ( 10.00000000000000000, 0.000000000000000000, 0.000000000000000000 ) ) ;
#35308=ORIENTED_EDGE ( 'NONE', *, *, #19235, .T. ) ;
#35315=DIRECTION ( 'NONE',  ( 0.000000000000000000, 1.000000000000000000, 0.000000000000000000 ) ) ;
#35318=CARTESIAN_POINT ( 'NONE',  ( 0.000000000000000000, -76.66974797899828786, -11.30684508768421992 ) ) ;
#35322=DIRECTION ( 'NONE',  ( -1.000000000000000000, 0.000000000000000000, 0.000000000000000000 ) ) ;
#35324=EDGE_CURVE ( 'NONE', #1645, #30814, #6923, .T. ) ;
#35327=CARTESIAN_POINT ( 'NONE',  ( 10.00000000000000000, -79.10210256391353312, -21.60688246758667574 ) ) ;
#35332=ORIENTED_EDGE ( 'NONE', *, *, #17739, .F. ) ;
#35336=VECTOR ( 'NONE', #24719, 1000.000000000000000 ) ;
#35348=DIRECTION ( 'NONE',  ( 0.000000000000000000, -0.4539904997395541875, 0.8910065241883642351 ) ) ;
#35351=DIRECTION ( 'NONE',  ( 0.000000000000000000, 0.000000000000000000, 1.000000000000000000 ) ) ;
#35352=ORIENTED_EDGE ( 'NONE', *, *, #27913, .T. ) ;
#35357=CIRCLE ( 'NONE', #42428, 31.99999999999999289 ) ;
#35369=CARTESIAN_POINT ( 'NONE',  ( 0.000000000000000000, -71.87247863392386193, -39.47590169984923136 ) ) ;
#35378=ORIENTED_EDGE ( 'NONE', *, *, #9895, .F. ) ;
#35379=DIRECTION ( 'NONE',  ( -1.000000000000000000, 0.000000000000000000, -0.000000000000000000 ) ) ;
#35380=AXIS2_PLACEMENT_3D ( 'NONE', #3296, #44190, #33415 ) ;
#35384=DIRECTION ( 'NONE',  ( 0.000000000000000000, 0.000000000000000000, 1.000000000000000000 ) ) ;
#35389=CIRCLE ( 'NONE', #42420, 77.49899999999999523 ) ;
#35401=ORIENTED_EDGE ( 'NONE', *, *, #47834, .T. ) ;
#35404=AXIS2_PLACEMENT_3D ( 'NONE', #10098, #20151, #25019 ) ;
#35407=AXIS2_PLACEMENT_3D ( 'NONE', #30708, #45160, #30470 ) ;
#35409=ORIENTED_EDGE ( 'NONE', *, *, #40511, .F. ) ;
#35415=VERTEX_POINT ( 'NONE', #21839 ) ;
#35417=ORIENTED_EDGE ( 'NONE', *, *, #29218, .T. ) ;
#35428=AXIS2_PLACEMENT_3D ( 'NONE', #25454, #14210, #24505 ) ;
#35436=CARTESIAN_POINT ( 'NONE',  ( 0.000000000000000000, -76.41127070299262414, -12.93880638057396304 ) ) ;
#35441=DIRECTION ( 'NONE',  ( 0.000000000000000000, 0.000000000000000000, 1.000000000000000000 ) ) ;
#35446=CARTESIAN_POINT ( 'NONE',  ( 0.000000000000000000, -26.01480285779885904, 70.53064760720306481 ) ) ;
#35447=CARTESIAN_POINT ( 'NONE',  ( 5.000000000000002665, 74.18225833017888249, 34.94270380257665209 ) ) ;
#35449=VERTEX_POINT ( 'NONE', #36766 ) ;
#35460=EDGE_CURVE ( 'NONE', #5074, #17824, #7408, .T. ) ;
#35463=CYLINDRICAL_SURFACE ( 'NONE', #5844, 31.99999999999999289 ) ;
#35468=AXIS2_PLACEMENT_3D ( 'NONE', #18983, #4074, #22907 ) ;
#35473=VERTEX_POINT ( 'NONE', #3729 ) ;
#35481=VECTOR ( 'NONE', #33100, 1000.000000000000000 ) ;
#35498=ORIENTED_EDGE ( 'NONE', *, *, #2414, .F. ) ;
#35505=CYLINDRICAL_SURFACE ( 'NONE', #38610, 82.00000000000000000 ) ;
#35510=FACE_OUTER_BOUND ( 'NONE', #39334, .T. ) ;
#35514=DIRECTION ( 'NONE',  ( -1.000000000000000000, -0.000000000000000000, 0.000000000000000000 ) ) ;
#35522=ORIENTED_EDGE ( 'NONE', *, *, #30008, .F. ) ;
#35524=CIRCLE ( 'NONE', #12090, 77.49899999999999523 ) ;
#35527=CYLINDRICAL_SURFACE ( 'NONE', #14289, 31.99999999999999289 ) ;
#35529=EDGE_CURVE ( 'NONE', #21026, #13144, #29546, .T. ) ;
#35533=AXIS2_PLACEMENT_3D ( 'NONE', #48378, #4561, #14856 ) ;
#35537=DIRECTION ( 'NONE',  ( 0.000000000000000000, 0.000000000000000000, 1.000000000000000000 ) ) ;
#35554=CARTESIAN_POINT ( 'NONE',  ( 0.000000000000000000, -59.03961581697432592, 46.53671651293927880 ) ) ;
#35558=VECTOR ( 'NONE', #42950, 1000.000000000000000 ) ;
#35573=DIRECTION ( 'NONE',  ( 0.000000000000000000, 0.000000000000000000, 1.000000000000000000 ) ) ;
#35574=CYLINDRICAL_SURFACE ( 'NONE', #980, 31.99999999999998579 ) ;
#35576=CARTESIAN_POINT ( 'NONE',  ( 10.00000000000000000, -74.74816331893404708, -33.71516098798818462 ) ) ;
#35581=ORIENTED_EDGE ( 'NONE', *, *, #9828, .F. ) ;
#35583=AXIS2_PLACEMENT_3D ( 'NONE', #21107, #31437, #43638 ) ;
#35587=AXIS2_PLACEMENT_3D ( 'NONE', #16248, #11374, #22609 ) ;
#35590=EDGE_CURVE ( 'NONE', #18992, #25663, #45205, .T. ) ;
#35595=CARTESIAN_POINT ( 'NONE',  ( 10.00000000000000000, 0.000000000000000000, 0.000000000000000000 ) ) ;
#35602=LINE ( 'NONE', #39030, #8091 ) ;
#35603=EDGE_CURVE ( 'NONE', #13811, #17121, #39689, .T. ) ;
#35607=DIRECTION ( 'NONE',  ( -1.000000000000000000, -0.000000000000000000, -0.000000000000000000 ) ) ;
#35608=CIRCLE ( 'NONE', #24678, 77.49900000000000944 ) ;
#35611=DIRECTION ( 'NONE',  ( -1.000000000000000000, -0.000000000000000000, -0.000000000000000000 ) ) ;
#35613=DIRECTION ( 'NONE',  ( -1.000000000000000000, -0.000000000000000000, -0.000000000000000000 ) ) ;
#35617=EDGE_LOOP ( 'NONE', ( #6151, #37961, #34729, #27379 ) ) ;
#35618=DIRECTION ( 'NONE',  ( 0.000000000000000000, 0.000000000000000000, 1.000000000000000000 ) ) ;
#35619=ORIENTED_EDGE ( 'NONE', *, *, #25172, .F. ) ;
#35624=DIRECTION ( 'NONE',  ( 0.000000000000000000, 0.000000000000000000, 1.000000000000000000 ) ) ;
#35630=FACE_OUTER_BOUND ( 'NONE', #8576, .T. ) ;
#35642=AXIS2_PLACEMENT_3D ( 'NONE', #18482, #4523, #15307 ) ;
#35644=EDGE_CURVE ( 'NONE', #41084, #23915, #47489, .T. ) ;
#35648=CIRCLE ( 'NONE', #20795, 82.00000000000000000 ) ;
#35649=CARTESIAN_POINT ( 'NONE',  ( -10.00000000000000000, 0.000000000000000000, 0.000000000000000000 ) ) ;
#35650=VERTEX_POINT ( 'NONE', #28405 ) ;
#35652=ORIENTED_EDGE ( 'NONE', *, *, #29619, .F. ) ;
#35655=EDGE_CURVE ( 'NONE', #2889, #4582, #20982, .T. ) ;
#35656=EDGE_CURVE ( 'NONE', #14155, #19851, #29572, .T. ) ;
#35657=CARTESIAN_POINT ( 'NONE',  ( -10.00000000000000000, 0.000000000000000000, 0.000000000000000000 ) ) ;
#35659=ORIENTED_EDGE ( 'NONE', *, *, #8499, .F. ) ;
#35666=ORIENTED_EDGE ( 'NONE', *, *, #26877, .F. ) ;
#35668=CARTESIAN_POINT ( 'NONE',  ( 10.00000000000000000, 0.000000000000000000, 0.000000000000000000 ) ) ;
#35677=DIRECTION ( 'NONE',  ( 0.000000000000000000, 0.5224985647159440250, 0.8526401643540951758 ) ) ;
#35694=FACE_OUTER_BOUND ( 'NONE', #25707, .T. ) ;
#35700=ORIENTED_EDGE ( 'NONE', *, *, #41549, .T. ) ;
#35707=ADVANCED_FACE ( 'NONE', ( #9003 ), #16351, .T. ) ;
#35713=CIRCLE ( 'NONE', #2864, 82.00000000000000000 ) ;
#35714=CARTESIAN_POINT ( 'NONE',  ( 0.000000000000000000, 0.000000000000000000, 0.000000000000000000 ) ) ;
#35721=CIRCLE ( 'NONE', #41989, 82.00000000000000000 ) ;
#35723=ORIENTED_EDGE ( 'NONE', *, *, #45776, .F. ) ;
#35726=ORIENTED_EDGE ( 'NONE', *, *, #15487, .F. ) ;
#35728=AXIS2_PLACEMENT_3D ( 'NONE', #19529, #46482, #1687 ) ;
#35732=LINE ( 'NONE', #13937, #28243 ) ;
#35733=ORIENTED_EDGE ( 'NONE', *, *, #8783, .T. ) ;
#35736=CIRCLE ( 'NONE', #14646, 31.99999999999998934 ) ;
#35744=ADVANCED_FACE ( 'NONE', ( #8750 ), #12209, .T. ) ;
#35747=DIRECTION ( 'NONE',  ( 0.000000000000000000, 0.000000000000000000, 1.000000000000000000 ) ) ;
#35754=DIRECTION ( 'NONE',  ( -1.000000000000000000, -0.000000000000000000, 0.000000000000000000 ) ) ;
#35758=DIRECTION ( 'NONE',  ( -1.000000000000000000, -0.000000000000000000, 0.000000000000000000 ) ) ;
#35769=CARTESIAN_POINT ( 'NONE',  ( 0.000000000000000000, -73.44644590900077219, 24.73286445877675632 ) ) ;
#35771=ORIENTED_EDGE ( 'NONE', *, *, #24458, .T. ) ;
#35772=AXIS2_PLACEMENT_3D ( 'NONE', #3971, #37734, #29664 ) ;
#35779=AXIS2_PLACEMENT_3D ( 'NONE', #16021, #8426, #20578 ) ;
#35783=CARTESIAN_POINT ( 'NONE',  ( 10.00000000000000000, 36.72794159290241822, 65.59268652807223532 ) ) ;
#35784=ORIENTED_EDGE ( 'NONE', *, *, #37128, .T. ) ;
#35787=DIRECTION ( 'NONE',  ( -1.000000000000000000, -0.000000000000000000, 0.000000000000000000 ) ) ;
#35794=CYLINDRICAL_SURFACE ( 'NONE', #2943, 82.00000000000000000 ) ;
#35800=CARTESIAN_POINT ( 'NONE',  ( 10.00000000000000000, 8.840884882376133902, -74.65374052328640175 ) ) ;
#35801=CARTESIAN_POINT ( 'NONE',  ( 10.00000000000000000, 2.543863470249530856, -81.96053171279901051 ) ) ;
#35803=ORIENTED_EDGE ( 'NONE', *, *, #41648, .F. ) ;
#35805=CIRCLE ( 'NONE', #12367, 82.00000000000000000 ) ;
#35820=EDGE_CURVE ( 'NONE', #1310, #45334, #28093, .T. ) ;
#35822=ORIENTED_EDGE ( 'NONE', *, *, #2062, .F. ) ;
#35824=ORIENTED_EDGE ( 'NONE', *, *, #4572, .F. ) ;
#35826=DIRECTION ( 'NONE',  ( -1.000000000000000000, -0.000000000000000000, 0.000000000000000000 ) ) ;
#35827=ORIENTED_EDGE ( 'NONE', *, *, #6394, .T. ) ;
#35830=AXIS2_PLACEMENT_3D ( 'NONE', #34299, #4693, #767 ) ;
#35841=CYLINDRICAL_SURFACE ( 'NONE', #10826, 77.49899999999999523 ) ;
#35846=EDGE_LOOP ( 'NONE', ( #19676, #7141, #23553, #34928 ) ) ;
#35854=DIRECTION ( 'NONE',  ( -1.000000000000000000, 0.000000000000000000, -0.000000000000000000 ) ) ;
#35883=CARTESIAN_POINT ( 'NONE',  ( 0.000000000000000000, 0.000000000000000000, 0.000000000000000000 ) ) ;
#35886=AXIS2_PLACEMENT_3D ( 'NONE', #29, #37249, #2749 ) ;
#35887=VECTOR ( 'NONE', #2645, 1000.000000000000000 ) ;
#35893=ORIENTED_EDGE ( 'NONE', *, *, #29169, .T. ) ;
#35901=DIRECTION ( 'NONE',  ( 0.000000000000000000, 0.000000000000000000, 1.000000000000000000 ) ) ;
#35902=ORIENTED_EDGE ( 'NONE', *, *, #8542, .T. ) ;
#35907=DIRECTION ( 'NONE',  ( -1.000000000000000000, 0.000000000000000000, 0.000000000000000000 ) ) ;
#35909=EDGE_CURVE ( 'NONE', #17390, #39882, #13987, .T. ) ;
#35910=EDGE_CURVE ( 'NONE', #16057, #29685, #6071, .T. ) ;
#35911=DIRECTION ( 'NONE',  ( 0.000000000000000000, 0.000000000000000000, 1.000000000000000000 ) ) ;
#35914=ORIENTED_EDGE ( 'NONE', *, *, #5531, .F. ) ;
#35918=DIRECTION ( 'NONE',  ( 0.000000000000000000, 0.000000000000000000, 1.000000000000000000 ) ) ;
#35926=ORIENTED_EDGE ( 'NONE', *, *, #41494, .F. ) ;
#35929=CIRCLE ( 'NONE', #14831, 31.99999999999999645 ) ;
#35930=CARTESIAN_POINT ( 'NONE',  ( 10.00000000000000000, 0.000000000000000000, 0.000000000000000000 ) ) ;
#35931=EDGE_CURVE ( 'NONE', #1317, #16336, #5370, .T. ) ;
#35939=AXIS2_PLACEMENT_3D ( 'NONE', #42906, #48252, #10811 ) ;
#35950=EDGE_LOOP ( 'NONE', ( #42910, #10846, #23265, #38254 ) ) ;
#35952=AXIS2_PLACEMENT_3D ( 'NONE', #29112, #10272, #6610 ) ;
#35959=CARTESIAN_POINT ( 'NONE',  ( 0.000000000000000000, -74.65491531819111515, -8.830959090343204920 ) ) ;
#35960=CIRCLE ( 'NONE', #779, 82.00000000000000000 ) ;
#35961=DIRECTION ( 'NONE',  ( -1.000000000000000000, 0.000000000000000000, -0.000000000000000000 ) ) ;
#35970=DIRECTION ( 'NONE',  ( -1.000000000000000000, 0.000000000000000000, -0.000000000000000000 ) ) ;
#35971=ORIENTED_EDGE ( 'NONE', *, *, #48121, .F. ) ;
#35974=ADVANCED_FACE ( 'NONE', ( #23979 ), #1217, .T. ) ;
#35978=CARTESIAN_POINT ( 'NONE',  ( 0.000000000000000000, 68.55367621811205936, -44.99326035065983120 ) ) ;
#35979=LINE ( 'NONE', #24735, #47728 ) ;
#35980=CARTESIAN_POINT ( 'NONE',  ( -10.00000000000000000, 0.000000000000000000, 0.000000000000000000 ) ) ;
#35983=DIRECTION ( 'NONE',  ( -1.000000000000000000, 0.000000000000000000, 0.000000000000000000 ) ) ;
#35990=VERTEX_POINT ( 'NONE', #43054 ) ;
#35991=CIRCLE ( 'NONE', #14090, 31.99999999999999289 ) ;
#35993=CARTESIAN_POINT ( 'NONE',  ( 0.000000000000000000, 0.000000000000000000, 0.000000000000000000 ) ) ;
#35999=AXIS2_PLACEMENT_3D ( 'NONE', #19824, #34763, #31114 ) ;
#36004=VERTEX_POINT ( 'NONE', #31825 ) ;
#36012=DIRECTION ( 'NONE',  ( 0.000000000000000000, 0.000000000000000000, 1.000000000000000000 ) ) ;
#36017=CARTESIAN_POINT ( 'NONE',  ( 0.000000000000000000, -74.74816331893454446, 33.71516098798714722 ) ) ;
#36020=CARTESIAN_POINT ( 'NONE',  ( 10.00000000000000000, -65.64334221924939072, 41.19522573413710376 ) ) ;
#36021=VERTEX_POINT ( 'NONE', #13435 ) ;
#36022=DIRECTION ( 'NONE',  ( -1.000000000000000000, 0.000000000000000000, 0.000000000000000000 ) ) ;
#36024=CIRCLE ( 'NONE', #7868, 82.00000000000000000 ) ;
#36025=FACE_OUTER_BOUND ( 'NONE', #29521, .T. ) ;
#36030=AXIS2_PLACEMENT_3D ( 'NONE', #40449, #39490, #32835 ) ;
#36031=EDGE_LOOP ( 'NONE', ( #42036, #19802, #46586, #27065 ) ) ;
#36033=CARTESIAN_POINT ( 'NONE',  ( 10.00000000000000000, 0.000000000000000000, 0.000000000000000000 ) ) ;
#36034=EDGE_CURVE ( 'NONE', #11188, #6193, #4593, .T. ) ;
#36035=CARTESIAN_POINT ( 'NONE',  ( 10.00000000000000000, 36.73666225445894185, 65.58780272294090707 ) ) ;
#36039=CARTESIAN_POINT ( 'NONE',  ( 0.000000000000000000, 71.87247863392414615, 39.47590169984871267 ) ) ;
#36047=DIRECTION ( 'NONE',  ( 0.000000000000000000, 0.000000000000000000, 1.000000000000000000 ) ) ;
#36051=DIRECTION ( 'NONE',  ( 0.000000000000000000, 0.000000000000000000, 1.000000000000000000 ) ) ;
#36056=ORIENTED_EDGE ( 'NONE', *, *, #4094, .T. ) ;
#36060=AXIS2_PLACEMENT_3D ( 'NONE', #30164, #37251, #48265 ) ;
#36061=EDGE_CURVE ( 'NONE', #31833, #45052, #39386, .T. ) ;
#36064=AXIS2_PLACEMENT_3D ( 'NONE', #27863, #42782, #20249 ) ;
#36066=CYLINDRICAL_SURFACE ( 'NONE', #40137, 82.00000000000000000 ) ;
#36068=ORIENTED_EDGE ( 'NONE', *, *, #25439, .F. ) ;
#36073=EDGE_LOOP ( 'NONE', ( #29091, #7821, #30717, #23536 ) ) ;
#36075=DIRECTION ( 'NONE',  ( -1.000000000000000000, 0.000000000000000000, 0.000000000000000000 ) ) ;
#36077=CIRCLE ( 'NONE', #15750, 31.99999999999999289 ) ;
#36079=DIRECTION ( 'NONE',  ( 0.000000000000000000, 0.000000000000000000, 1.000000000000000000 ) ) ;
#36085=CARTESIAN_POINT ( 'NONE',  ( 10.00000000000000000, 73.72996012237460661, -14.67089635893632504 ) ) ;
#36088=ORIENTED_EDGE ( 'NONE', *, *, #42458, .F. ) ;
#36099=CARTESIAN_POINT ( 'NONE',  ( 0.000000000000000000, 0.000000000000000000, 0.000000000000000000 ) ) ;
#36100=CIRCLE ( 'NONE', #24357, 31.99999999999998934 ) ;
#36105=DIRECTION ( 'NONE',  ( 0.000000000000000000, 0.000000000000000000, 1.000000000000000000 ) ) ;
#36108=CARTESIAN_POINT ( 'NONE',  ( 10.00000000000000000, -74.65374052328654386, 8.840884882374837161 ) ) ;
#36110=CARTESIAN_POINT ( 'NONE',  ( 0.000000000000000000, 71.91182617369230456, -28.89263327155667938 ) ) ;
#36112=CARTESIAN_POINT ( 'NONE',  ( -10.00000000000000000, 0.000000000000000000, 0.000000000000000000 ) ) ;
#36114=VERTEX_POINT ( 'NONE', #28360 ) ;
#36117=DIRECTION ( 'NONE',  ( -1.000000000000000000, -0.000000000000000000, 0.000000000000000000 ) ) ;
#36128=DIRECTION ( 'NONE',  ( -1.000000000000000000, 0.000000000000000000, 0.000000000000000000 ) ) ;
#36133=ORIENTED_EDGE ( 'NONE', *, *, #31128, .F. ) ;
#36138=LINE ( 'NONE', #2596, #45387 ) ;
#36139=CARTESIAN_POINT ( 'NONE',  ( 10.00000000000000000, 55.38113227695782115, 54.21277698773695164 ) ) ;
#36141=ORIENTED_EDGE ( 'NONE', *, *, #35909, .F. ) ;
#36158=CARTESIAN_POINT ( 'NONE',  ( 10.00000000000000000, 0.000000000000000000, 0.000000000000000000 ) ) ;
#36163=CARTESIAN_POINT ( 'NONE',  ( 5.000000000000000000, 33.71516098798849015, -74.74816331893393340 ) ) ;
#36170=AXIS2_PLACEMENT_3D ( 'NONE', #27873, #1179, #13403 ) ;
#36173=ORIENTED_EDGE ( 'NONE', *, *, #15009, .F. ) ;
#36175=AXIS2_PLACEMENT_3D ( 'NONE', #38517, #23104, #4981 ) ;
#36177=CIRCLE ( 'NONE', #10403, 31.99999999999998579 ) ;
#36192=CARTESIAN_POINT ( 'NONE',  ( 10.00000000000000000, -77.32052557432845674, 5.256550761632577284 ) ) ;
#36193=VERTEX_POINT ( 'NONE', #32522 ) ;
#36196=ORIENTED_EDGE ( 'NONE', *, *, #18050, .F. ) ;
#36200=AXIS2_PLACEMENT_3D ( 'NONE', #3333, #6300, #40073 ) ;
#36203=AXIS2_PLACEMENT_3D ( 'NONE', #14384, #29315, #44243 ) ;
#36213=CARTESIAN_POINT ( 'NONE',  ( 10.00000000000000000, 27.74655509720778568, -77.16300072079631889 ) ) ;
#36216=ORIENTED_EDGE ( 'NONE', *, *, #8542, .F. ) ;
#36221=CARTESIAN_POINT ( 'NONE',  ( 0.000000000000000000, 46.53671651294032330, -59.03961581697353012 ) ) ;
#36222=AXIS2_PLACEMENT_3D ( 'NONE', #25768, #7176, #10365 ) ;
#36223=DIRECTION ( 'NONE',  ( 0.000000000000000000, 0.000000000000000000, 1.000000000000000000 ) ) ;
#36225=CARTESIAN_POINT ( 'NONE',  ( 5.000000000000000000, -71.21200624218768382, -40.65526001592689909 ) ) ;
#36227=DIRECTION ( 'NONE',  ( -1.000000000000000000, -0.000000000000000000, -0.000000000000000000 ) ) ;
#36231=DIRECTION ( 'NONE',  ( -1.000000000000000000, -0.000000000000000000, 0.000000000000000000 ) ) ;
#36235=DIRECTION ( 'NONE',  ( 0.000000000000000000, -0.8526401643540970632, 0.5224985647159409163 ) ) ;
#36236=AXIS2_PLACEMENT_3D ( 'NONE', #2321, #17241, #28525 ) ;
#36240=CARTESIAN_POINT ( 'NONE',  ( 10.00000000000000000, 66.50666863322055633, -39.78640506895536078 ) ) ;
#36242=EDGE_CURVE ( 'NONE', #18377, #44907, #40580, .T. ) ;
#36244=CIRCLE ( 'NONE', #15159, 77.49899999999999523 ) ;
#36245=AXIS2_PLACEMENT_3D ( 'NONE', #1570, #34847, #1329 ) ;
#36247=DIRECTION ( 'NONE',  ( 0.000000000000000000, 0.000000000000000000, 1.000000000000000000 ) ) ;
#36258=CARTESIAN_POINT ( 'NONE',  ( 10.00000000000000000, 0.000000000000000000, -2.500000000000000000 ) ) ;
#36259=ORIENTED_EDGE ( 'NONE', *, *, #4046, .T. ) ;
#36263=AXIS2_PLACEMENT_3D ( 'NONE', #5607, #9503, #39381 ) ;
#36265=ORIENTED_EDGE ( 'NONE', *, *, #13319, .T. ) ;
#36267=AXIS2_PLACEMENT_3D ( 'NONE', #37974, #12038, #26716 ) ;
#36268=DIRECTION ( 'NONE',  ( -1.000000000000000000, 0.000000000000000000, -0.000000000000000000 ) ) ;
#36273=DIRECTION ( 'NONE',  ( 0.000000000000000000, 0.000000000000000000, 1.000000000000000000 ) ) ;
#36280=DIRECTION ( 'NONE',  ( -1.000000000000000000, -0.000000000000000000, 0.000000000000000000 ) ) ;
#36282=CARTESIAN_POINT ( 'NONE',  ( 0.000000000000000000, -64.81221759200379040, 50.23322058963324110 ) ) ;
#36287=CARTESIAN_POINT ( 'NONE',  ( 10.00000000000000178, 0.000000000000000000, 12.50000000000000000 ) ) ;
#36289=EDGE_LOOP ( 'NONE', ( #40703, #6762, #44806, #43499 ) ) ;
#36295=DIRECTION ( 'NONE',  ( 0.000000000000000000, 0.000000000000000000, 1.000000000000000000 ) ) ;
#36306=EDGE_CURVE ( 'NONE', #28615, #10023, #26864, .T. ) ;
#36312=AXIS2_PLACEMENT_3D ( 'NONE', #5482, #24321, #1573 ) ;
#36318=AXIS2_PLACEMENT_3D ( 'NONE', #8590, #38466, #19137 ) ;
#36324=CARTESIAN_POINT ( 'NONE',  ( 0.000000000000000000, -41.19522573413780009, 65.64334221924896440 ) ) ;
#36330=CARTESIAN_POINT ( 'NONE',  ( 0.000000000000000000, -29.01471420065617224, 76.69515212746007649 ) ) ;
#36331=ORIENTED_EDGE ( 'NONE', *, *, #3087, .T. ) ;
#36334=ORIENTED_EDGE ( 'NONE', *, *, #7305, .F. ) ;
#36338=CARTESIAN_POINT ( 'NONE',  ( 10.00000000000000000, 71.27951684758069462, -30.41916302227035729 ) ) ;
#36346=ORIENTED_EDGE ( 'NONE', *, *, #33526, .T. ) ;
#36360=FACE_OUTER_BOUND ( 'NONE', #33726, .T. ) ;
#36361=AXIS2_PLACEMENT_3D ( 'NONE', #38584, #5050, #42019 ) ;
#36364=AXIS2_PLACEMENT_3D ( 'NONE', #16059, #46393, #20429 ) ;
#36369=ORIENTED_EDGE ( 'NONE', *, *, #20476, .F. ) ;
#36372=AXIS2_PLACEMENT_3D ( 'NONE', #11258, #41596, #48442 ) ;
#36374=CARTESIAN_POINT ( 'NONE',  ( 10.00000000000000000, 44.88180994100376608, 63.18004540533043922 ) ) ;
#36375=ORIENTED_EDGE ( 'NONE', *, *, #2062, .T. ) ;
#36381=EDGE_CURVE ( 'NONE', #40628, #29274, #7770, .T. ) ;
#36384=VERTEX_POINT ( 'NONE', #26138 ) ;
#36386=DIRECTION ( 'NONE',  ( 0.000000000000000000, 0.000000000000000000, 1.000000000000000000 ) ) ;
#36391=AXIS2_PLACEMENT_3D ( 'NONE', #29463, #6946, #25538 ) ;
#36392=VERTEX_POINT ( 'NONE', #39323 ) ;
#36393=EDGE_LOOP ( 'NONE', ( #6912, #1078, #45125, #18355 ) ) ;
#36395=EDGE_LOOP ( 'NONE', ( #21194, #2736, #17358, #29089 ) ) ;
#36396=DIRECTION ( 'NONE',  ( 0.000000000000000000, -0.3090169943749548898, 0.9510565162951511997 ) ) ;
#36397=FACE_OUTER_BOUND ( 'NONE', #4678, .T. ) ;
#36398=ORIENTED_EDGE ( 'NONE', *, *, #17748, .T. ) ;
#36401=ADVANCED_FACE ( 'NONE', ( #39085 ), #23421, .T. ) ;
#36407=EDGE_CURVE ( 'NONE', #40883, #38585, #5319, .T. ) ;
#36410=DIRECTION ( 'NONE',  ( -1.000000000000000000, -0.000000000000000000, 0.000000000000000000 ) ) ;
#36414=DIRECTION ( 'NONE',  ( -1.000000000000000000, -0.000000000000000000, 0.000000000000000000 ) ) ;
#36416=AXIS2_PLACEMENT_3D ( 'NONE', #12758, #39434, #42629 ) ;
#36418=LINE ( 'NONE', #25631, #8127 ) ;
#36421=AXIS2_PLACEMENT_3D ( 'NONE', #24617, #42247, #20445 ) ;
#36425=ORIENTED_EDGE ( 'NONE', *, *, #18537, .T. ) ;
#36427=AXIS2_PLACEMENT_3D ( 'NONE', #24714, #40124, #37167 ) ;
#36431=AXIS2_PLACEMENT_3D ( 'NONE', #4203, #12513, #19117 ) ;
#36440=VECTOR ( 'NONE', #36934, 1000.000000000000000 ) ;
#36448=ORIENTED_EDGE ( 'NONE', *, *, #2005, .T. ) ;
#36453=CIRCLE ( 'NONE', #2064, 31.99999999999999289 ) ;
#36456=VERTEX_POINT ( 'NONE', #31768 ) ;
#36459=VERTEX_POINT ( 'NONE', #46685 ) ;
#36460=ORIENTED_EDGE ( 'NONE', *, *, #19790, .T. ) ;
#36461=EDGE_CURVE ( 'NONE', #43803, #35290, #48400, .T. ) ;
#36464=DIRECTION ( 'NONE',  ( 0.000000000000000000, -0.9238795325112906243, 0.3826834323650804004 ) ) ;
#36468=VECTOR ( 'NONE', #10888, 1000.000000000000000 ) ;
#36471=CARTESIAN_POINT ( 'NONE',  ( 10.00000000000000000, 74.65491531819118620, 23.16904090965733332 ) ) ;
#36478=ORIENTED_EDGE ( 'NONE', *, *, #720, .T. ) ;
#36485=ORIENTED_EDGE ( 'NONE', *, *, #18901, .F. ) ;
#36487=DIRECTION ( 'NONE',  ( 0.000000000000000000, 0.000000000000000000, 1.000000000000000000 ) ) ;
#36488=DIRECTION ( 'NONE',  ( -1.000000000000000000, 0.000000000000000000, 0.000000000000000000 ) ) ;
#36499=ORIENTED_EDGE ( 'NONE', *, *, #8151, .F. ) ;
#36503=CARTESIAN_POINT ( 'NONE',  ( 10.00000000000000000, 73.44644590900094272, -24.73286445877628026 ) ) ;
#36505=CARTESIAN_POINT ( 'NONE',  ( 5.000000000000000000, 67.80270845531887858, 46.11716303203210998 ) ) ;
#36506=VERTEX_POINT ( 'NONE', #5076 ) ;
#36515=DIRECTION ( 'NONE',  ( -1.000000000000000000, 0.000000000000000000, 0.000000000000000000 ) ) ;
#36519=EDGE_CURVE ( 'NONE', #47062, #20918, #20963, .T. ) ;
#36527=EDGE_CURVE ( 'NONE', #4758, #14404, #24957, .T. ) ;
#36533=CIRCLE ( 'NONE', #30295, 82.00000000000000000 ) ;
#36536=FACE_OUTER_BOUND ( 'NONE', #24997, .T. ) ;
#36537=CARTESIAN_POINT ( 'NONE',  ( 0.000000000000000000, 72.35432306680455383, 20.40083707023012494 ) ) ;
#36543=EDGE_CURVE ( 'NONE', #7024, #29160, #37471, .T. ) ;
#36546=CARTESIAN_POINT ( 'NONE',  ( 0.000000000000000000, -55.38113227695743745, -54.21277698773734244 ) ) ;
#36548=CIRCLE ( 'NONE', #15452, 82.00000000000000000 ) ;
#36558=DIRECTION ( 'NONE',  ( -1.000000000000000000, 0.000000000000000000, -0.000000000000000000 ) ) ;
#36559=AXIS2_PLACEMENT_3D ( 'NONE', #32009, #28084, #16340 ) ;
#36566=CARTESIAN_POINT ( 'NONE',  ( 10.00000000000000000, -44.88180994100421373, 63.18004540533011948 ) ) ;
#36574=VERTEX_POINT ( 'NONE', #36374 ) ;
#36583=CARTESIAN_POINT ( 'NONE',  ( 0.000000000000000000, 75.11764819372149304, 29.05362095685338986 ) ) ;
#36589=CARTESIAN_POINT ( 'NONE',  ( 0.000000000000000000, 0.000000000000000000, 0.000000000000000000 ) ) ;
#36591=CARTESIAN_POINT ( 'NONE',  ( 10.00000000000000000, -34.94270380257693631, 74.18225833017875459 ) ) ;
#36593=ORIENTED_EDGE ( 'NONE', *, *, #23476, .T. ) ;
#36594=CYLINDRICAL_SURFACE ( 'NONE', #17584, 77.49899999999999523 ) ;
#36596=AXIS2_PLACEMENT_3D ( 'NONE', #20480, #9464, #46444 ) ;
#36599=VERTEX_POINT ( 'NONE', #32689 ) ;
#36602=VERTEX_POINT ( 'NONE', #47614 ) ;
#36606=DIRECTION ( 'NONE',  ( 0.000000000000000000, 0.000000000000000000, 1.000000000000000000 ) ) ;
#36608=ORIENTED_EDGE ( 'NONE', *, *, #7463, .T. ) ;
#36612=ORIENTED_EDGE ( 'NONE', *, *, #8493, .F. ) ;
#36616=EDGE_CURVE ( 'NONE', #47158, #18503, #32044, .T. ) ;
#36622=ORIENTED_EDGE ( 'NONE', *, *, #44583, .F. ) ;
#36623=EDGE_CURVE ( 'NONE', #29380, #24346, #2584, .T. ) ;
#36643=DIRECTION ( 'NONE',  ( 0.000000000000000000, 0.3090169943749412895, 0.9510565162951556406 ) ) ;
#36645=FACE_OUTER_BOUND ( 'NONE', #17594, .T. ) ;
#36648=DIRECTION ( 'NONE',  ( -1.000000000000000000, 0.000000000000000000, -0.000000000000000000 ) ) ;
#36653=ORIENTED_EDGE ( 'NONE', *, *, #13978, .T. ) ;
#36654=VECTOR ( 'NONE', #32054, 1000.000000000000000 ) ;
#36664=EDGE_CURVE ( 'NONE', #22222, #9352, #737, .T. ) ;
#36665=ORIENTED_EDGE ( 'NONE', *, *, #44154, .F. ) ;
#36671=DIRECTION ( 'NONE',  ( 1.000000000000000000, -0.000000000000000000, -0.000000000000000000 ) ) ;
#36677=FACE_OUTER_BOUND ( 'NONE', #44976, .T. ) ;
#36679=EDGE_CURVE ( 'NONE', #32425, #38732, #42967, .T. ) ;
#36682=CARTESIAN_POINT ( 'NONE',  ( 10.00000000000000000, 0.000000000000000000, 0.000000000000000000 ) ) ;
#36686=ORIENTED_EDGE ( 'NONE', *, *, #25464, .F. ) ;
#36691=AXIS2_PLACEMENT_3D ( 'NONE', #18717, #10907, #33651 ) ;
#36697=ADVANCED_FACE ( 'NONE', ( #11876 ), #18953, .T. ) ;
#36699=CARTESIAN_POINT ( 'NONE',  ( 0.000000000000000000, 59.03961581697399907, 46.53671651293969802 ) ) ;
#36701=DIRECTION ( 'NONE',  ( -1.000000000000000000, 0.000000000000000000, 0.000000000000000000 ) ) ;
#36705=DIRECTION ( 'NONE',  ( -1.000000000000000000, 0.000000000000000000, 0.000000000000000000 ) ) ;
#36712=ORIENTED_EDGE ( 'NONE', *, *, #9064, .T. ) ;
#36720=EDGE_CURVE ( 'NONE', #11808, #11292, #11634, .T. ) ;
#36721=ORIENTED_EDGE ( 'NONE', *, *, #34982, .T. ) ;
#36725=AXIS2_PLACEMENT_3D ( 'NONE', #16304, #5292, #46653 ) ;
#36727=AXIS2_PLACEMENT_3D ( 'NONE', #42118, #37964, #19349 ) ;
#36736=DIRECTION ( 'NONE',  ( 0.000000000000000000, 0.000000000000000000, 1.000000000000000000 ) ) ;
#36743=ORIENTED_EDGE ( 'NONE', *, *, #28280, .F. ) ;
#36746=EDGE_LOOP ( 'NONE', ( #3635, #11464, #44352, #29633 ) ) ;
#36748=CARTESIAN_POINT ( 'NONE',  ( 10.00000000000000000, 0.000000000000000000, 0.000000000000000000 ) ) ;
#36750=ORIENTED_EDGE ( 'NONE', *, *, #5543, .T. ) ;
#36753=ADVANCED_FACE ( 'NONE', ( #34139 ), #33182, .T. ) ;
#36754=CARTESIAN_POINT ( 'NONE',  ( 10.00000000000000000, 63.18004540533092239, -44.88180994100307686 ) ) ;
#36756=VERTEX_POINT ( 'NONE', #37335 ) ;
#36760=CYLINDRICAL_SURFACE ( 'NONE', #17745, 82.00000000000000000 ) ;
#36763=AXIS2_PLACEMENT_3D ( 'NONE', #7606, #22536, #37465 ) ;
#36766=CARTESIAN_POINT ( 'NONE',  ( 0.000000000000000000, 75.16055320797030959, 18.89407956138283851 ) ) ;
#36768=CIRCLE ( 'NONE', #45365, 31.99999999999999289 ) ;
#36770=ORIENTED_EDGE ( 'NONE', *, *, #28674, .F. ) ;
#36772=AXIS2_PLACEMENT_3D ( 'NONE', #36915, #3147, #33008 ) ;
#36774=CARTESIAN_POINT ( 'NONE',  ( 0.000000000000000000, 73.73191006444551476, 14.66109333815590254 ) ) ;
#36779=EDGE_CURVE ( 'NONE', #22693, #39455, #26567, .T. ) ;
#36782=EDGE_CURVE ( 'NONE', #47457, #3764, #15062, .T. ) ;
#36785=CIRCLE ( 'NONE', #4764, 31.99999999999999289 ) ;
#36787=CARTESIAN_POINT ( 'NONE',  ( 10.00000000000000000, -3.894527615418464705, 81.90746397400387480 ) ) ;
#36795=CARTESIAN_POINT ( 'NONE',  ( 0.000000000000000000, 51.03279382321166224, -55.19960302592011914 ) ) ;
#36798=AXIS2_PLACEMENT_3D ( 'NONE', #46047, #31123, #12515 ) ;
#36804=ORIENTED_EDGE ( 'NONE', *, *, #11746, .T. ) ;
#36806=ADVANCED_FACE ( 'NONE', ( #19436 ), #17392, .T. ) ;
#36809=CARTESIAN_POINT ( 'NONE',  ( 10.00000000000000000, -68.67312586195023982, 35.91791733033450384 ) ) ;
#36817=CARTESIAN_POINT ( 'NONE',  ( 0.000000000000000000, -77.32052557432845674, 5.256550761632577284 ) ) ;
#36821=FACE_OUTER_BOUND ( 'NONE', #42327, .T. ) ;
#36834=EDGE_LOOP ( 'NONE', ( #14251, #19062, #43646, #8367 ) ) ;
#36848=CARTESIAN_POINT ( 'NONE',  ( -10.00000000000000000, 0.000000000000000000, 0.000000000000000000 ) ) ;
#36855=CIRCLE ( 'NONE', #11088, 77.49899999999998101 ) ;
#36862=VECTOR ( 'NONE', #13992, 1000.000000000000000 ) ;
#36864=CARTESIAN_POINT ( 'NONE',  ( 10.00000000000000000, 0.000000000000000000, 0.000000000000000000 ) ) ;
#36868=AXIS2_PLACEMENT_3D ( 'NONE', #20637, #12823, #38782 ) ;
#36870=DIRECTION ( 'NONE',  ( -1.000000000000000000, 0.000000000000000000, -0.000000000000000000 ) ) ;
#36878=LINE ( 'NONE', #3346, #17442 ) ;
#36880=DIRECTION ( 'NONE',  ( 1.000000000000000000, 0.000000000000000000, -0.000000000000000000 ) ) ;
#36883=CARTESIAN_POINT ( 'NONE',  ( 0.000000000000000000, 2.543863470249527303, -81.96053171279901051 ) ) ;
#36890=EDGE_LOOP ( 'NONE', ( #36460, #12210, #47861, #3906 ) ) ;
#36891=CIRCLE ( 'NONE', #25187, 82.00000000000000000 ) ;
#36900=AXIS2_PLACEMENT_3D ( 'NONE', #21182, #17513, #9446 ) ;
#36906=CARTESIAN_POINT ( 'NONE',  ( 0.000000000000000000, -51.03279382321125723, 55.19960302592048862 ) ) ;
#36910=DIRECTION ( 'NONE',  ( -1.000000000000000000, 0.000000000000000000, 0.000000000000000000 ) ) ;
#36915=CARTESIAN_POINT ( 'NONE',  ( 0.000000000000000000, -73.72996012237449293, 14.67089635893687571 ) ) ;
#36918=ORIENTED_EDGE ( 'NONE', *, *, #30966, .F. ) ;
#36923=CIRCLE ( 'NONE', #31514, 31.99999999999999289 ) ;
#36929=CARTESIAN_POINT ( 'NONE',  ( 0.000000000000000000, 63.97538442413498672, -51.29473840253155714 ) ) ;
#36931=DIRECTION ( 'NONE',  ( -1.000000000000000000, 0.000000000000000000, -0.000000000000000000 ) ) ;
#36934=DIRECTION ( 'NONE',  ( -1.000000000000000000, 0.000000000000000000, 0.000000000000000000 ) ) ;
#36937=AXIS2_PLACEMENT_3D ( 'NONE', #31447, #12837, #20649 ) ;
#36938=EDGE_CURVE ( 'NONE', #40294, #28131, #24987, .T. ) ;
#36940=DIRECTION ( 'NONE',  ( 1.000000000000000000, -0.000000000000000000, -0.000000000000000000 ) ) ;
#36949=VERTEX_POINT ( 'NONE', #44792 ) ;
#36952=AXIS2_PLACEMENT_3D ( 'NONE', #43350, #9805, #40157 ) ;
#36953=VECTOR ( 'NONE', #4451, 1000.000000000000000 ) ;
#36956=AXIS2_PLACEMENT_3D ( 'NONE', #24060, #5448, #20361 ) ;
#36958=DIRECTION ( 'NONE',  ( -1.000000000000000000, 0.000000000000000000, 0.000000000000000000 ) ) ;
#36962=EDGE_CURVE ( 'NONE', #17873, #30560, #35960, .T. ) ;
#36968=CIRCLE ( 'NONE', #35404, 77.49899999999999523 ) ;
#36970=ORIENTED_EDGE ( 'NONE', *, *, #26068, .F. ) ;
#36971=CYLINDRICAL_SURFACE ( 'NONE', #18879, 82.00000000000000000 ) ;
#36974=EDGE_CURVE ( 'NONE', #2823, #10347, #47979, .T. ) ;
#36988=CYLINDRICAL_SURFACE ( 'NONE', #29920, 31.99999999999999289 ) ;
#36989=CARTESIAN_POINT ( 'NONE',  ( 10.00000000000000000, 49.70050353004977239, -59.46389618801908483 ) ) ;
#36996=CARTESIAN_POINT ( 'NONE',  ( 10.00000000000000000, 74.65491531819118620, 23.16904090965733332 ) ) ;
#36997=EDGE_CURVE ( 'NONE', #6193, #10782, #3680, .T. ) ;
#37003=CARTESIAN_POINT ( 'NONE',  ( 10.00000000000000000, -5.256550761632340141, -77.32052557432847095 ) ) ;
#37009=CARTESIAN_POINT ( 'NONE',  ( 5.000000000000002665, -40.65526001592565564, -71.21200624218839437 ) ) ;
#37015=AXIS2_PLACEMENT_3D ( 'NONE', #32116, #39211, #35537 ) ;
#37017=AXIS2_PLACEMENT_3D ( 'NONE', #48092, #18219, #37071 ) ;
#37018=ORIENTED_EDGE ( 'NONE', *, *, #11506, .T. ) ;
#37019=AXIS2_PLACEMENT_3D ( 'NONE', #26477, #14981, #29657 ) ;
#37024=CARTESIAN_POINT ( 'NONE',  ( 0.000000000000000000, -81.34940948281328588, -10.30890764327469711 ) ) ;
#37027=ADVANCED_FACE ( 'NONE', ( #10791 ), #29394, .T. ) ;
#37032=EDGE_CURVE ( 'NONE', #11671, #29028, #14768, .T. ) ;
#37041=ORIENTED_EDGE ( 'NONE', *, *, #43267, .T. ) ;
#37046=CARTESIAN_POINT ( 'NONE',  ( 10.00000000000000000, -59.75363087400034345, -56.15606465355021015 ) ) ;
#37047=CARTESIAN_POINT ( 'NONE',  ( 0.000000000000000000, 0.000000000000000000, 0.000000000000000000 ) ) ;
#37050=ORIENTED_EDGE ( 'NONE', *, *, #35094, .T. ) ;
#37051=CARTESIAN_POINT ( 'NONE',  ( 10.00000000000000000, 0.000000000000000000, 0.000000000000000000 ) ) ;
#37055=DIRECTION ( 'NONE',  ( 0.000000000000000000, 0.000000000000000000, 1.000000000000000000 ) ) ;
#37057=DIRECTION ( 'NONE',  ( 0.000000000000000000, 0.000000000000000000, 1.000000000000000000 ) ) ;
#37058=CARTESIAN_POINT ( 'NONE',  ( -10.00000000000000000, 0.000000000000000000, 0.000000000000000000 ) ) ;
#37066=DIRECTION ( 'NONE',  ( -1.000000000000000000, 0.000000000000000000, -0.000000000000000000 ) ) ;
#37068=CARTESIAN_POINT ( 'NONE',  ( 10.00000000000000000, 39.78640506895700213, -66.50666863321957578 ) ) ;
#37070=DIRECTION ( 'NONE',  ( 0.000000000000000000, 0.000000000000000000, 1.000000000000000000 ) ) ;
#37071=DIRECTION ( 'NONE',  ( 0.000000000000000000, 0.000000000000000000, 1.000000000000000000 ) ) ;
#37074=CIRCLE ( 'NONE', #22233, 77.49900000000000944 ) ;
#37075=DIRECTION ( 'NONE',  ( 1.000000000000000000, 0.000000000000000000, 0.000000000000000000 ) ) ;
#37089=AXIS2_PLACEMENT_3D ( 'NONE', #39850, #2871, #13416 ) ;
#37093=VECTOR ( 'NONE', #23245, 1000.000000000000000 ) ;
#37095=DIRECTION ( 'NONE',  ( 0.000000000000000000, 0.000000000000000000, 1.000000000000000000 ) ) ;
#37096=DIRECTION ( 'NONE',  ( -1.000000000000000000, 0.000000000000000000, 0.000000000000000000 ) ) ;
#37098=VERTEX_POINT ( 'NONE', #34740 ) ;
#37103=DIRECTION ( 'NONE',  ( -1.000000000000000000, 0.000000000000000000, 0.000000000000000000 ) ) ;
#37104=CARTESIAN_POINT ( 'NONE',  ( 10.00000000000000000, 0.000000000000000000, 0.000000000000000000 ) ) ;
#37110=VERTEX_POINT ( 'NONE', #26686 ) ;
#37112=DIRECTION ( 'NONE',  ( 0.000000000000000000, 0.000000000000000000, 1.000000000000000000 ) ) ;
#37113=CARTESIAN_POINT ( 'NONE',  ( 0.000000000000000000, 74.65491531819105830, 8.830959090343693418 ) ) ;
#37114=DIRECTION ( 'NONE',  ( 0.000000000000000000, 0.000000000000000000, 1.000000000000000000 ) ) ;
#37116=FACE_OUTER_BOUND ( 'NONE', #33615, .T. ) ;
#37124=ORIENTED_EDGE ( 'NONE', *, *, #29727, .T. ) ;
#37126=CARTESIAN_POINT ( 'NONE',  ( 10.00000000000000000, 77.19088730480524418, 6.903761155838049390 ) ) ;
#37128=EDGE_CURVE ( 'NONE', #14493, #46638, #11728, .T. ) ;
#37131=CARTESIAN_POINT ( 'NONE',  ( 0.000000000000000000, -22.90783923731686045, 78.73519480814945837 ) ) ;
#37133=AXIS2_PLACEMENT_3D ( 'NONE', #32441, #17016, #39556 ) ;
#37141=EDGE_CURVE ( 'NONE', #28726, #690, #25028, .T. ) ;
#37147=EDGE_LOOP ( 'NONE', ( #9454, #44549, #9819, #33254 ) ) ;
#37150=AXIS2_PLACEMENT_3D ( 'NONE', #4205, #45306, #7861 ) ;
#37156=ORIENTED_EDGE ( 'NONE', *, *, #19659, .F. ) ;
#37157=EDGE_CURVE ( 'NONE', #35449, #2830, #24225, .T. ) ;
#37159=CARTESIAN_POINT ( 'NONE',  ( 0.000000000000000000, 74.65491531819118620, -8.830959090342659579 ) ) ;
#37162=EDGE_CURVE ( 'NONE', #43853, #30369, #31094, .T. ) ;
#37164=EDGE_CURVE ( 'NONE', #41833, #36384, #4424, .T. ) ;
#37167=DIRECTION ( 'NONE',  ( 0.000000000000000000, 0.000000000000000000, 1.000000000000000000 ) ) ;
#37170=DIRECTION ( 'NONE',  ( -1.000000000000000000, -0.000000000000000000, 0.000000000000000000 ) ) ;
#37172=CARTESIAN_POINT ( 'NONE',  ( 10.00000000000000000, 0.000000000000000000, 0.000000000000000000 ) ) ;
#37180=ORIENTED_EDGE ( 'NONE', *, *, #42273, .F. ) ;
#37181=EDGE_CURVE ( 'NONE', #11996, #10143, #44555, .T. ) ;
#37191=CYLINDRICAL_SURFACE ( 'NONE', #35153, 31.99999999999998579 ) ;
#37192=CARTESIAN_POINT ( 'NONE',  ( 10.00000000000000000, 36.73666225445894185, 65.58780272294090707 ) ) ;
#37195=ADVANCED_FACE ( 'NONE', ( #232 ), #24702, .T. ) ;
#37208=ORIENTED_EDGE ( 'NONE', *, *, #15759, .T. ) ;
#37209=VECTOR ( 'NONE', #25195, 1000.000000000000000 ) ;
#37214=EDGE_LOOP ( 'NONE', ( #32755, #17216, #13772, #37816 ) ) ;
#37219=CARTESIAN_POINT ( 'NONE',  ( 10.00000000000000000, 0.000000000000000000, 0.000000000000000000 ) ) ;
#37227=ORIENTED_EDGE ( 'NONE', *, *, #32797, .F. ) ;
#37233=VERTEX_POINT ( 'NONE', #42589 ) ;
#37239=VERTEX_POINT ( 'NONE', #46503 ) ;
#37244=FACE_OUTER_BOUND ( 'NONE', #20129, .T. ) ;
#37246=CYLINDRICAL_SURFACE ( 'NONE', #37019, 82.00000000000000000 ) ;
#37248=AXIS2_PLACEMENT_3D ( 'NONE', #15215, #7618, #47997 ) ;
#37249=DIRECTION ( 'NONE',  ( -1.000000000000000000, 0.000000000000000000, 0.000000000000000000 ) ) ;
#37251=DIRECTION ( 'NONE',  ( -1.000000000000000000, 0.000000000000000000, 0.000000000000000000 ) ) ;
#37264=DIRECTION ( 'NONE',  ( 0.000000000000000000, -0.07845909572783058006, -0.9969173337331290741 ) ) ;
#37271=FACE_OUTER_BOUND ( 'NONE', #43310, .T. ) ;
#37275=VERTEX_POINT ( 'NONE', #38919 ) ;
#37276=CIRCLE ( 'NONE', #4478, 82.00000000000000000 ) ;
#37277=DIRECTION ( 'NONE',  ( 0.000000000000000000, 0.000000000000000000, 1.000000000000000000 ) ) ;
#37280=VERTEX_POINT ( 'NONE', #42336 ) ;
#37290=EDGE_CURVE ( 'NONE', #36459, #18078, #33617, .T. ) ;
#37293=DIRECTION ( 'NONE',  ( 0.000000000000000000, 0.000000000000000000, 1.000000000000000000 ) ) ;
#37294=DIRECTION ( 'NONE',  ( -1.000000000000000000, 0.000000000000000000, -0.000000000000000000 ) ) ;
#37299=DIRECTION ( 'NONE',  ( -1.000000000000000000, 0.000000000000000000, 0.000000000000000000 ) ) ;
#37300=ORIENTED_EDGE ( 'NONE', *, *, #26148, .F. ) ;
#37303=AXIS2_PLACEMENT_3D ( 'NONE', #24431, #9745, #43043 ) ;
#37310=EDGE_CURVE ( 'NONE', #46337, #11996, #47594, .T. ) ;
#37316=DIRECTION ( 'NONE',  ( -1.000000000000000000, -0.000000000000000000, -0.000000000000000000 ) ) ;
#37320=CARTESIAN_POINT ( 'NONE',  ( 10.00000000000000000, 55.20638768913760686, 51.02545421589343988 ) ) ;
#37323=VECTOR ( 'NONE', #36231, 1000.000000000000000 ) ;
#37330=VERTEX_POINT ( 'NONE', #17335 ) ;
#37335=CARTESIAN_POINT ( 'NONE',  ( 0.000000000000000000, 73.95703589263973754, 23.16143007188453851 ) ) ;
#37337=EDGE_CURVE ( 'NONE', #10502, #2146, #5619, .T. ) ;
#37348=DIRECTION ( 'NONE',  ( -1.000000000000000000, 0.000000000000000000, 0.000000000000000000 ) ) ;
#37352=ORIENTED_EDGE ( 'NONE', *, *, #23312, .F. ) ;
#37354=ORIENTED_EDGE ( 'NONE', *, *, #882, .F. ) ;
#37358=DIRECTION ( 'NONE',  ( -1.000000000000000000, 0.000000000000000000, 0.000000000000000000 ) ) ;
#37359=CARTESIAN_POINT ( 'NONE',  ( 10.00000000000000000, -31.46837873494930093, -68.27212725128309501 ) ) ;
#37365=EDGE_CURVE ( 'NONE', #42351, #41545, #706, .T. ) ;
#37371=EDGE_CURVE ( 'NONE', #21081, #40538, #6341, .T. ) ;
#37378=CARTESIAN_POINT ( 'NONE',  ( 10.00000000000000000, 46.53671651294032330, -59.03961581697353012 ) ) ;
#37379=CIRCLE ( 'NONE', #36596, 77.49900000000000944 ) ;
#37381=DIRECTION ( 'NONE',  ( -1.000000000000000000, -0.000000000000000000, -0.000000000000000000 ) ) ;
#37387=( NAMED_UNIT ( * ) SI_UNIT ( $, .STERADIAN. ) SOLID_ANGLE_UNIT ( ) );
#37388=DIRECTION ( 'NONE',  ( 0.000000000000000000, -0.7604059656000368150, 0.6494480483301767748 ) ) ;
#37391=ORIENTED_EDGE ( 'NONE', *, *, #24377, .T. ) ;
#37395=DIRECTION ( 'NONE',  ( 0.000000000000000000, 0.000000000000000000, 1.000000000000000000 ) ) ;
#37399=EDGE_LOOP ( 'NONE', ( #40123, #13897, #6919, #42786 ) ) ;
#37400=AXIS2_PLACEMENT_3D ( 'NONE', #4341, #19472, #15102 ) ;
#37403=DIRECTION ( 'NONE',  ( -1.000000000000000000, 0.000000000000000000, -0.000000000000000000 ) ) ;
#37408=DIRECTION ( 'NONE',  ( -1.000000000000000000, -0.000000000000000000, 0.000000000000000000 ) ) ;
#37412=CARTESIAN_POINT ( 'NONE',  ( 0.000000000000000000, -77.32052557432837148, -5.256550761633697277 ) ) ;
#37414=CARTESIAN_POINT ( 'NONE',  ( 10.00000000000000000, -71.87247863392384772, -39.47590169984921005 ) ) ;
#37415=ORIENTED_EDGE ( 'NONE', *, *, #17040, .T. ) ;
#37416=ORIENTED_EDGE ( 'NONE', *, *, #25059, .T. ) ;
#37418=EDGE_CURVE ( 'NONE', #15863, #39100, #42150, .T. ) ;
#37419=AXIS2_PLACEMENT_3D ( 'NONE', #24255, #2004, #2454 ) ;
#37422=EDGE_LOOP ( 'NONE', ( #3122, #7369, #2066, #45291 ) ) ;
#37429=DIRECTION ( 'NONE',  ( -1.000000000000000000, 0.000000000000000000, 0.000000000000000000 ) ) ;
#37432=DIRECTION ( 'NONE',  ( 0.000000000000000000, 0.000000000000000000, -1.000000000000000000 ) ) ;
#37442=CARTESIAN_POINT ( 'NONE',  ( 0.000000000000000000, 18.89407956138256139, 75.16055320797038064 ) ) ;
#37445=VERTEX_POINT ( 'NONE', #13918 ) ;
#37449=AXIS2_PLACEMENT_3D ( 'NONE', #1686, #17565, #12700 ) ;
#37455=EDGE_CURVE ( 'NONE', #1792, #16097, #7733, .T. ) ;
#37456=CARTESIAN_POINT ( 'NONE',  ( 0.000000000000000000, 0.000000000000000000, 0.000000000000000000 ) ) ;
#37458=VERTEX_POINT ( 'NONE', #21249 ) ;
#37462=CARTESIAN_POINT ( 'NONE',  ( -10.00000000000000000, 0.000000000000000000, 0.000000000000000000 ) ) ;
#37463=EDGE_CURVE ( 'NONE', #26870, #10088, #17820, .T. ) ;
#37464=AXIS2_PLACEMENT_3D ( 'NONE', #19123, #534, #37491 ) ;
#37465=DIRECTION ( 'NONE',  ( 0.000000000000000000, -0.7071067811865537900, 0.7071067811865413555 ) ) ;
#37470=ORIENTED_EDGE ( 'NONE', *, *, #42255, .F. ) ;
#37471=CIRCLE ( 'NONE', #20242, 82.00000000000000000 ) ;
#37476=CARTESIAN_POINT ( 'NONE',  ( 0.000000000000000000, -71.27951684758046724, 30.41916302227088309 ) ) ;
#37478=VERTEX_POINT ( 'NONE', #22703 ) ;
#37479=DIRECTION ( 'NONE',  ( 0.000000000000000000, 0.000000000000000000, 1.000000000000000000 ) ) ;
#37484=AXIS2_PLACEMENT_3D ( 'NONE', #37047, #2367, #44399 ) ;
#37486=DIRECTION ( 'NONE',  ( 1.000000000000000000, 0.000000000000000000, -0.000000000000000000 ) ) ;
#37491=DIRECTION ( 'NONE',  ( 0.000000000000000000, 0.1564344650402244852, 0.9876883405951387696 ) ) ;
#37493=DIRECTION ( 'NONE',  ( 0.000000000000000000, 0.000000000000000000, -1.000000000000000000 ) ) ;
#37494=ORIENTED_EDGE ( 'NONE', *, *, #13604, .F. ) ;
#37497=FACE_OUTER_BOUND ( 'NONE', #33424, .T. ) ;
#37508=CARTESIAN_POINT ( 'NONE',  ( 0.000000000000000000, -60.67117009219098378, -55.16347631943106933 ) ) ;
#37510=CARTESIAN_POINT ( 'NONE',  ( 10.00000000000000000, -60.67117009219097667, -55.16347631943105512 ) ) ;
#37511=EDGE_LOOP ( 'NONE', ( #40767, #35417, #1245, #11721 ) ) ;
#37516=ADVANCED_FACE ( 'NONE', ( #44735 ), #4367, .T. ) ;
#37527=DIRECTION ( 'NONE',  ( -1.000000000000000000, 0.000000000000000000, 0.000000000000000000 ) ) ;
#37528=LINE ( 'NONE', #18912, #15776 ) ;
#37529=CIRCLE ( 'NONE', #16437, 82.00000000000000000 ) ;
#37531=ORIENTED_EDGE ( 'NONE', *, *, #15630, .T. ) ;
#37536=DIRECTION ( 'NONE',  ( 0.000000000000000000, 0.3090169943749411785, 0.9510565162951556406 ) ) ;
#37541=DIRECTION ( 'NONE',  ( 1.000000000000000000, 0.000000000000000000, 0.000000000000000000 ) ) ;
#37542=CARTESIAN_POINT ( 'NONE',  ( 10.00000000000000000, 0.000000000000000000, 0.000000000000000000 ) ) ;
#37543=ORIENTED_EDGE ( 'NONE', *, *, #13116, .T. ) ;
#37545=CARTESIAN_POINT ( 'NONE',  ( 10.00000000000000000, 0.000000000000000000, 0.000000000000000000 ) ) ;
#37546=AXIS2_PLACEMENT_3D ( 'NONE', #31648, #17162, #32118 ) ;
#37551=CIRCLE ( 'NONE', #7841, 31.99999999999999289 ) ;
#37552=CARTESIAN_POINT ( 'NONE',  ( 5.000000000000002665, 10.30890764327501863, -81.34940948281325745 ) ) ;
#37554=DIRECTION ( 'NONE',  ( -1.000000000000000000, 0.000000000000000000, 0.000000000000000000 ) ) ;
#37556=DIRECTION ( 'NONE',  ( -1.000000000000000000, 0.000000000000000000, 0.000000000000000000 ) ) ;
#37560=DIRECTION ( 'NONE',  ( 1.000000000000000000, 0.000000000000000000, 0.000000000000000000 ) ) ;
#37564=ADVANCED_FACE ( 'NONE', ( #41557 ), #33955, .T. ) ;
#37571=CIRCLE ( 'NONE', #36030, 77.49899999999999523 ) ;
#37572=AXIS2_PLACEMENT_3D ( 'NONE', #3934, #29631, #45286 ) ;
#37577=EDGE_CURVE ( 'NONE', #42453, #42302, #24925, .T. ) ;
#37578=EDGE_CURVE ( 'NONE', #25169, #4138, #15384, .T. ) ;
#37581=AXIS2_PLACEMENT_3D ( 'NONE', #46220, #23952, #17072 ) ;
#37582=CARTESIAN_POINT ( 'NONE',  ( 10.00000000000000000, 0.000000000000000000, 0.000000000000000000 ) ) ;
#37588=VERTEX_POINT ( 'NONE', #4832 ) ;
#37589=FACE_OUTER_BOUND ( 'NONE', #13078, .T. ) ;
#37591=CARTESIAN_POINT ( 'NONE',  ( 0.000000000000000000, -8.840884882375609877, 74.65374052328647281 ) ) ;
#37595=DIRECTION ( 'NONE',  ( -1.000000000000000000, 0.000000000000000000, 0.000000000000000000 ) ) ;
#37596=ORIENTED_EDGE ( 'NONE', *, *, #3140, .F. ) ;
#37612=DIRECTION ( 'NONE',  ( -1.000000000000000000, -0.000000000000000000, 0.000000000000000000 ) ) ;
#37615=FACE_OUTER_BOUND ( 'NONE', #15400, .T. ) ;
#37624=VECTOR ( 'NONE', #3836, 1000.000000000000000 ) ;
#37629=ADVANCED_FACE ( 'NONE', ( #900 ), #15134, .T. ) ;
#37631=ORIENTED_EDGE ( 'NONE', *, *, #32199, .T. ) ;
#37633=VERTEX_POINT ( 'NONE', #15849 ) ;
#37635=DIRECTION ( 'NONE',  ( -1.000000000000000000, 0.000000000000000000, 0.000000000000000000 ) ) ;
#37638=EDGE_CURVE ( 'NONE', #19851, #13864, #48407, .T. ) ;
#37639=EDGE_CURVE ( 'NONE', #28820, #16811, #21798, .T. ) ;
#37640=AXIS2_PLACEMENT_3D ( 'NONE', #42748, #38589, #46894 ) ;
#37641=AXIS2_PLACEMENT_3D ( 'NONE', #24344, #31723, #8680 ) ;
#37645=CARTESIAN_POINT ( 'NONE',  ( 10.00000000000000000, 30.41916302227216562, -71.27951684757994144 ) ) ;
#37654=AXIS2_PLACEMENT_3D ( 'NONE', #25955, #10074, #47512 ) ;
#37656=DIRECTION ( 'NONE',  ( -1.000000000000000000, 0.000000000000000000, 0.000000000000000000 ) ) ;
#37659=LINE ( 'NONE', #33732, #25871 ) ;
#37665=DIRECTION ( 'NONE',  ( 1.000000000000000000, 0.000000000000000000, 0.000000000000000000 ) ) ;
#37670=CARTESIAN_POINT ( 'NONE',  ( 10.00000000000000000, -44.88180994100329713, -63.18004540533077318 ) ) ;
#37671=CARTESIAN_POINT ( 'NONE',  ( 5.000000000000002665, 8.966570791701863996, -81.50828551894218776 ) ) ;
#37677=EDGE_CURVE ( 'NONE', #36949, #3853, #5555, .T. ) ;
#37683=AXIS2_PLACEMENT_3D ( 'NONE', #8953, #15820, #46165 ) ;
#37688=CARTESIAN_POINT ( 'NONE',  ( 10.00000000000000000, 26.02418014898407961, -70.52718814184231633 ) ) ;
#37690=ORIENTED_EDGE ( 'NONE', *, *, #21130, .F. ) ;
#37693=EDGE_CURVE ( 'NONE', #46360, #2363, #16333, .T. ) ;
#37699=EDGE_CURVE ( 'NONE', #13885, #34506, #12914, .T. ) ;
#37706=ORIENTED_EDGE ( 'NONE', *, *, #8129, .T. ) ;
#37710=VECTOR ( 'NONE', #18588, 1000.000000000000000 ) ;
#37713=ORIENTED_EDGE ( 'NONE', *, *, #3637, .F. ) ;
#37719=CARTESIAN_POINT ( 'NONE',  ( 0.000000000000000000, -59.75363087400113926, 56.15606465354937882 ) ) ;
#37727=DIRECTION ( 'NONE',  ( 0.000000000000000000, 0.000000000000000000, 1.000000000000000000 ) ) ;
#37734=DIRECTION ( 'NONE',  ( -1.000000000000000000, -0.000000000000000000, -0.000000000000000000 ) ) ;
#37740=CARTESIAN_POINT ( 'NONE',  ( -10.00000000000000000, 0.000000000000000000, 0.000000000000000000 ) ) ;
#37744=ADVANCED_FACE ( 'NONE', ( #2135 ), #17048, .T. ) ;
#37753=CIRCLE ( 'NONE', #30695, 31.99999999999999289 ) ;
#37754=DIRECTION ( 'NONE',  ( 0.000000000000000000, -0.2334453638558921240, -0.9723699203976797767 ) ) ;
#37755=VECTOR ( 'NONE', #19778, 1000.000000000000000 ) ;
#37761=EDGE_CURVE ( 'NONE', #40687, #13194, #35117, .T. ) ;
#37770=CARTESIAN_POINT ( 'NONE',  ( 10.00000000000000000, -26.01480285779885904, 70.53064760720306481 ) ) ;
#37772=AXIS2_PLACEMENT_3D ( 'NONE', #6563, #47199, #20774 ) ;
#37780=VECTOR ( 'NONE', #6073, 1000.000000000000000 ) ;
#37783=CARTESIAN_POINT ( 'NONE',  ( 0.000000000000000000, 34.44570377933598593, 69.42325613327452061 ) ) ;
#37791=LINE ( 'NONE', #40739, #9804 ) ;
#37794=LINE ( 'NONE', #22621, #4469 ) ;
#37804=FACE_OUTER_BOUND ( 'NONE', #4803, .T. ) ;
#37807=VERTEX_POINT ( 'NONE', #6765 ) ;
#37808=ADVANCED_FACE ( 'NONE', ( #18000 ), #25347, .T. ) ;
#37814=AXIS2_PLACEMENT_3D ( 'NONE', #21655, #25311, #10150 ) ;
#37816=ORIENTED_EDGE ( 'NONE', *, *, #42451, .T. ) ;
#37818=ORIENTED_EDGE ( 'NONE', *, *, #6333, .F. ) ;
#37820=CARTESIAN_POINT ( 'NONE',  ( 10.00000000000000000, -70.53064760720297954, -26.01480285779911839 ) ) ;
#37827=VERTEX_POINT ( 'NONE', #29025 ) ;
#37834=EDGE_LOOP ( 'NONE', ( #16342, #4310, #29627, #4379 ) ) ;
#37840=ADVANCED_FACE ( 'NONE', ( #44207 ), #14600, .T. ) ;
#37842=DIRECTION ( 'NONE',  ( -1.000000000000000000, -0.000000000000000000, 0.000000000000000000 ) ) ;
#37849=ORIENTED_EDGE ( 'NONE', *, *, #9505, .F. ) ;
#37850=DIRECTION ( 'NONE',  ( -1.000000000000000000, 0.000000000000000000, 0.000000000000000000 ) ) ;
#37854=AXIS2_PLACEMENT_3D ( 'NONE', #469, #22503, #41353 ) ;
#37857=CIRCLE ( 'NONE', #16755, 31.99999999999998579 ) ;
#37858=CARTESIAN_POINT ( 'NONE',  ( 10.00000000000000000, 14.66109333815564852, -73.73191006444555740 ) ) ;
#37864=CARTESIAN_POINT ( 'NONE',  ( 10.00000000000000000, 59.03961581697399907, 46.53671651293969802 ) ) ;
#37867=CIRCLE ( 'NONE', #16760, 77.49900000000002365 ) ;
#37868=LINE ( 'NONE', #30520, #4459 ) ;
#37869=DIRECTION ( 'NONE',  ( -1.000000000000000000, 0.000000000000000000, 0.000000000000000000 ) ) ;
#37870=CIRCLE ( 'NONE', #48055, 82.00000000000000000 ) ;
#37876=ORIENTED_EDGE ( 'NONE', *, *, #5145, .T. ) ;
#37877=EDGE_LOOP ( 'NONE', ( #6795, #16033, #45288, #9760 ) ) ;
#37882=CARTESIAN_POINT ( 'NONE',  ( 10.00000000000000000, 40.65526001592713357, -71.21200624218752750 ) ) ;
#37883=ORIENTED_EDGE ( 'NONE', *, *, #44340, .T. ) ;
#37885=CARTESIAN_POINT ( 'NONE',  ( 0.000000000000000000, 8.830959090343430518, -74.65491531819107252 ) ) ;
#37892=CARTESIAN_POINT ( 'NONE',  ( 10.00000000000000000, 0.000000000000000000, 0.000000000000000000 ) ) ;
#37894=ADVANCED_FACE ( 'NONE', ( #25108 ), #6519, .T. ) ;
#37895=VERTEX_POINT ( 'NONE', #34371 ) ;
#37902=CARTESIAN_POINT ( 'NONE',  ( 0.000000000000000000, -26.01480285779785362, -70.53064760720343429 ) ) ;
#37903=EDGE_CURVE ( 'NONE', #12095, #34190, #35929, .T. ) ;
#37904=AXIS2_PLACEMENT_3D ( 'NONE', #15227, #30156, #10321 ) ;
#37909=ORIENTED_EDGE ( 'NONE', *, *, #5196, .T. ) ;
#37911=DIRECTION ( 'NONE',  ( -1.000000000000000000, 0.000000000000000000, 0.000000000000000000 ) ) ;
#37914=CARTESIAN_POINT ( 'NONE',  ( 10.00000000000000000, 62.50329211542494789, -41.76937507738723099 ) ) ;
#37917=CARTESIAN_POINT ( 'NONE',  ( 10.00000000000000000, -74.65491531819111515, -8.830959090343204920 ) ) ;
#37922=EDGE_CURVE ( 'NONE', #31513, #42004, #14028, .T. ) ;
#37923=EDGE_CURVE ( 'NONE', #6602, #3764, #42963, .T. ) ;
#37928=ORIENTED_EDGE ( 'NONE', *, *, #21664, .T. ) ;
#37932=EDGE_CURVE ( 'NONE', #6665, #32258, #15069, .T. ) ;
#37933=ORIENTED_EDGE ( 'NONE', *, *, #25439, .T. ) ;
#37936=UNCERTAINTY_MEASURE_WITH_UNIT (LENGTH_MEASURE( 1.000000000000000082E-05 ), #9344, 'distance_accuracy_value', 'NONE');
#37941=AXIS2_PLACEMENT_3D ( 'NONE', #17237, #39781, #13346 ) ;
#37945=CARTESIAN_POINT ( 'NONE',  ( 10.00000000000000000, -59.46389618801999433, 49.70050353004867816 ) ) ;
#37949=VERTEX_POINT ( 'NONE', #19218 ) ;
#37956=ORIENTED_EDGE ( 'NONE', *, *, #29275, .T. ) ;
#37961=ORIENTED_EDGE ( 'NONE', *, *, #14657, .F. ) ;
#37964=DIRECTION ( 'NONE',  ( -1.000000000000000000, 0.000000000000000000, 0.000000000000000000 ) ) ;
#37968=DIRECTION ( 'NONE',  ( 0.000000000000000000, -0.07845909572785220165, 0.9969173337331274087 ) ) ;
#37969=ORIENTED_EDGE ( 'NONE', *, *, #44156, .F. ) ;
#37973=ORIENTED_EDGE ( 'NONE', *, *, #11353, .T. ) ;
#37974=CARTESIAN_POINT ( 'NONE',  ( 10.00000000000000000, 0.000000000000000000, 0.000000000000000000 ) ) ;
#37978=FACE_OUTER_BOUND ( 'NONE', #21443, .T. ) ;
#37979=LINE ( 'NONE', #45814, #34341 ) ;
#37984=ORIENTED_EDGE ( 'NONE', *, *, #23582, .F. ) ;
#37986=EDGE_CURVE ( 'NONE', #23867, #11188, #30479, .T. ) ;
#37990=FACE_OUTER_BOUND ( 'NONE', #36746, .T. ) ;
#37997=EDGE_CURVE ( 'NONE', #21394, #29885, #11881, .T. ) ;
#37999=CIRCLE ( 'NONE', #48111, 82.00000000000000000 ) ;
#38001=EDGE_LOOP ( 'NONE', ( #12006, #28641, #33902, #47453 ) ) ;
#38004=ORIENTED_EDGE ( 'NONE', *, *, #34778, .F. ) ;
#38005=CARTESIAN_POINT ( 'NONE',  ( 10.00000000000000000, 55.38113227695858143, -54.21277698773617715 ) ) ;
#38013=CYLINDRICAL_SURFACE ( 'NONE', #22686, 77.49899999999999523 ) ;
#38014=DIRECTION ( 'NONE',  ( -1.000000000000000000, 0.000000000000000000, 0.000000000000000000 ) ) ;
#38015=ORIENTED_EDGE ( 'NONE', *, *, #37181, .T. ) ;
#38016=ORIENTED_EDGE ( 'NONE', *, *, #11743, .T. ) ;
#38022=CARTESIAN_POINT ( 'NONE',  ( 0.000000000000000000, 0.000000000000000000, 0.000000000000000000 ) ) ;
#38029=ADVANCED_FACE ( 'NONE', ( #7718 ), #22644, .T. ) ;
#38031=ORIENTED_EDGE ( 'NONE', *, *, #26696, .T. ) ;
#38038=EDGE_LOOP ( 'NONE', ( #31324, #4771, #32930, #1375 ) ) ;
#38041=DIRECTION ( 'NONE',  ( 0.000000000000000000, 0.000000000000000000, 1.000000000000000000 ) ) ;
#38048=DIRECTION ( 'NONE',  ( -1.000000000000000000, -0.000000000000000000, -0.000000000000000000 ) ) ;
#38049=AXIS2_PLACEMENT_3D ( 'NONE', #46537, #39432, #36223 ) ;
#38052=CARTESIAN_POINT ( 'NONE',  ( 10.00000000000000000, -34.44570377933549565, -69.42325613327476219 ) ) ;
#38057=CARTESIAN_POINT ( 'NONE',  ( 0.000000000000000000, 0.000000000000000000, 0.000000000000000000 ) ) ;
#38059=CIRCLE ( 'NONE', #18520, 82.00000000000000000 ) ;
#38064=ORIENTED_EDGE ( 'NONE', *, *, #11352, .F. ) ;
#38065=EDGE_LOOP ( 'NONE', ( #8727, #4602, #14656, #2888 ) ) ;
#38068=CARTESIAN_POINT ( 'NONE',  ( 10.00000000000000000, -72.35160999960831418, 20.41045688087797672 ) ) ;
#38071=EDGE_CURVE ( 'NONE', #13186, #9766, #42712, .T. ) ;
#38072=CIRCLE ( 'NONE', #6827, 82.00000000000000000 ) ;
#38074=ADVANCED_FACE ( 'NONE', ( #39031 ), #12607, .T. ) ;
#38078=AXIS2_PLACEMENT_3D ( 'NONE', #704, #34718, #41359 ) ;
#38082=CARTESIAN_POINT ( 'NONE',  ( 10.00000000000000000, -76.41127070299262414, -12.93880638057396304 ) ) ;
#38083=DIRECTION ( 'NONE',  ( 0.000000000000000000, 0.5224985647159500202, -0.8526401643540915121 ) ) ;
#38085=CIRCLE ( 'NONE', #21661, 82.00000000000000000 ) ;
#38088=ORIENTED_EDGE ( 'NONE', *, *, #17701, .F. ) ;
#38094=DIRECTION ( 'NONE',  ( 0.000000000000000000, 8.881784197001252323E-16, 1.000000000000000000 ) ) ;
#38095=CARTESIAN_POINT ( 'NONE',  ( 5.000000000000000000, 81.96053171279902472, 2.543863470248670211 ) ) ;
#38096=FACE_OUTER_BOUND ( 'NONE', #39511, .T. ) ;
#38103=ORIENTED_EDGE ( 'NONE', *, *, #33797, .T. ) ;
#38105=DIRECTION ( 'NONE',  ( -1.000000000000000000, 0.000000000000000000, 0.000000000000000000 ) ) ;
#38107=DIRECTION ( 'NONE',  ( -1.000000000000000000, -0.000000000000000000, 0.000000000000000000 ) ) ;
#38111=AXIS2_PLACEMENT_3D ( 'NONE', #37051, #37299, #18683 ) ;
#38116=( LENGTH_UNIT ( ) NAMED_UNIT ( * ) SI_UNIT ( .MILLI., .METRE. ) );
#38120=ORIENTED_EDGE ( 'NONE', *, *, #29347, .F. ) ;
#38133=DIRECTION ( 'NONE',  ( -1.000000000000000000, -0.000000000000000000, 0.000000000000000000 ) ) ;
#38134=VECTOR ( 'NONE', #39228, 1000.000000000000000 ) ;
#38139=ORIENTED_EDGE ( 'NONE', *, *, #6635, .T. ) ;
#38145=EDGE_CURVE ( 'NONE', #48048, #17812, #1563, .T. ) ;
#38149=ORIENTED_EDGE ( 'NONE', *, *, #18419, .T. ) ;
#38150=ORIENTED_EDGE ( 'NONE', *, *, #21274, .F. ) ;
#38160=( GEOMETRIC_REPRESENTATION_CONTEXT ( 3 ) GLOBAL_UNCERTAINTY_ASSIGNED_CONTEXT ( ( #30582 ) ) GLOBAL_UNIT_ASSIGNED_CONTEXT ( ( #38116, #33944, #37387 ) ) REPRESENTATION_CONTEXT ( 'NONE', 'WORKASPACE' ) );
#38163=LINE ( 'NONE', #26665, #46684 ) ;
#38174=ADVANCED_FACE ( 'NONE', ( #16515 ), #1588, .T. ) ;
#38175=CARTESIAN_POINT ( 'NONE',  ( 0.000000000000000000, 41.76106447765489094, 62.50884508063442269 ) ) ;
#38179=CARTESIAN_POINT ( 'NONE',  ( 10.00000000000000000, -18.89407956138203204, -75.16055320797050854 ) ) ;
#38187=VERTEX_POINT ( 'NONE', #23370 ) ;
#38192=AXIS2_PLACEMENT_3D ( 'NONE', #36537, #10841, #26257 ) ;
#38194=ORIENTED_EDGE ( 'NONE', *, *, #15094, .T. ) ;
#38198=ORIENTED_EDGE ( 'NONE', *, *, #20784, .F. ) ;
#38208=ORIENTED_EDGE ( 'NONE', *, *, #36997, .F. ) ;
#38211=ORIENTED_EDGE ( 'NONE', *, *, #8671, .F. ) ;
#38218=CYLINDRICAL_SURFACE ( 'NONE', #19054, 82.00000000000000000 ) ;
#38219=AXIS2_PLACEMENT_3D ( 'NONE', #10460, #21948, #6796 ) ;
#38221=DIRECTION ( 'NONE',  ( -1.000000000000000000, 0.000000000000000000, -0.000000000000000000 ) ) ;
#38232=CARTESIAN_POINT ( 'NONE',  ( 10.00000000000000000, 15.33399622253600292, -80.55351364060572905 ) ) ;
#38233=ORIENTED_EDGE ( 'NONE', *, *, #34036, .T. ) ;
#38235=EDGE_CURVE ( 'NONE', #15455, #42951, #39532, .T. ) ;
#38238=CARTESIAN_POINT ( 'NONE',  ( 10.00000000000000000, -59.03342792756297541, 46.54456581323783126 ) ) ;
#38243=ORIENTED_EDGE ( 'NONE', *, *, #9317, .T. ) ;
#38251=AXIS2_PLACEMENT_3D ( 'NONE', #1307, #27497, #5226 ) ;
#38254=ORIENTED_EDGE ( 'NONE', *, *, #8906, .T. ) ;
#38258=CARTESIAN_POINT ( 'NONE',  ( 0.000000000000000000, 46.54456581323805153, 59.03342792756280488 ) ) ;
#38261=ORIENTED_EDGE ( 'NONE', *, *, #5630, .F. ) ;
#38267=DIRECTION ( 'NONE',  ( -1.000000000000000000, -0.000000000000000000, -0.000000000000000000 ) ) ;
#38273=DIRECTION ( 'NONE',  ( -1.000000000000000000, 0.000000000000000000, 0.000000000000000000 ) ) ;
#38279=DIRECTION ( 'NONE',  ( -1.000000000000000000, 0.000000000000000000, 0.000000000000000000 ) ) ;
#38285=ORIENTED_EDGE ( 'NONE', *, *, #35529, .T. ) ;
#38296=EDGE_CURVE ( 'NONE', #32513, #30166, #9373, .T. ) ;
#38302=CYLINDRICAL_SURFACE ( 'NONE', #12883, 31.99999999999999289 ) ;
#38308=VERTEX_POINT ( 'NONE', #36787 ) ;
#38311=AXIS2_PLACEMENT_3D ( 'NONE', #23795, #20123, #1766 ) ;
#38312=CARTESIAN_POINT ( 'NONE',  ( 10.00000000000000000, 46.11716303203188261, 67.80270845531904911 ) ) ;
#38320=CIRCLE ( 'NONE', #18737, 31.99999999999998579 ) ;
#38322=ORIENTED_EDGE ( 'NONE', *, *, #15682, .F. ) ;
#38323=DIRECTION ( 'NONE',  ( -1.000000000000000000, 0.000000000000000000, -0.000000000000000000 ) ) ;
#38327=CARTESIAN_POINT ( 'NONE',  ( 0.000000000000000000, 0.000000000000000000, 0.000000000000000000 ) ) ;
#38329=DIRECTION ( 'NONE',  ( -1.000000000000000000, -0.000000000000000000, -0.000000000000000000 ) ) ;
#38331=DIRECTION ( 'NONE',  ( -1.000000000000000000, -0.000000000000000000, -0.000000000000000000 ) ) ;
#38332=EDGE_CURVE ( 'NONE', #24479, #29380, #41426, .T. ) ;
#38339=CYLINDRICAL_SURFACE ( 'NONE', #40819, 31.99999999999999289 ) ;
#38349=VECTOR ( 'NONE', #39053, 1000.000000000000000 ) ;
#38350=AXIS2_PLACEMENT_3D ( 'NONE', #10071, #3441, #18376 ) ;
#38351=EDGE_CURVE ( 'NONE', #33111, #18992, #41211, .T. ) ;
#38353=DIRECTION ( 'NONE',  ( -1.000000000000000000, -0.000000000000000000, -0.000000000000000000 ) ) ;
#38358=ORIENTED_EDGE ( 'NONE', *, *, #30580, .F. ) ;
#38367=ORIENTED_EDGE ( 'NONE', *, *, #30368, .T. ) ;
#38369=CARTESIAN_POINT ( 'NONE',  ( 0.000000000000000000, 0.000000000000000000, 0.000000000000000000 ) ) ;
#38378=EDGE_LOOP ( 'NONE', ( #46249, #33143, #5888, #41640 ) ) ;
#38379=ORIENTED_EDGE ( 'NONE', *, *, #43262, .F. ) ;
#38383=ORIENTED_EDGE ( 'NONE', *, *, #34854, .F. ) ;
#38387=VERTEX_POINT ( 'NONE', #45339 ) ;
#38388=AXIS2_PLACEMENT_3D ( 'NONE', #48193, #21758, #11239 ) ;
#38390=CIRCLE ( 'NONE', #36798, 82.00000000000000000 ) ;
#38413=EDGE_CURVE ( 'NONE', #46842, #4186, #47657, .T. ) ;
#38414=AXIS2_PLACEMENT_3D ( 'NONE', #20304, #19569, #26954 ) ;
#38419=ORIENTED_EDGE ( 'NONE', *, *, #22610, .T. ) ;
#38420=VECTOR ( 'NONE', #43270, 1000.000000000000000 ) ;
#38422=DIRECTION ( 'NONE',  ( 0.000000000000000000, 0.5224985647159441360, 0.8526401643540952868 ) ) ;
#38428=VERTEX_POINT ( 'NONE', #44625 ) ;
#38430=CYLINDRICAL_SURFACE ( 'NONE', #28178, 32.00000000000000000 ) ;
#38432=CARTESIAN_POINT ( 'NONE',  ( 10.00000000000000000, 77.19088730480534366, -6.903761155836915187 ) ) ;
#38436=DIRECTION ( 'NONE',  ( 0.000000000000000000, 0.000000000000000000, 1.000000000000000000 ) ) ;
#38439=ORIENTED_EDGE ( 'NONE', *, *, #20967, .F. ) ;
#38442=CARTESIAN_POINT ( 'NONE',  ( 10.00000000000000000, 0.000000000000000000, 0.000000000000000000 ) ) ;
#38446=ORIENTED_EDGE ( 'NONE', *, *, #26378, .T. ) ;
#38449=CARTESIAN_POINT ( 'NONE',  ( 10.00000000000000000, 0.000000000000000000, 0.000000000000000000 ) ) ;
#38458=CIRCLE ( 'NONE', #10311, 31.99999999999999645 ) ;
#38460=CARTESIAN_POINT ( 'NONE',  ( 10.00000000000000000, -51.03279382321125723, 55.19960302592048862 ) ) ;
#38466=DIRECTION ( 'NONE',  ( -1.000000000000000000, -0.000000000000000000, -0.000000000000000000 ) ) ;
#38468=ADVANCED_FACE ( 'NONE', ( #25769 ), #38013, .T. ) ;
#38481=AXIS2_PLACEMENT_3D ( 'NONE', #17251, #10161, #25565 ) ;
#38487=CIRCLE ( 'NONE', #14276, 31.99999999999999645 ) ;
#38490=VERTEX_POINT ( 'NONE', #20126 ) ;
#38498=ADVANCED_FACE ( 'NONE', ( #16454 ), #41938, .T. ) ;
#38499=CARTESIAN_POINT ( 'NONE',  ( 0.000000000000000000, -46.11716303203234446, 67.80270845531873647 ) ) ;
#38505=ORIENTED_EDGE ( 'NONE', *, *, #40653, .T. ) ;
#38517=CARTESIAN_POINT ( 'NONE',  ( 10.00000000000000000, 62.50329211542435104, 41.76937507738811917 ) ) ;
#38527=CIRCLE ( 'NONE', #8039, 31.99999999999999289 ) ;
#38528=VECTOR ( 'NONE', #23945, 1000.000000000000000 ) ;
#38529=CYLINDRICAL_SURFACE ( 'NONE', #34581, 31.99999999999999289 ) ;
#38530=FACE_OUTER_BOUND ( 'NONE', #8434, .T. ) ;
#38534=ADVANCED_FACE ( 'NONE', ( #31159 ), #42656, .T. ) ;
#38538=ORIENTED_EDGE ( 'NONE', *, *, #29619, .T. ) ;
#38551=DIRECTION ( 'NONE',  ( -1.000000000000000000, -0.000000000000000000, 0.000000000000000000 ) ) ;
#38553=AXIS2_PLACEMENT_3D ( 'NONE', #31904, #28694, #13513 ) ;
#38555=VERTEX_POINT ( 'NONE', #5443 ) ;
#38558=VERTEX_POINT ( 'NONE', #24052 ) ;
#38559=CIRCLE ( 'NONE', #45609, 31.99999999999999289 ) ;
#38574=CARTESIAN_POINT ( 'NONE',  ( 10.00000000000000000, -5.256550761633413060, 77.32052557432841411 ) ) ;
#38576=CARTESIAN_POINT ( 'NONE',  ( -10.00000000000000000, 0.000000000000000000, 0.000000000000000000 ) ) ;
#38580=ORIENTED_EDGE ( 'NONE', *, *, #44924, .T. ) ;
#38584=CARTESIAN_POINT ( 'NONE',  ( 0.000000000000000000, -62.50329211542407393, -41.76937507738853839 ) ) ;
#38585=VERTEX_POINT ( 'NONE', #19868 ) ;
#38589=DIRECTION ( 'NONE',  ( -1.000000000000000000, 0.000000000000000000, 0.000000000000000000 ) ) ;
#38594=CARTESIAN_POINT ( 'NONE',  ( 10.00000000000000000, 50.23322058963347558, 64.81221759200361987 ) ) ;
#38600=VERTEX_POINT ( 'NONE', #23316 ) ;
#38602=LINE ( 'NONE', #1144, #29895 ) ;
#38603=ORIENTED_EDGE ( 'NONE', *, *, #16514, .T. ) ;
#38608=CIRCLE ( 'NONE', #9652, 31.99999999999998934 ) ;
#38610=AXIS2_PLACEMENT_3D ( 'NONE', #19583, #45545, #4918 ) ;
#38612=AXIS2_PLACEMENT_3D ( 'NONE', #954, #44788, #45506 ) ;
#38613=ORIENTED_EDGE ( 'NONE', *, *, #15009, .T. ) ;
#38618=DIRECTION ( 'NONE',  ( -1.000000000000000000, 0.000000000000000000, 0.000000000000000000 ) ) ;
#38621=ORIENTED_EDGE ( 'NONE', *, *, #42354, .F. ) ;
#38629=CARTESIAN_POINT ( 'NONE',  ( 10.00000000000000000, -75.11764819372149304, 2.946379043146075905 ) ) ;
#38630=VERTEX_POINT ( 'NONE', #42405 ) ;
#38631=ORIENTED_EDGE ( 'NONE', *, *, #12249, .T. ) ;
#38635=AXIS2_PLACEMENT_3D ( 'NONE', #24608, #5518, #39551 ) ;
#38636=DIRECTION ( 'NONE',  ( -1.000000000000000000, 0.000000000000000000, 0.000000000000000000 ) ) ;
#38641=CARTESIAN_POINT ( 'NONE',  ( 0.000000000000000000, 68.55367621811141987, 44.99326035066078333 ) ) ;
#38647=LINE ( 'NONE', #12941, #21151 ) ;
#38650=AXIS2_PLACEMENT_3D ( 'NONE', #40224, #6921, #10838 ) ;
#38657=LINE ( 'NONE', #16138, #41041 ) ;
#38660=CARTESIAN_POINT ( 'NONE',  ( 10.00000000000000000, 0.8261519478441983200, -77.49459641780885022 ) ) ;
#38671=AXIS2_PLACEMENT_3D ( 'NONE', #26475, #11553, #34049 ) ;
#38673=VECTOR ( 'NONE', #7489, 1000.000000000000000 ) ;
#38674=CIRCLE ( 'NONE', #8148, 31.99999999999999289 ) ;
#38681=AXIS2_PLACEMENT_3D ( 'NONE', #29608, #47710, #48446 ) ;
#38684=AXIS2_PLACEMENT_3D ( 'NONE', #22098, #58, #44860 ) ;
#38689=EDGE_CURVE ( 'NONE', #27618, #45989, #35192, .T. ) ;
#38690=LINE ( 'NONE', #12728, #4003 ) ;
#38692=EDGE_LOOP ( 'NONE', ( #8763, #14452, #23932, #8609 ) ) ;
#38694=ORIENTED_EDGE ( 'NONE', *, *, #13496, .T. ) ;
#38702=ORIENTED_EDGE ( 'NONE', *, *, #16751, .T. ) ;
#38704=VECTOR ( 'NONE', #5354, 1000.000000000000000 ) ;
#38708=ORIENTED_EDGE ( 'NONE', *, *, #18381, .F. ) ;
#38711=CARTESIAN_POINT ( 'NONE',  ( 0.000000000000000000, 0.8261519478431083030, 77.49459641780886443 ) ) ;
#38713=DIRECTION ( 'NONE',  ( 0.000000000000000000, 0.000000000000000000, 1.000000000000000000 ) ) ;
#38719=DIRECTION ( 'NONE',  ( 0.000000000000000000, 0.000000000000000000, 1.000000000000000000 ) ) ;
#38720=ORIENTED_EDGE ( 'NONE', *, *, #46259, .T. ) ;
#38722=DIRECTION ( 'NONE',  ( 0.000000000000000000, 0.000000000000000000, 1.000000000000000000 ) ) ;
#38725=AXIS2_PLACEMENT_3D ( 'NONE', #42618, #39172, #28643 ) ;
#38726=DIRECTION ( 'NONE',  ( 0.000000000000000000, 0.000000000000000000, 1.000000000000000000 ) ) ;
#38727=CARTESIAN_POINT ( 'NONE',  ( 10.00000000000000000, -39.78640506895559525, -66.50666863322042843 ) ) ;
#38729=DIRECTION ( 'NONE',  ( -1.000000000000000000, 0.000000000000000000, 0.000000000000000000 ) ) ;
#38732=VERTEX_POINT ( 'NONE', #17164 ) ;
#38733=ORIENTED_EDGE ( 'NONE', *, *, #28713, .T. ) ;
#38755=AXIS2_PLACEMENT_3D ( 'NONE', #47816, #29234, #14301 ) ;
#38762=ORIENTED_EDGE ( 'NONE', *, *, #11353, .F. ) ;
#38763=DIRECTION ( 'NONE',  ( -1.000000000000000000, 0.000000000000000000, 0.000000000000000000 ) ) ;
#38764=EDGE_LOOP ( 'NONE', ( #33363, #10748, #33643, #32311 ) ) ;
#38767=LINE ( 'NONE', #8165, #20786 ) ;
#38769=VECTOR ( 'NONE', #13674, 1000.000000000000000 ) ;
#38771=DIRECTION ( 'NONE',  ( 1.000000000000000000, -0.000000000000000000, -0.000000000000000000 ) ) ;
#38777=CARTESIAN_POINT ( 'NONE',  ( 10.00000000000000000, 80.28980883073779751, -16.65972982744850839 ) ) ;
#38778=CARTESIAN_POINT ( 'NONE',  ( 10.00000000000000000, -73.44644590900078640, 24.73286445877676343 ) ) ;
#38782=DIRECTION ( 'NONE',  ( 0.000000000000000000, 0.7071067811865487940, -0.7071067811865462405 ) ) ;
#38791=AXIS2_PLACEMENT_3D ( 'NONE', #33089, #22068, #37493 ) ;
#38796=ADVANCED_FACE ( 'NONE', ( #13983 ), #31047, .T. ) ;
#38802=EDGE_LOOP ( 'NONE', ( #22085, #24451, #35926, #13910 ) ) ;
#38803=EDGE_CURVE ( 'NONE', #2295, #31513, #19549, .T. ) ;
#38811=ORIENTED_EDGE ( 'NONE', *, *, #42885, .F. ) ;
#38813=ORIENTED_EDGE ( 'NONE', *, *, #40179, .T. ) ;
#38815=EDGE_CURVE ( 'NONE', #30126, #39866, #13326, .T. ) ;
#38817=CARTESIAN_POINT ( 'NONE',  ( 5.000000000000002665, -71.21200624218825226, 40.65526001592589722 ) ) ;
#38820=ORIENTED_EDGE ( 'NONE', *, *, #7949, .T. ) ;
#38821=ORIENTED_EDGE ( 'NONE', *, *, #40061, .T. ) ;
#38823=ORIENTED_EDGE ( 'NONE', *, *, #44797, .F. ) ;
#38824=CARTESIAN_POINT ( 'NONE',  ( 10.00000000000000000, -71.91182617369207719, 28.89263327155721228 ) ) ;
#38830=DIRECTION ( 'NONE',  ( 0.000000000000000000, 0.000000000000000000, 1.000000000000000000 ) ) ;
#38833=DIRECTION ( 'NONE',  ( 0.000000000000000000, 0.000000000000000000, -1.000000000000000000 ) ) ;
#38846=DIRECTION ( 'NONE',  ( -1.000000000000000000, 0.000000000000000000, 0.000000000000000000 ) ) ;
#38850=CARTESIAN_POINT ( 'NONE',  ( 0.000000000000000000, -20.40083707022935400, 72.35432306680478121 ) ) ;
#38853=VERTEX_POINT ( 'NONE', #23432 ) ;
#38860=CIRCLE ( 'NONE', #33362, 31.99999999999998579 ) ;
#38862=FACE_OUTER_BOUND ( 'NONE', #11100, .T. ) ;
#38871=ORIENTED_EDGE ( 'NONE', *, *, #6209, .T. ) ;
#38884=DIRECTION ( 'NONE',  ( -1.000000000000000000, 0.000000000000000000, 0.000000000000000000 ) ) ;
#38885=ORIENTED_EDGE ( 'NONE', *, *, #7746, .T. ) ;
#38891=VERTEX_POINT ( 'NONE', #16115 ) ;
#38892=CARTESIAN_POINT ( 'NONE',  ( 10.00000000000000000, 81.90746397400394585, -3.894527615416976118 ) ) ;
#38893=ORIENTED_EDGE ( 'NONE', *, *, #20974, .T. ) ;
#38895=VECTOR ( 'NONE', #22925, 1000.000000000000000 ) ;
#38896=CARTESIAN_POINT ( 'NONE',  ( 0.000000000000000000, 0.000000000000000000, 0.000000000000000000 ) ) ;
#38897=LINE ( 'NONE', #41838, #15967 ) ;
#38902=DIRECTION ( 'NONE',  ( 0.000000000000000000, 0.000000000000000000, 1.000000000000000000 ) ) ;
#38903=CYLINDRICAL_SURFACE ( 'NONE', #34022, 31.99999999999999289 ) ;
#38905=CARTESIAN_POINT ( 'NONE',  ( 0.000000000000000000, -41.76106447765443619, -62.50884508063471401 ) ) ;
#38908=CIRCLE ( 'NONE', #24049, 77.49899999999999523 ) ;
#38913=DIRECTION ( 'NONE',  ( 0.000000000000000000, -0.5877852522924625900, -0.8090169943749551118 ) ) ;
#38914=EDGE_CURVE ( 'NONE', #26793, #14170, #36785, .T. ) ;
#38916=EDGE_CURVE ( 'NONE', #42004, #12188, #837, .T. ) ;
#38917=AXIS2_PLACEMENT_3D ( 'NONE', #28448, #38763, #13053 ) ;
#38919=CARTESIAN_POINT ( 'NONE',  ( 10.00000000000000000, -27.74655509720617275, -77.16300072079690153 ) ) ;
#38922=VERTEX_POINT ( 'NONE', #28085 ) ;
#38926=CARTESIAN_POINT ( 'NONE',  ( 0.000000000000000000, 55.20638768913760686, 51.02545421589343988 ) ) ;
#38932=CARTESIAN_POINT ( 'NONE',  ( 10.00000000000000000, -62.20884554313985149, -46.21855187248698371 ) ) ;
#38936=ORIENTED_EDGE ( 'NONE', *, *, #35025, .T. ) ;
#38942=CARTESIAN_POINT ( 'NONE',  ( 10.00000000000000000, 0.000000000000000000, 0.000000000000000000 ) ) ;
#38944=DIRECTION ( 'NONE',  ( -1.000000000000000000, -0.000000000000000000, 0.000000000000000000 ) ) ;
#38946=ORIENTED_EDGE ( 'NONE', *, *, #43755, .F. ) ;
#38948=CARTESIAN_POINT ( 'NONE',  ( 0.000000000000000000, 41.19522573413826194, -65.64334221924865176 ) ) ;
#38949=CARTESIAN_POINT ( 'NONE',  ( 0.000000000000000000, -59.03961581697367933, -46.53671651294010303 ) ) ;
#38954=DIRECTION ( 'NONE',  ( 0.000000000000000000, 0.1564344650402311743, -0.9876883405951377704 ) ) ;
#38955=ADVANCED_FACE ( 'NONE', ( #12673 ), #2141, .T. ) ;
#38965=VERTEX_POINT ( 'NONE', #24398 ) ;
#38967=DIRECTION ( 'NONE',  ( 1.000000000000000000, 0.000000000000000000, 0.000000000000000000 ) ) ;
#38969=DIRECTION ( 'NONE',  ( 0.000000000000000000, 0.000000000000000000, 1.000000000000000000 ) ) ;
#38972=DIRECTION ( 'NONE',  ( -1.000000000000000000, 0.000000000000000000, 0.000000000000000000 ) ) ;
#38979=VERTEX_POINT ( 'NONE', #27861 ) ;
#38983=ORIENTED_EDGE ( 'NONE', *, *, #29985, .F. ) ;
#38986=VECTOR ( 'NONE', #12475, 1000.000000000000000 ) ;
#38987=CIRCLE ( 'NONE', #43661, 77.49899999999999523 ) ;
#38991=DIRECTION ( 'NONE',  ( 0.000000000000000000, 0.7604059656000323741, -0.6494480483301819929 ) ) ;
#38995=ORIENTED_EDGE ( 'NONE', *, *, #2270, .T. ) ;
#39009=DIRECTION ( 'NONE',  ( 0.000000000000000000, 0.000000000000000000, 1.000000000000000000 ) ) ;
#39010=CARTESIAN_POINT ( 'NONE',  ( 0.000000000000000000, -59.46389618801928378, -49.70050353004953791 ) ) ;
#39011=DIRECTION ( 'NONE',  ( 0.000000000000000000, 0.000000000000000000, -1.000000000000000000 ) ) ;
#39012=CARTESIAN_POINT ( 'NONE',  ( 10.00000000000000000, 0.000000000000000000, 0.000000000000000000 ) ) ;
#39014=VERTEX_POINT ( 'NONE', #1906 ) ;
#39017=ORIENTED_EDGE ( 'NONE', *, *, #24458, .F. ) ;
#39019=CARTESIAN_POINT ( 'NONE',  ( 0.000000000000000000, -26.02418014898359289, 70.52718814184250107 ) ) ;
#39022=CARTESIAN_POINT ( 'NONE',  ( 0.000000000000000000, 65.59268652807210742, 36.72794159290264560 ) ) ;
#39023=ORIENTED_EDGE ( 'NONE', *, *, #2379, .T. ) ;
#39030=CARTESIAN_POINT ( 'NONE',  ( 5.000000000000000000, -77.16300072079681627, 27.74655509720641078 ) ) ;
#39031=FACE_OUTER_BOUND ( 'NONE', #42707, .T. ) ;
#39032=CARTESIAN_POINT ( 'NONE',  ( 10.00000000000000000, 28.89263327155746097, 71.91182617369197771 ) ) ;
#39038=EDGE_LOOP ( 'NONE', ( #42073, #29812, #33305, #8383 ) ) ;
#39047=ORIENTED_EDGE ( 'NONE', *, *, #10211, .F. ) ;
#39052=CYLINDRICAL_SURFACE ( 'NONE', #5008, 77.49899999999999523 ) ;
#39053=DIRECTION ( 'NONE',  ( -1.000000000000000000, -0.000000000000000000, 0.000000000000000000 ) ) ;
#39054=CARTESIAN_POINT ( 'NONE',  ( 10.00000000000000000, 0.8261519478431083030, 77.49459641780886443 ) ) ;
#39060=CARTESIAN_POINT ( 'NONE',  ( 10.00000000000000000, -50.23322058963393033, 64.81221759200326460 ) ) ;
#39063=AXIS2_PLACEMENT_3D ( 'NONE', #48306, #10869, #25778 ) ;
#39072=CARTESIAN_POINT ( 'NONE',  ( 10.00000000000000000, 44.88180994100468268, -63.18004540532978552 ) ) ;
#39082=AXIS2_PLACEMENT_3D ( 'NONE', #7178, #29691, #29460 ) ;
#39085=FACE_OUTER_BOUND ( 'NONE', #36834, .T. ) ;
#39091=DIRECTION ( 'NONE',  ( 0.000000000000000000, 0.000000000000000000, 1.000000000000000000 ) ) ;
#39092=ORIENTED_EDGE ( 'NONE', *, *, #12606, .F. ) ;
#39094=VERTEX_POINT ( 'NONE', #25357 ) ;
#39095=DIRECTION ( 'NONE',  ( -1.000000000000000000, -0.000000000000000000, -0.000000000000000000 ) ) ;
#39098=CARTESIAN_POINT ( 'NONE',  ( 10.00000000000000000, 0.000000000000000000, 0.000000000000000000 ) ) ;
#39100=VERTEX_POINT ( 'NONE', #17775 ) ;
#39105=DIRECTION ( 'NONE',  ( 0.000000000000000000, 0.000000000000000000, 1.000000000000000000 ) ) ;
#39107=FACE_OUTER_BOUND ( 'NONE', #230, .T. ) ;
#39115=EDGE_CURVE ( 'NONE', #7784, #24221, #36138, .T. ) ;
#39119=ORIENTED_EDGE ( 'NONE', *, *, #36720, .T. ) ;
#39121=EDGE_CURVE ( 'NONE', #9352, #16510, #36024, .T. ) ;
#39123=DIRECTION ( 'NONE',  ( 0.000000000000000000, -6.982962677686266711E-15, 1.000000000000000000 ) ) ;
#39126=EDGE_CURVE ( 'NONE', #40831, #38630, #3322, .T. ) ;
#39129=DIRECTION ( 'NONE',  ( -1.000000000000000000, 0.000000000000000000, 0.000000000000000000 ) ) ;
#39135=CYLINDRICAL_SURFACE ( 'NONE', #36263, 82.00000000000000000 ) ;
#39146=VECTOR ( 'NONE', #31680, 1000.000000000000000 ) ;
#39149=CIRCLE ( 'NONE', #3175, 31.99999999999998579 ) ;
#39150=CIRCLE ( 'NONE', #19595, 32.00000000000000000 ) ;
#39160=DIRECTION ( 'NONE',  ( -1.000000000000000000, 0.000000000000000000, -0.000000000000000000 ) ) ;
#39165=EDGE_LOOP ( 'NONE', ( #31808, #18082, #9405, #2343 ) ) ;
#39167=FACE_OUTER_BOUND ( 'NONE', #2854, .T. ) ;
#39168=CYLINDRICAL_SURFACE ( 'NONE', #24854, 32.00000000000000000 ) ;
#39172=DIRECTION ( 'NONE',  ( -1.000000000000000000, -0.000000000000000000, -0.000000000000000000 ) ) ;
#39173=ORIENTED_EDGE ( 'NONE', *, *, #32184, .F. ) ;
#39176=CARTESIAN_POINT ( 'NONE',  ( 0.000000000000000000, -31.47745569255189224, 68.26794271651249346 ) ) ;
#39178=DIRECTION ( 'NONE',  ( -1.000000000000000000, 0.000000000000000000, -0.000000000000000000 ) ) ;
#39179=ADVANCED_FACE ( 'NONE', ( #6774 ), #40779, .T. ) ;
#39180=CARTESIAN_POINT ( 'NONE',  ( 0.000000000000000000, 2.956366410621684260, -75.11725578898465017 ) ) ;
#39183=ORIENTED_EDGE ( 'NONE', *, *, #32927, .T. ) ;
#39187=DIRECTION ( 'NONE',  ( 0.000000000000000000, -0.6494480483301903195, 0.7604059656000252687 ) ) ;
#39189=CIRCLE ( 'NONE', #34482, 82.00000000000000000 ) ;
#39198=EDGE_CURVE ( 'NONE', #13864, #24652, #16506, .T. ) ;
#39211=DIRECTION ( 'NONE',  ( -1.000000000000000000, -0.000000000000000000, -0.000000000000000000 ) ) ;
#39214=DIRECTION ( 'NONE',  ( 0.000000000000000000, -0.5877852522924802425, 0.8090169943749422332 ) ) ;
#39216=ORIENTED_EDGE ( 'NONE', *, *, #46858, .T. ) ;
#39218=AXIS2_PLACEMENT_3D ( 'NONE', #979, #30610, #15929 ) ;
#39219=ORIENTED_EDGE ( 'NONE', *, *, #34986, .F. ) ;
#39223=CARTESIAN_POINT ( 'NONE',  ( 10.00000000000000000, -11.30684508768284680, -76.66974797899850103 ) ) ;
#39228=DIRECTION ( 'NONE',  ( -1.000000000000000000, 0.000000000000000000, 0.000000000000000000 ) ) ;
#39229=ORIENTED_EDGE ( 'NONE', *, *, #6098, .T. ) ;
#39230=EDGE_CURVE ( 'NONE', #13774, #7495, #14842, .T. ) ;
#39234=DIRECTION ( 'NONE',  ( 0.000000000000000000, 0.000000000000000000, 1.000000000000000000 ) ) ;
#39237=ORIENTED_EDGE ( 'NONE', *, *, #20974, .F. ) ;
#39241=CARTESIAN_POINT ( 'NONE',  ( 0.000000000000000000, 0.000000000000000000, 0.000000000000000000 ) ) ;
#39246=EDGE_CURVE ( 'NONE', #42000, #34549, #33715, .T. ) ;
#39247=CARTESIAN_POINT ( 'NONE',  ( 5.000000000000000000, 60.67117009219135326, 55.16347631943062169 ) ) ;
#39248=FACE_OUTER_BOUND ( 'NONE', #44763, .T. ) ;
#39250=ORIENTED_EDGE ( 'NONE', *, *, #11543, .T. ) ;
#39254=DIRECTION ( 'NONE',  ( 0.000000000000000000, 0.7071067811865436870, 0.7071067811865512365 ) ) ;
#39258=ORIENTED_EDGE ( 'NONE', *, *, #28519, .T. ) ;
#39261=ORIENTED_EDGE ( 'NONE', *, *, #36779, .T. ) ;
#39275=CYLINDRICAL_SURFACE ( 'NONE', #31404, 77.49899999999999523 ) ;
#39285=CARTESIAN_POINT ( 'NONE',  ( 0.000000000000000000, -8.830959090341869100, -74.65491531819127147 ) ) ;
#39289=CARTESIAN_POINT ( 'NONE',  ( 10.00000000000000000, -65.64334221924882229, -41.19522573413803457 ) ) ;
#39293=CARTESIAN_POINT ( 'NONE',  ( 10.00000000000000000, 0.000000000000000000, 0.000000000000000000 ) ) ;
#39297=AXIS2_PLACEMENT_3D ( 'NONE', #46162, #20204, #12627 ) ;
#39303=CYLINDRICAL_SURFACE ( 'NONE', #37640, 77.49899999999999523 ) ;
#39306=CARTESIAN_POINT ( 'NONE',  ( 10.00000000000000000, -66.50666863322028632, 39.78640506895582973 ) ) ;
#39307=DIRECTION ( 'NONE',  ( -1.000000000000000000, -0.000000000000000000, 0.000000000000000000 ) ) ;
#39310=DIRECTION ( 'NONE',  ( 0.000000000000000000, -0.5877852522924625900, -0.8090169943749551118 ) ) ;
#39314=CYLINDRICAL_SURFACE ( 'NONE', #47088, 82.00000000000000000 ) ;
#39322=CIRCLE ( 'NONE', #3316, 31.99999999999999289 ) ;
#39323=CARTESIAN_POINT ( 'NONE',  ( 0.000000000000000000, -18.89407956138310496, 75.16055320797023853 ) ) ;
#39326=ORIENTED_EDGE ( 'NONE', *, *, #34640, .F. ) ;
#39330=DIRECTION ( 'NONE',  ( -1.000000000000000000, 0.000000000000000000, 0.000000000000000000 ) ) ;
#39334=EDGE_LOOP ( 'NONE', ( #21322, #40070, #39183, #5671 ) ) ;
#39338=LINE ( 'NONE', #24653, #3213 ) ;
#39346=CARTESIAN_POINT ( 'NONE',  ( 10.00000000000000000, 62.20884554314020676, 46.21855187248652896 ) ) ;
#39355=CARTESIAN_POINT ( 'NONE',  ( 10.00000000000000000, -50.95692526931286181, -58.39081064771806240 ) ) ;
#39359=ADVANCED_FACE ( 'NONE', ( #5755 ), #16773, .T. ) ;
#39364=DIRECTION ( 'NONE',  ( 0.000000000000000000, 0.000000000000000000, 1.000000000000000000 ) ) ;
#39368=ADVANCED_FACE ( 'NONE', ( #46383 ), #42959, .T. ) ;
#39369=CARTESIAN_POINT ( 'NONE',  ( 10.00000000000000000, 68.55367621811141987, 44.99326035066078333 ) ) ;
#39375=CIRCLE ( 'NONE', #1064, 77.49900000000000944 ) ;
#39376=CARTESIAN_POINT ( 'NONE',  ( 0.000000000000000000, 0.000000000000000000, 0.000000000000000000 ) ) ;
#39381=DIRECTION ( 'NONE',  ( 0.000000000000000000, 0.000000000000000000, 1.000000000000000000 ) ) ;
#39384=ORIENTED_EDGE ( 'NONE', *, *, #3755, .F. ) ;
#39386=LINE ( 'NONE', #1462, #38986 ) ;
#39390=CIRCLE ( 'NONE', #3418, 77.49900000000000944 ) ;
#39392=DIRECTION ( 'NONE',  ( -1.000000000000000000, 0.000000000000000000, -0.000000000000000000 ) ) ;
#39395=AXIS2_PLACEMENT_3D ( 'NONE', #3290, #47838, #6499 ) ;
#39396=EDGE_CURVE ( 'NONE', #18013, #25055, #17000, .T. ) ;
#39398=VERTEX_POINT ( 'NONE', #28261 ) ;
#39414=ORIENTED_EDGE ( 'NONE', *, *, #39740, .T. ) ;
#39415=EDGE_CURVE ( 'NONE', #33470, #44331, #45433, .T. ) ;
#39421=DIRECTION ( 'NONE',  ( -1.000000000000000000, 0.000000000000000000, 0.000000000000000000 ) ) ;
#39429=FACE_OUTER_BOUND ( 'NONE', #18968, .T. ) ;
#39432=DIRECTION ( 'NONE',  ( -1.000000000000000000, 0.000000000000000000, 0.000000000000000000 ) ) ;
#39434=DIRECTION ( 'NONE',  ( -1.000000000000000000, -0.000000000000000000, -0.000000000000000000 ) ) ;
#39436=CIRCLE ( 'NONE', #12050, 82.00000000000000000 ) ;
#39439=DIRECTION ( 'NONE',  ( -1.000000000000000000, -0.000000000000000000, 0.000000000000000000 ) ) ;
#39446=VECTOR ( 'NONE', #32697, 1000.000000000000000 ) ;
#39451=VECTOR ( 'NONE', #19023, 1000.000000000000000 ) ;
#39453=VECTOR ( 'NONE', #13118, 1000.000000000000000 ) ;
#39455=VERTEX_POINT ( 'NONE', #12379 ) ;
#39456=EDGE_CURVE ( 'NONE', #45729, #30299, #42322, .T. ) ;
#39460=ADVANCED_FACE ( 'NONE', ( #46635 ), #39275, .T. ) ;
#39463=EDGE_CURVE ( 'NONE', #23327, #32575, #7896, .T. ) ;
#39465=CARTESIAN_POINT ( 'NONE',  ( 0.000000000000000000, 0.000000000000000000, 0.000000000000000000 ) ) ;
#39479=FACE_OUTER_BOUND ( 'NONE', #24774, .T. ) ;
#39488=CYLINDRICAL_SURFACE ( 'NONE', #47211, 77.49899999999999523 ) ;
#39489=CARTESIAN_POINT ( 'NONE',  ( 10.00000000000000000, -80.28980883073744224, -16.65972982745018882 ) ) ;
#39490=DIRECTION ( 'NONE',  ( -1.000000000000000000, 0.000000000000000000, -0.000000000000000000 ) ) ;
#39493=CIRCLE ( 'NONE', #1182, 82.00000000000000000 ) ;
#39495=FACE_OUTER_BOUND ( 'NONE', #39672, .T. ) ;
#39500=DIRECTION ( 'NONE',  ( -1.000000000000000000, 0.000000000000000000, 0.000000000000000000 ) ) ;
#39508=ORIENTED_EDGE ( 'NONE', *, *, #42083, .T. ) ;
#39511=EDGE_LOOP ( 'NONE', ( #45274, #16852, #3820, #45597 ) ) ;
#39513=CIRCLE ( 'NONE', #21500, 31.99999999999999289 ) ;
#39516=AXIS2_PLACEMENT_3D ( 'NONE', #23802, #9349, #20128 ) ;
#39518=EDGE_CURVE ( 'NONE', #36114, #34421, #875, .T. ) ;
#39519=CIRCLE ( 'NONE', #30896, 31.99999999999999289 ) ;
#39523=ORIENTED_EDGE ( 'NONE', *, *, #35324, .T. ) ;
#39529=CARTESIAN_POINT ( 'NONE',  ( 10.00000000000000000, -34.44570377933649041, 69.42325613327427902 ) ) ;
#39531=EDGE_CURVE ( 'NONE', #21412, #39579, #48068, .T. ) ;
#39532=LINE ( 'NONE', #3256, #10141 ) ;
#39534=VERTEX_POINT ( 'NONE', #36330 ) ;
#39542=DIRECTION ( 'NONE',  ( 0.000000000000000000, -0.5224985647159560154, 0.8526401643540879594 ) ) ;
#39544=VERTEX_POINT ( 'NONE', #32886 ) ;
#39551=DIRECTION ( 'NONE',  ( 0.000000000000000000, 0.5224985647159500202, -0.8526401643540915121 ) ) ;
#39556=DIRECTION ( 'NONE',  ( 0.000000000000000000, 0.8910065241883657894, 0.4539904997395510788 ) ) ;
#39558=EDGE_CURVE ( 'NONE', #23195, #22033, #2446, .T. ) ;
#39559=CARTESIAN_POINT ( 'NONE',  ( 0.000000000000000000, 0.000000000000000000, 0.000000000000000000 ) ) ;
#39564=CARTESIAN_POINT ( 'NONE',  ( 10.00000000000000000, -65.59268652807183742, -36.72794159290312166 ) ) ;
#39565=FACE_OUTER_BOUND ( 'NONE', #22973, .T. ) ;
#39579=VERTEX_POINT ( 'NONE', #25775 ) ;
#39584=DIRECTION ( 'NONE',  ( 0.000000000000000000, -0.8090169943749532244, 0.5877852522924652545 ) ) ;
#39586=EDGE_CURVE ( 'NONE', #6313, #18371, #18092, .T. ) ;
#39590=DIRECTION ( 'NONE',  ( 0.000000000000000000, 0.000000000000000000, -1.000000000000000000 ) ) ;
#39591=LINE ( 'NONE', #10189, #3477 ) ;
#39599=ORIENTED_EDGE ( 'NONE', *, *, #1036, .T. ) ;
#39604=AXIS2_PLACEMENT_3D ( 'NONE', #6652, #25958, #29149 ) ;
#39605=VERTEX_POINT ( 'NONE', #18189 ) ;
#39606=DIRECTION ( 'NONE',  ( -1.000000000000000000, 0.000000000000000000, -0.000000000000000000 ) ) ;
#39610=CIRCLE ( 'NONE', #41077, 77.49900000000000944 ) ;
#39613=DIRECTION ( 'NONE',  ( -1.000000000000000000, 0.000000000000000000, 0.000000000000000000 ) ) ;
#39622=DIRECTION ( 'NONE',  ( -1.000000000000000000, -0.000000000000000000, -0.000000000000000000 ) ) ;
#39626=LINE ( 'NONE', #28109, #20074 ) ;
#39628=EDGE_LOOP ( 'NONE', ( #30508, #43555, #11224, #43438 ) ) ;
#39631=CYLINDRICAL_SURFACE ( 'NONE', #4384, 77.49899999999999523 ) ;
#39632=ORIENTED_EDGE ( 'NONE', *, *, #2858, .T. ) ;
#39634=CARTESIAN_POINT ( 'NONE',  ( 0.000000000000000000, 8.966570791701863996, -81.50828551894218776 ) ) ;
#39637=EDGE_LOOP ( 'NONE', ( #2593, #44070, #784, #19992 ) ) ;
#39645=DIRECTION ( 'NONE',  ( -1.000000000000000000, -0.000000000000000000, -0.000000000000000000 ) ) ;
#39647=AXIS2_PLACEMENT_3D ( 'NONE', #41480, #37075, #105 ) ;
#39650=DIRECTION ( 'NONE',  ( -1.000000000000000000, 0.000000000000000000, 0.000000000000000000 ) ) ;
#39651=ORIENTED_EDGE ( 'NONE', *, *, #317, .F. ) ;
#39653=ORIENTED_EDGE ( 'NONE', *, *, #8180, .F. ) ;
#39655=ORIENTED_EDGE ( 'NONE', *, *, #42451, .F. ) ;
#39658=VERTEX_POINT ( 'NONE', #45347 ) ;
#39659=ORIENTED_EDGE ( 'NONE', *, *, #19067, .T. ) ;
#39662=CARTESIAN_POINT ( 'NONE',  ( 10.00000000000000000, 59.03342792756263435, 46.54456581323825048 ) ) ;
#39672=EDGE_LOOP ( 'NONE', ( #37352, #8320, #31720, #9524 ) ) ;
#39681=CIRCLE ( 'NONE', #35779, 31.99999999999999289 ) ;
#39685=DIRECTION ( 'NONE',  ( -1.000000000000000000, 0.000000000000000000, -0.000000000000000000 ) ) ;
#39689=LINE ( 'NONE', #13732, #11589 ) ;
#39692=CARTESIAN_POINT ( 'NONE',  ( 10.00000000000000000, 0.000000000000000000, 0.000000000000000000 ) ) ;
#39696=DIRECTION ( 'NONE',  ( 1.000000000000000000, -0.000000000000000000, -0.000000000000000000 ) ) ;
#39698=AXIS2_PLACEMENT_3D ( 'NONE', #31256, #14263, #35384 ) ;
#39702=ADVANCED_FACE ( 'NONE', ( #3759 ), #29944, .T. ) ;
#39705=AXIS2_PLACEMENT_3D ( 'NONE', #27105, #12895, #5787 ) ;
#39708=VERTEX_POINT ( 'NONE', #26285 ) ;
#39721=DIRECTION ( 'NONE',  ( -1.000000000000000000, 0.000000000000000000, 0.000000000000000000 ) ) ;
#39722=DIRECTION ( 'NONE',  ( -1.000000000000000000, 0.000000000000000000, 0.000000000000000000 ) ) ;
#39724=CYLINDRICAL_SURFACE ( 'NONE', #38917, 32.00000000000000000 ) ;
#39734=DIRECTION ( 'NONE',  ( -1.000000000000000000, 0.000000000000000000, -0.000000000000000000 ) ) ;
#39740=EDGE_CURVE ( 'NONE', #14155, #8812, #37528, .T. ) ;
#39743=DIRECTION ( 'NONE',  ( 1.000000000000000000, -0.000000000000000000, -0.000000000000000000 ) ) ;
#39750=ORIENTED_EDGE ( 'NONE', *, *, #23213, .T. ) ;
#39751=VECTOR ( 'NONE', #12158, 1000.000000000000000 ) ;
#39754=EDGE_LOOP ( 'NONE', ( #32143, #26690, #38383, #28965 ) ) ;
#39764=VERTEX_POINT ( 'NONE', #37046 ) ;
#39776=CARTESIAN_POINT ( 'NONE',  ( 10.00000000000000000, 62.20884554314086046, -46.21855187248561236 ) ) ;
#39777=AXIS2_PLACEMENT_3D ( 'NONE', #8837, #38729, #291 ) ;
#39779=DIRECTION ( 'NONE',  ( 0.000000000000000000, 0.6494480483301793283, 0.7604059656000345946 ) ) ;
#39781=DIRECTION ( 'NONE',  ( -1.000000000000000000, -0.000000000000000000, -0.000000000000000000 ) ) ;
#39783=DIRECTION ( 'NONE',  ( -1.000000000000000000, 0.000000000000000000, -0.000000000000000000 ) ) ;
#39796=AXIS2_PLACEMENT_3D ( 'NONE', #30758, #37612, #4804 ) ;
#39805=EDGE_CURVE ( 'NONE', #46337, #26870, #22009, .T. ) ;
#39806=DIRECTION ( 'NONE',  ( 0.000000000000000000, 0.000000000000000000, 1.000000000000000000 ) ) ;
#39808=VERTEX_POINT ( 'NONE', #38499 ) ;
#39810=EDGE_CURVE ( 'NONE', #4186, #23327, #899, .T. ) ;
#39815=ORIENTED_EDGE ( 'NONE', *, *, #36034, .T. ) ;
#39818=VECTOR ( 'NONE', #46340, 1000.000000000000000 ) ;
#39821=CARTESIAN_POINT ( 'NONE',  ( 0.000000000000000000, 30.41916302227113178, 71.27951684758036777 ) ) ;
#39831=ORIENTED_EDGE ( 'NONE', *, *, #882, .T. ) ;
#39832=ORIENTED_EDGE ( 'NONE', *, *, #34856, .T. ) ;
#39835=VERTEX_POINT ( 'NONE', #19880 ) ;
#39838=CARTESIAN_POINT ( 'NONE',  ( 0.000000000000000000, 0.000000000000000000, 2.500000000000000000 ) ) ;
#39850=CARTESIAN_POINT ( 'NONE',  ( 10.00000000000000000, 0.000000000000000000, 0.000000000000000000 ) ) ;
#39852=EDGE_CURVE ( 'NONE', #17581, #36114, #23811, .T. ) ;
#39857=AXIS2_PLACEMENT_3D ( 'NONE', #45399, #8206, #11416 ) ;
#39858=CARTESIAN_POINT ( 'NONE',  ( 10.00000000000000000, 0.000000000000000000, 0.000000000000000000 ) ) ;
#39862=( NAMED_UNIT ( * ) PLANE_ANGLE_UNIT ( ) SI_UNIT ( $, .RADIAN. ) );
#39863=CIRCLE ( 'NONE', #46223, 77.49899999999998101 ) ;
#39865=ORIENTED_EDGE ( 'NONE', *, *, #9505, .T. ) ;
#39866=VERTEX_POINT ( 'NONE', #27980 ) ;
#39867=CIRCLE ( 'NONE', #13311, 32.00000000000000000 ) ;
#39868=DIRECTION ( 'NONE',  ( 0.000000000000000000, 0.000000000000000000, 1.000000000000000000 ) ) ;
#39869=FACE_OUTER_BOUND ( 'NONE', #14307, .T. ) ;
#39870=VERTEX_POINT ( 'NONE', #9356 ) ;
#39872=CARTESIAN_POINT ( 'NONE',  ( 5.000000000000002665, 71.87247863392414615, 39.47590169984871267 ) ) ;
#39877=VECTOR ( 'NONE', #3568, 1000.000000000000000 ) ;
#39878=DIRECTION ( 'NONE',  ( -1.000000000000000000, 0.000000000000000000, 0.000000000000000000 ) ) ;
#39882=VERTEX_POINT ( 'NONE', #15427 ) ;
#39885=CARTESIAN_POINT ( 'NONE',  ( 10.00000000000000000, -23.16143007188481207, 73.95703589263968070 ) ) ;
#39887=ORIENTED_EDGE ( 'NONE', *, *, #27844, .F. ) ;
#39890=VERTEX_POINT ( 'NONE', #38179 ) ;
#39900=ORIENTED_EDGE ( 'NONE', *, *, #4810, .F. ) ;
#39902=CARTESIAN_POINT ( 'NONE',  ( 0.000000000000000000, 11.30684508768339569, 76.66974797899841576 ) ) ;
#39907=DIRECTION ( 'NONE',  ( -1.000000000000000000, -0.000000000000000000, 0.000000000000000000 ) ) ;
#39908=CARTESIAN_POINT ( 'NONE',  ( 0.000000000000000000, 70.53064760720278059, 26.01480285779964774 ) ) ;
#39912=ADVANCED_FACE ( 'NONE', ( #41139 ), #30118, .T. ) ;
#39917=CARTESIAN_POINT ( 'NONE',  ( -10.00000000000000000, 0.000000000000000000, 0.000000000000000000 ) ) ;
#39920=AXIS2_PLACEMENT_3D ( 'NONE', #19651, #816, #35078 ) ;
#39924=AXIS2_PLACEMENT_3D ( 'NONE', #37219, #3688, #14953 ) ;
#39926=CARTESIAN_POINT ( 'NONE',  ( 0.000000000000000000, -35.91791733033525702, 68.67312586194982771 ) ) ;
#39929=CIRCLE ( 'NONE', #9410, 32.00000000000000000 ) ;
#39931=AXIS2_PLACEMENT_3D ( 'NONE', #6791, #13892, #35911 ) ;
#39932=CARTESIAN_POINT ( 'NONE',  ( 5.000000000000002665, -16.65972982744877484, -80.28980883073775487 ) ) ;
#39939=CARTESIAN_POINT ( 'NONE',  ( 10.00000000000000000, 31.46837873495072913, -68.27212725128242710 ) ) ;
#39941=EDGE_LOOP ( 'NONE', ( #32669, #38871, #1765, #18131 ) ) ;
#39942=DIRECTION ( 'NONE',  ( 0.000000000000000000, -0.8526401643540859610, -0.5224985647159591240 ) ) ;
#39950=AXIS2_PLACEMENT_3D ( 'NONE', #25249, #5967, #35573 ) ;
#39952=ORIENTED_EDGE ( 'NONE', *, *, #4805, .T. ) ;
#39957=VERTEX_POINT ( 'NONE', #23003 ) ;
#39958=ORIENTED_EDGE ( 'NONE', *, *, #35603, .F. ) ;
#39959=FACE_OUTER_BOUND ( 'NONE', #36289, .T. ) ;
#39960=FACE_OUTER_BOUND ( 'NONE', #24945, .T. ) ;
#39962=EDGE_LOOP ( 'NONE', ( #1629, #16558, #7040, #18109 ) ) ;
#39970=CYLINDRICAL_SURFACE ( 'NONE', #35886, 32.00000000000000000 ) ;
#39971=VECTOR ( 'NONE', #30559, 1000.000000000000000 ) ;
#39979=CARTESIAN_POINT ( 'NONE',  ( 10.00000000000000000, 0.000000000000000000, 0.000000000000000000 ) ) ;
#39984=LINE ( 'NONE', #47325, #26126 ) ;
#39985=ORIENTED_EDGE ( 'NONE', *, *, #10236, .F. ) ;
#39991=VECTOR ( 'NONE', #38107, 1000.000000000000000 ) ;
#39998=ADVANCED_FACE ( 'NONE', ( #22754 ), #227, .T. ) ;
#40002=DIRECTION ( 'NONE',  ( -1.000000000000000000, 0.000000000000000000, 0.000000000000000000 ) ) ;
#40011=DIRECTION ( 'NONE',  ( -1.000000000000000000, -0.000000000000000000, -0.000000000000000000 ) ) ;
#40021=DIRECTION ( 'NONE',  ( 0.000000000000000000, 0.5877852522924742473, -0.8090169943749466741 ) ) ;
#40023=CARTESIAN_POINT ( 'NONE',  ( 0.000000000000000000, -75.11764819372145041, -2.946379043147127064 ) ) ;
#40024=DIRECTION ( 'NONE',  ( 0.000000000000000000, 0.1564344650402242631, 0.9876883405951387696 ) ) ;
#40025=CARTESIAN_POINT ( 'NONE',  ( 10.00000000000000000, -77.32052557432845674, 5.256550761632577284 ) ) ;
#40029=ORIENTED_EDGE ( 'NONE', *, *, #29500, .F. ) ;
#40034=VECTOR ( 'NONE', #9146, 1000.000000000000000 ) ;
#40035=CIRCLE ( 'NONE', #37683, 31.99999999999999289 ) ;
#40040=ORIENTED_EDGE ( 'NONE', *, *, #47311, .T. ) ;
#40043=VERTEX_POINT ( 'NONE', #39529 ) ;
#40047=ORIENTED_EDGE ( 'NONE', *, *, #20633, .T. ) ;
#40050=ORIENTED_EDGE ( 'NONE', *, *, #32488, .T. ) ;
#40058=LINE ( 'NONE', #25111, #41424 ) ;
#40059=ORIENTED_EDGE ( 'NONE', *, *, #45510, .F. ) ;
#40060=ORIENTED_EDGE ( 'NONE', *, *, #15599, .F. ) ;
#40061=EDGE_CURVE ( 'NONE', #18610, #17380, #1828, .T. ) ;
#40062=CIRCLE ( 'NONE', #18938, 32.00000000000000000 ) ;
#40064=DIRECTION ( 'NONE',  ( 0.000000000000000000, 0.9876883405951371042, 0.1564344650402346437 ) ) ;
#40070=ORIENTED_EDGE ( 'NONE', *, *, #43663, .F. ) ;
#40071=DIRECTION ( 'NONE',  ( -1.000000000000000000, 0.000000000000000000, 0.000000000000000000 ) ) ;
#40072=CIRCLE ( 'NONE', #35380, 82.00000000000000000 ) ;
#40073=DIRECTION ( 'NONE',  ( 0.000000000000000000, 0.5877852522924685852, 0.8090169943749507819 ) ) ;
#40083=FACE_OUTER_BOUND ( 'NONE', #22683, .T. ) ;
#40091=CIRCLE ( 'NONE', #40848, 32.00000000000000000 ) ;
#40103=EDGE_LOOP ( 'NONE', ( #23674, #43857, #23259, #30751 ) ) ;
#40110=ORIENTED_EDGE ( 'NONE', *, *, #8115, .T. ) ;
#40116=AXIS2_PLACEMENT_3D ( 'NONE', #40878, #14459, #45276 ) ;
#40117=EDGE_CURVE ( 'NONE', #23147, #40294, #35602, .T. ) ;
#40118=EDGE_CURVE ( 'NONE', #11188, #8273, #13554, .T. ) ;
#40119=AXIS2_PLACEMENT_3D ( 'NONE', #27952, #5187, #45824 ) ;
#40123=ORIENTED_EDGE ( 'NONE', *, *, #31252, .F. ) ;
#40124=DIRECTION ( 'NONE',  ( -1.000000000000000000, -0.000000000000000000, -0.000000000000000000 ) ) ;
#40126=VERTEX_POINT ( 'NONE', #43665 ) ;
#40127=DIRECTION ( 'NONE',  ( 0.000000000000000000, 0.9723699203976756689, 0.2334453638559093047 ) ) ;
#40128=CIRCLE ( 'NONE', #17437, 32.00000000000000000 ) ;
#40129=CIRCLE ( 'NONE', #2583, 77.49899999999999523 ) ;
#40132=AXIS2_PLACEMENT_3D ( 'NONE', #36108, #10162, #6262 ) ;
#40135=DIRECTION ( 'NONE',  ( -1.000000000000000000, -0.000000000000000000, 0.000000000000000000 ) ) ;
#40137=AXIS2_PLACEMENT_3D ( 'NONE', #20653, #5490, #24815 ) ;
#40145=VERTEX_POINT ( 'NONE', #48292 ) ;
#40153=EDGE_CURVE ( 'NONE', #13467, #15723, #15930, .T. ) ;
#40155=DIRECTION ( 'NONE',  ( 0.000000000000000000, 0.000000000000000000, -1.000000000000000000 ) ) ;
#40157=DIRECTION ( 'NONE',  ( 0.000000000000000000, 0.000000000000000000, 1.000000000000000000 ) ) ;
#40158=CYLINDRICAL_SURFACE ( 'NONE', #38681, 77.49899999999999523 ) ;
#40160=ORIENTED_EDGE ( 'NONE', *, *, #6098, .F. ) ;
#40164=CYLINDRICAL_SURFACE ( 'NONE', #35428, 82.00000000000000000 ) ;
#40171=VECTOR ( 'NONE', #40176, 1000.000000000000000 ) ;
#40172=AXIS2_PLACEMENT_3D ( 'NONE', #44367, #3231, #18421 ) ;
#40176=DIRECTION ( 'NONE',  ( -1.000000000000000000, 0.000000000000000000, 0.000000000000000000 ) ) ;
#40178=DIRECTION ( 'NONE',  ( -1.000000000000000000, -0.000000000000000000, 0.000000000000000000 ) ) ;
#40179=EDGE_CURVE ( 'NONE', #44958, #14299, #47159, .T. ) ;
#40184=ADVANCED_FACE ( 'NONE', ( #47562 ), #43901, .T. ) ;
#40189=CARTESIAN_POINT ( 'NONE',  ( -10.00000000000000000, 0.000000000000000000, 0.000000000000000000 ) ) ;
#40196=CIRCLE ( 'NONE', #34684, 82.00000000000000000 ) ;
#40197=CARTESIAN_POINT ( 'NONE',  ( 10.00000000000000000, 72.35160999960844208, -20.41045688087747223 ) ) ;
#40198=ORIENTED_EDGE ( 'NONE', *, *, #6328, .T. ) ;
#40205=AXIS2_PLACEMENT_3D ( 'NONE', #40517, #33169, #26062 ) ;
#40217=AXIS2_PLACEMENT_3D ( 'NONE', #17376, #32327, #47257 ) ;
#40219=CARTESIAN_POINT ( 'NONE',  ( 10.00000000000000000, -49.70050353004846500, -59.46389618802017907 ) ) ;
#40220=CARTESIAN_POINT ( 'NONE',  ( 10.00000000000000000, -24.73286445877757345, 73.44644590900053061 ) ) ;
#40221=CARTESIAN_POINT ( 'NONE',  ( 0.000000000000000000, 0.000000000000000000, 0.000000000000000000 ) ) ;
#40222=AXIS2_PLACEMENT_3D ( 'NONE', #45748, #24190, #43750 ) ;
#40224=CARTESIAN_POINT ( 'NONE',  ( 10.00000000000000000, -8.840884882374576037, -74.65374052328658649 ) ) ;
#40225=DIRECTION ( 'NONE',  ( -1.000000000000000000, 0.000000000000000000, 0.000000000000000000 ) ) ;
#40226=CARTESIAN_POINT ( 'NONE',  ( 0.000000000000000000, 0.000000000000000000, 0.000000000000000000 ) ) ;
#40244=AXIS2_PLACEMENT_3D ( 'NONE', #24391, #39330, #24644 ) ;
#40245=VECTOR ( 'NONE', #40288, 1000.000000000000000 ) ;
#40247=EDGE_LOOP ( 'NONE', ( #44756, #43772, #42813, #47551 ) ) ;
#40253=ORIENTED_EDGE ( 'NONE', *, *, #31577, .T. ) ;
#40257=ORIENTED_EDGE ( 'NONE', *, *, #46212, .F. ) ;
#40267=CARTESIAN_POINT ( 'NONE',  ( 10.00000000000000000, -36.73666225445845157, -65.58780272294114866 ) ) ;
#40277=DIRECTION ( 'NONE',  ( 0.000000000000000000, 0.000000000000000000, 1.000000000000000000 ) ) ;
#40278=AXIS2_PLACEMENT_3D ( 'NONE', #35800, #13523, #28456 ) ;
#40279=DIRECTION ( 'NONE',  ( -1.000000000000000000, 0.000000000000000000, 0.000000000000000000 ) ) ;
#40288=DIRECTION ( 'NONE',  ( -1.000000000000000000, 0.000000000000000000, 0.000000000000000000 ) ) ;
#40289=EDGE_CURVE ( 'NONE', #41512, #46575, #27670, .T. ) ;
#40294=VERTEX_POINT ( 'NONE', #34552 ) ;
#40297=VECTOR ( 'NONE', #43411, 1000.000000000000000 ) ;
#40300=DIRECTION ( 'NONE',  ( 1.000000000000000000, -0.000000000000000000, -0.000000000000000000 ) ) ;
#40309=DIRECTION ( 'NONE',  ( -1.000000000000000000, 0.000000000000000000, 0.000000000000000000 ) ) ;
#40322=ORIENTED_EDGE ( 'NONE', *, *, #13723, .F. ) ;
#40324=ORIENTED_EDGE ( 'NONE', *, *, #41446, .T. ) ;
#40325=LINE ( 'NONE', #25364, #6011 ) ;
#40328=AXIS2_PLACEMENT_3D ( 'NONE', #6969, #29962, #94 ) ;
#40338=ORIENTED_EDGE ( 'NONE', *, *, #40061, .F. ) ;
#40341=AXIS2_PLACEMENT_3D ( 'NONE', #46147, #27541, #42469 ) ;
#40348=CARTESIAN_POINT ( 'NONE',  ( 0.000000000000000000, 80.28980883073781172, -16.65972982744850839 ) ) ;
#40350=EDGE_CURVE ( 'NONE', #3813, #39835, #42523, .T. ) ;
#40351=DIRECTION ( 'NONE',  ( -1.000000000000000000, 0.000000000000000000, -0.000000000000000000 ) ) ;
#40352=AXIS2_PLACEMENT_3D ( 'NONE', #19710, #34647, #45204 ) ;
#40370=CIRCLE ( 'NONE', #5195, 82.00000000000000000 ) ;
#40371=CARTESIAN_POINT ( 'NONE',  ( 0.000000000000000000, -70.52718814184277107, 26.02418014898285037 ) ) ;
#40372=ORIENTED_EDGE ( 'NONE', *, *, #28878, .T. ) ;
#40377=CARTESIAN_POINT ( 'NONE',  ( 10.00000000000000000, 14.66109333815460225, 73.73191006444577056 ) ) ;
#40379=ORIENTED_EDGE ( 'NONE', *, *, #36623, .F. ) ;
#40381=FACE_OUTER_BOUND ( 'NONE', #18026, .T. ) ;
#40390=AXIS2_PLACEMENT_3D ( 'NONE', #39908, #1741, #16666 ) ;
#40395=VECTOR ( 'NONE', #14573, 1000.000000000000000 ) ;
#40405=ORIENTED_EDGE ( 'NONE', *, *, #1219, .F. ) ;
#40419=VERTEX_POINT ( 'NONE', #13269 ) ;
#40420=CARTESIAN_POINT ( 'NONE',  ( 10.00000000000000000, 55.16347631943041563, 60.67117009219156643 ) ) ;
#40421=CIRCLE ( 'NONE', #37303, 31.99999999999999645 ) ;
#40427=DIRECTION ( 'NONE',  ( 0.000000000000000000, 0.07845909572784530439, -0.9969173337331279638 ) ) ;
#40428=ORIENTED_EDGE ( 'NONE', *, *, #17515, .F. ) ;
#40433=VERTEX_POINT ( 'NONE', #8861 ) ;
#40435=CARTESIAN_POINT ( 'NONE',  ( 10.00000000000000000, 35.91791733033475253, 68.67312586195009771 ) ) ;
#40439=DIRECTION ( 'NONE',  ( 0.000000000000000000, -0.1564344650402381687, 0.9876883405951365491 ) ) ;
#40440=VERTEX_POINT ( 'NONE', #9345 ) ;
#40442=ORIENTED_EDGE ( 'NONE', *, *, #5158, .F. ) ;
#40443=ORIENTED_EDGE ( 'NONE', *, *, #25841, .F. ) ;
#40445=CARTESIAN_POINT ( 'NONE',  ( 0.000000000000000000, -74.65491531819111515, -8.830959090343204920 ) ) ;
#40447=CARTESIAN_POINT ( 'NONE',  ( 10.00000000000000000, 0.000000000000000000, 0.000000000000000000 ) ) ;
#40448=CARTESIAN_POINT ( 'NONE',  ( 10.00000000000000000, -70.53064760720297954, -26.01480285779911839 ) ) ;
#40449=CARTESIAN_POINT ( 'NONE',  ( 10.00000000000000000, 0.000000000000000000, 0.000000000000000000 ) ) ;
#40451=CARTESIAN_POINT ( 'NONE',  ( 10.00000000000000000, -78.73519480814971416, 22.90783923731600069 ) ) ;
#40462=EDGE_CURVE ( 'NONE', #36114, #4419, #47201, .T. ) ;
#40463=DIRECTION ( 'NONE',  ( -1.000000000000000000, 0.000000000000000000, 0.000000000000000000 ) ) ;
#40467=ADVANCED_FACE ( 'NONE', ( #5681 ), #5441, .T. ) ;
#40468=ORIENTED_EDGE ( 'NONE', *, *, #29559, .F. ) ;
#40469=ORIENTED_EDGE ( 'NONE', *, *, #22695, .F. ) ;
#40474=CARTESIAN_POINT ( 'NONE',  ( 10.00000000000000000, 68.26794271651307611, -31.47745569255064169 ) ) ;
#40477=ORIENTED_EDGE ( 'NONE', *, *, #31014, .F. ) ;
#40478=AXIS2_PLACEMENT_3D ( 'NONE', #10534, #10285, #18101 ) ;
#40486=VERTEX_POINT ( 'NONE', #46803 ) ;
#40488=DIRECTION ( 'NONE',  ( -1.000000000000000000, -0.000000000000000000, 0.000000000000000000 ) ) ;
#40498=CYLINDRICAL_SURFACE ( 'NONE', #1220, 82.00000000000000000 ) ;
#40501=DIRECTION ( 'NONE',  ( 0.000000000000000000, 0.000000000000000000, 1.000000000000000000 ) ) ;
#40505=FACE_OUTER_BOUND ( 'NONE', #1406, .T. ) ;
#40509=ORIENTED_EDGE ( 'NONE', *, *, #30399, .F. ) ;
#40511=EDGE_CURVE ( 'NONE', #28496, #14564, #12547, .T. ) ;
#40514=EDGE_CURVE ( 'NONE', #10023, #15936, #1102, .T. ) ;
#40516=DIRECTION ( 'NONE',  ( 0.000000000000000000, 0.9723699203976756689, 0.2334453638559094157 ) ) ;
#40517=CARTESIAN_POINT ( 'NONE',  ( 10.00000000000000000, 70.52718814184294160, -26.02418014898236720 ) ) ;
#40527=CARTESIAN_POINT ( 'NONE',  ( 10.00000000000000000, 58.39081064771751528, 50.95692526931350841 ) ) ;
#40530=VECTOR ( 'NONE', #14755, 1000.000000000000000 ) ;
#40538=VERTEX_POINT ( 'NONE', #12789 ) ;
#40550=LINE ( 'NONE', #18017, #45183 ) ;
#40551=DIRECTION ( 'NONE',  ( 0.000000000000000000, -0.5224985647159380298, -0.8526401643540988395 ) ) ;
#40567=EDGE_CURVE ( 'NONE', #23195, #38922, #47283, .T. ) ;
#40580=CIRCLE ( 'NONE', #6974, 82.00000000000000000 ) ;
#40581=EDGE_CURVE ( 'NONE', #45240, #34021, #15173, .T. ) ;
#40585=EDGE_LOOP ( 'NONE', ( #38613, #7019, #43080, #42902 ) ) ;
#40586=CARTESIAN_POINT ( 'NONE',  ( 0.000000000000000000, 0.000000000000000000, 0.000000000000000000 ) ) ;
#40588=VERTEX_POINT ( 'NONE', #21797 ) ;
#40596=EDGE_CURVE ( 'NONE', #10624, #21719, #10983, .T. ) ;
#40611=ORIENTED_EDGE ( 'NONE', *, *, #25668, .T. ) ;
#40616=CARTESIAN_POINT ( 'NONE',  ( 0.000000000000000000, 70.52718814184294160, -26.02418014898236720 ) ) ;
#40617=CARTESIAN_POINT ( 'NONE',  ( 0.000000000000000000, 76.69515212746016175, 29.01471420065591289 ) ) ;
#40620=DIRECTION ( 'NONE',  ( 0.000000000000000000, 0.000000000000000000, 1.000000000000000000 ) ) ;
#40628=VERTEX_POINT ( 'NONE', #7116 ) ;
#40634=EDGE_LOOP ( 'NONE', ( #6797, #18454, #16024, #31630 ) ) ;
#40639=DIRECTION ( 'NONE',  ( -1.000000000000000000, 0.000000000000000000, -0.000000000000000000 ) ) ;
#40641=VECTOR ( 'NONE', #4647, 1000.000000000000000 ) ;
#40647=CARTESIAN_POINT ( 'NONE',  ( 5.000000000000000000, -67.80270845531855173, -46.11716303203261447 ) ) ;
#40648=CIRCLE ( 'NONE', #10158, 77.49899999999999523 ) ;
#40652=EDGE_LOOP ( 'NONE', ( #20922, #5075, #44582, #27294 ) ) ;
#40653=EDGE_CURVE ( 'NONE', #33790, #26325, #3974, .T. ) ;
#40655=CARTESIAN_POINT ( 'NONE',  ( 10.00000000000000000, -59.46389618801928378, -49.70050353004953791 ) ) ;
#40658=DIRECTION ( 'NONE',  ( 0.000000000000000000, -0.9969173337331287410, 0.07845909572783495156 ) ) ;
#40669=DIRECTION ( 'NONE',  ( -1.000000000000000000, 0.000000000000000000, 0.000000000000000000 ) ) ;
#40674=ORIENTED_EDGE ( 'NONE', *, *, #38413, .F. ) ;
#40680=AXIS2_PLACEMENT_3D ( 'NONE', #41813, #8272, #27126 ) ;
#40687=VERTEX_POINT ( 'NONE', #28903 ) ;
#40688=DIRECTION ( 'NONE',  ( 1.000000000000000000, -0.000000000000000000, -0.000000000000000000 ) ) ;
#40692=AXIS2_PLACEMENT_3D ( 'NONE', #40448, #17908, #14501 ) ;
#40701=ORIENTED_EDGE ( 'NONE', *, *, #9116, .F. ) ;
#40703=ORIENTED_EDGE ( 'NONE', *, *, #23260, .T. ) ;
#40713=ADVANCED_FACE ( 'NONE', ( #45059 ), #29871, .T. ) ;
#40718=CARTESIAN_POINT ( 'NONE',  ( 10.00000000000000000, -73.72996012237429397, -14.67089635893794508 ) ) ;
#40728=ORIENTED_EDGE ( 'NONE', *, *, #17635, .F. ) ;
#40731=CARTESIAN_POINT ( 'NONE',  ( 5.000000000000000000, -74.74816331893454446, 33.71516098798714722 ) ) ;
#40733=CYLINDRICAL_SURFACE ( 'NONE', #23482, 82.00000000000000000 ) ;
#40739=CARTESIAN_POINT ( 'NONE',  ( 10.00000000000000000, 71.91182617369230456, -28.89263327155667938 ) ) ;
#40747=EDGE_CURVE ( 'NONE', #17337, #17528, #47684, .T. ) ;
#40748=CARTESIAN_POINT ( 'NONE',  ( 10.00000000000000000, -62.50884508063395373, -41.76106447765554464 ) ) ;
#40750=AXIS2_PLACEMENT_3D ( 'NONE', #2311, #28750, #10867 ) ;
#40751=FACE_OUTER_BOUND ( 'NONE', #30428, .T. ) ;
#40754=VECTOR ( 'NONE', #21458, 1000.000000000000000 ) ;
#40761=VERTEX_POINT ( 'NONE', #18617 ) ;
#40763=EDGE_LOOP ( 'NONE', ( #26503, #26260, #38261, #22782 ) ) ;
#40767=ORIENTED_EDGE ( 'NONE', *, *, #30294, .T. ) ;
#40777=ORIENTED_EDGE ( 'NONE', *, *, #16095, .F. ) ;
#40779=CYLINDRICAL_SURFACE ( 'NONE', #10237, 77.49899999999999523 ) ;
#40780=CIRCLE ( 'NONE', #2473, 31.99999999999999289 ) ;
#40781=CARTESIAN_POINT ( 'NONE',  ( 0.000000000000000000, -46.21855187248673502, 62.20884554314003623 ) ) ;
#40782=AXIS2_PLACEMENT_3D ( 'NONE', #38258, #35063, #16466 ) ;
#40785=CARTESIAN_POINT ( 'NONE',  ( 10.00000000000000000, 0.000000000000000000, 0.000000000000000000 ) ) ;
#40786=ORIENTED_EDGE ( 'NONE', *, *, #11163, .T. ) ;
#40793=DIRECTION ( 'NONE',  ( -1.000000000000000000, -0.000000000000000000, 0.000000000000000000 ) ) ;
#40803=CIRCLE ( 'NONE', #9516, 31.99999999999999289 ) ;
#40804=CARTESIAN_POINT ( 'NONE',  ( 0.000000000000000000, 15.33399622253600292, -80.55351364060572905 ) ) ;
#40810=ORIENTED_EDGE ( 'NONE', *, *, #46405, .F. ) ;
#40816=DIRECTION ( 'NONE',  ( -1.000000000000000000, 0.000000000000000000, -0.000000000000000000 ) ) ;
#40819=AXIS2_PLACEMENT_3D ( 'NONE', #1386, #16311, #31253 ) ;
#40821=EDGE_CURVE ( 'NONE', #16336, #29421, #4732, .T. ) ;
#40830=CIRCLE ( 'NONE', #34556, 31.99999999999998579 ) ;
#40831=VERTEX_POINT ( 'NONE', #11290 ) ;
#40833=EDGE_CURVE ( 'NONE', #14124, #34627, #9401, .T. ) ;
#40834=EDGE_CURVE ( 'NONE', #4138, #14124, #43787, .T. ) ;
#40835=EDGE_CURVE ( 'NONE', #34606, #19209, #7059, .T. ) ;
#40839=ORIENTED_EDGE ( 'NONE', *, *, #13700, .F. ) ;
#40840=EDGE_CURVE ( 'NONE', #23867, #39890, #28938, .T. ) ;
#40841=DIRECTION ( 'NONE',  ( 0.000000000000000000, 0.5224985647159441360, 0.8526401643540952868 ) ) ;
#40847=ORIENTED_EDGE ( 'NONE', *, *, #826, .T. ) ;
#40848=AXIS2_PLACEMENT_3D ( 'NONE', #32848, #43166, #17440 ) ;
#40849=DIRECTION ( 'NONE',  ( 0.000000000000000000, -0.4539904997395350361, -0.8910065241883738940 ) ) ;
#40853=ORIENTED_EDGE ( 'NONE', *, *, #14087, .F. ) ;
#40855=CARTESIAN_POINT ( 'NONE',  ( 0.000000000000000000, 0.000000000000000000, 0.000000000000000000 ) ) ;
#40857=VECTOR ( 'NONE', #23947, 1000.000000000000000 ) ;
#40876=EDGE_CURVE ( 'NONE', #41232, #9926, #15662, .T. ) ;
#40877=PRODUCT_DEFINITION_CONTEXT ( 'detailed design', #6638, 'design' ) ;
#40878=CARTESIAN_POINT ( 'NONE',  ( 10.00000000000000000, 36.72794159290334903, -65.59268652807170952 ) ) ;
#40879=ADVANCED_FACE ( 'NONE', ( #16638 ), #38430, .T. ) ;
#40882=EDGE_CURVE ( 'NONE', #43246, #31653, #807, .T. ) ;
#40883=VERTEX_POINT ( 'NONE', #16884 ) ;
#40884=AXIS2_PLACEMENT_3D ( 'NONE', #31624, #15958, #38726 ) ;
#40893=ORIENTED_EDGE ( 'NONE', *, *, #47022, .T. ) ;
#40894=ORIENTED_EDGE ( 'NONE', *, *, #505, .F. ) ;
#40898=EDGE_CURVE ( 'NONE', #24887, #17865, #5155, .T. ) ;
#40903=EDGE_LOOP ( 'NONE', ( #30069, #26600, #41871, #47279 ) ) ;
#40911=CARTESIAN_POINT ( 'NONE',  ( 10.00000000000000000, 66.50666863322000211, 39.78640506895629869 ) ) ;
#40917=ORIENTED_EDGE ( 'NONE', *, *, #29390, .F. ) ;
#40920=ORIENTED_EDGE ( 'NONE', *, *, #2466, .F. ) ;
#40940=DIRECTION ( 'NONE',  ( -1.000000000000000000, 0.000000000000000000, 0.000000000000000000 ) ) ;
#40950=CIRCLE ( 'NONE', #24516, 31.99999999999999645 ) ;
#40955=ORIENTED_EDGE ( 'NONE', *, *, #15355, .F. ) ;
#40956=ORIENTED_EDGE ( 'NONE', *, *, #33453, .F. ) ;
#40964=EDGE_CURVE ( 'NONE', #46765, #24526, #38690, .T. ) ;
#40967=AXIS2_PLACEMENT_3D ( 'NONE', #25917, #5964, #46830 ) ;
#40972=CARTESIAN_POINT ( 'NONE',  ( 10.00000000000000000, -50.95692526931286181, -58.39081064771806240 ) ) ;
#40973=ORIENTED_EDGE ( 'NONE', *, *, #17245, .T. ) ;
#40974=DIRECTION ( 'NONE',  ( 0.000000000000000000, 0.9510565162951521989, 0.3090169943749515591 ) ) ;
#40978=DIRECTION ( 'NONE',  ( 0.000000000000000000, -0.7604059656000227152, -0.6494480483301933171 ) ) ;
#40983=ORIENTED_EDGE ( 'NONE', *, *, #7290, .T. ) ;
#40991=DIRECTION ( 'NONE',  ( 1.000000000000000000, -0.000000000000000000, -0.000000000000000000 ) ) ;
#41002=CARTESIAN_POINT ( 'NONE',  ( 10.00000000000000000, -55.20638768913797634, 51.02545421589302777 ) ) ;
#41014=ORIENTED_EDGE ( 'NONE', *, *, #39230, .F. ) ;
#41018=EDGE_CURVE ( 'NONE', #3149, #24941, #16508, .T. ) ;
#41019=CIRCLE ( 'NONE', #47267, 82.00000000000000000 ) ;
#41021=AXIS2_PLACEMENT_3D ( 'NONE', #43278, #9738, #24677 ) ;
#41041=VECTOR ( 'NONE', #31309, 1000.000000000000000 ) ;
#41046=ORIENTED_EDGE ( 'NONE', *, *, #39246, .T. ) ;
#41048=CARTESIAN_POINT ( 'NONE',  ( 0.000000000000000000, -75.54627589209931671, -17.28742895386164591 ) ) ;
#41052=DIRECTION ( 'NONE',  ( 0.000000000000000000, 0.000000000000000000, 1.000000000000000000 ) ) ;
#41058=EDGE_CURVE ( 'NONE', #42399, #28981, #39150, .T. ) ;
#41062=ORIENTED_EDGE ( 'NONE', *, *, #8512, .F. ) ;
#41063=CARTESIAN_POINT ( 'NONE',  ( 10.00000000000000000, 0.000000000000000000, 0.000000000000000000 ) ) ;
#41068=DIRECTION ( 'NONE',  ( 0.000000000000000000, 0.9969173337331276308, 0.07845909572784864894 ) ) ;
#41072=CARTESIAN_POINT ( 'NONE',  ( 0.000000000000000000, 0.000000000000000000, 0.000000000000000000 ) ) ;
#41077=AXIS2_PLACEMENT_3D ( 'NONE', #21774, #39685, #10040 ) ;
#41079=DIRECTION ( 'NONE',  ( -1.000000000000000000, -0.000000000000000000, 0.000000000000000000 ) ) ;
#41084=VERTEX_POINT ( 'NONE', #24938 ) ;
#41088=AXIS2_PLACEMENT_3D ( 'NONE', #2723, #14720, #39942 ) ;
#41097=DIRECTION ( 'NONE',  ( -1.000000000000000000, -0.000000000000000000, 0.000000000000000000 ) ) ;
#41102=ORIENTED_EDGE ( 'NONE', *, *, #6221, .F. ) ;
#41103=CARTESIAN_POINT ( 'NONE',  ( 0.000000000000000000, 35.91791733033570466, -68.67312586194960033 ) ) ;
#41109=CARTESIAN_POINT ( 'NONE',  ( 10.00000000000000000, 0.000000000000000000, 0.000000000000000000 ) ) ;
#41110=CYLINDRICAL_SURFACE ( 'NONE', #38388, 77.49899999999999523 ) ;
#41116=CARTESIAN_POINT ( 'NONE',  ( 0.000000000000000000, 2.946379043146343246, 75.11764819372150725 ) ) ;
#41120=DIRECTION ( 'NONE',  ( 1.000000000000000000, 0.000000000000000000, 0.000000000000000000 ) ) ;
#41126=EDGE_LOOP ( 'NONE', ( #13716, #27582, #38893, #32315 ) ) ;
#41130=EDGE_CURVE ( 'NONE', #17470, #25836, #21181, .T. ) ;
#41132=CARTESIAN_POINT ( 'NONE',  ( 5.000000000000000000, -27.74655509720617275, -77.16300072079690153 ) ) ;
#41133=EDGE_LOOP ( 'NONE', ( #22324, #22733, #16004, #42194 ) ) ;
#41134=CIRCLE ( 'NONE', #20009, 77.49899999999999523 ) ;
#41136=ADVANCED_FACE ( 'NONE', ( #10745 ), #25648, .T. ) ;
#41139=FACE_OUTER_BOUND ( 'NONE', #38692, .T. ) ;
#41157=EDGE_LOOP ( 'NONE', ( #47911, #7004, #9539, #45289 ) ) ;
#41161=VERTEX_POINT ( 'NONE', #36192 ) ;
#41162=ORIENTED_EDGE ( 'NONE', *, *, #10049, .T. ) ;
#41163=DIRECTION ( 'NONE',  ( 0.000000000000000000, -0.5224985647159379187, -0.8526401643540989506 ) ) ;
#41170=EDGE_LOOP ( 'NONE', ( #9389, #30782, #1417, #17678 ) ) ;
#41178=DIRECTION ( 'NONE',  ( 0.000000000000000000, 0.000000000000000000, 1.000000000000000000 ) ) ;
#41180=DIRECTION ( 'NONE',  ( 0.000000000000000000, -0.4539904997395541875, 0.8910065241883642351 ) ) ;
#41183=DIRECTION ( 'NONE',  ( -1.000000000000000000, 0.000000000000000000, 0.000000000000000000 ) ) ;
#41185=CIRCLE ( 'NONE', #8359, 82.00000000000000000 ) ;
#41186=CARTESIAN_POINT ( 'NONE',  ( 10.00000000000000000, 76.69515212746016175, 29.01471420065591289 ) ) ;
#41187=DIRECTION ( 'NONE',  ( -1.000000000000000000, -0.000000000000000000, -0.000000000000000000 ) ) ;
#41189=CARTESIAN_POINT ( 'NONE',  ( 10.00000000000000000, -8.830959090341869100, -74.65491531819127147 ) ) ;
#41191=CARTESIAN_POINT ( 'NONE',  ( 5.000000000000000000, -33.71516098798792171, 74.74816331893418919 ) ) ;
#41192=FACE_OUTER_BOUND ( 'NONE', #32770, .T. ) ;
#41194=ADVANCED_FACE ( 'NONE', ( #15143 ), #45467, .T. ) ;
#41198=EDGE_CURVE ( 'NONE', #35990, #39808, #34445, .T. ) ;
#41200=LINE ( 'NONE', #33587, #7304 ) ;
#41206=ORIENTED_EDGE ( 'NONE', *, *, #7660, .T. ) ;
#41211=LINE ( 'NONE', #22834, #42212 ) ;
#41214=EDGE_LOOP ( 'NONE', ( #37124, #37956, #2682, #10754 ) ) ;
#41216=CARTESIAN_POINT ( 'NONE',  ( 10.00000000000000000, 75.16055320797059380, -18.89407956138177269 ) ) ;
#41219=CARTESIAN_POINT ( 'NONE',  ( 10.00000000000000000, 73.73191006444572793, -14.66109333815486515 ) ) ;
#41229=FACE_OUTER_BOUND ( 'NONE', #5612, .T. ) ;
#41231=DIRECTION ( 'NONE',  ( -1.000000000000000000, 0.000000000000000000, -0.000000000000000000 ) ) ;
#41232=VERTEX_POINT ( 'NONE', #44504 ) ;
#41233=LINE ( 'NONE', #90, #9637 ) ;
#41250=CYLINDRICAL_SURFACE ( 'NONE', #8277, 31.99999999999998579 ) ;
#41251=CARTESIAN_POINT ( 'NONE',  ( 10.00000000000000000, 68.67312586195046720, -35.91791733033402068 ) ) ;
#41272=DIRECTION ( 'NONE',  ( 0.000000000000000000, 0.8526401643540936215, -0.5224985647159469115 ) ) ;
#41280=ORIENTED_EDGE ( 'NONE', *, *, #30399, .T. ) ;
#41283=LINE ( 'NONE', #10932, #47507 ) ;
#41285=CARTESIAN_POINT ( 'NONE',  ( 0.000000000000000000, -34.44570377933549565, -69.42325613327476219 ) ) ;
#41286=CARTESIAN_POINT ( 'NONE',  ( 10.00000000000000000, 0.000000000000000000, 0.000000000000000000 ) ) ;
#41292=CARTESIAN_POINT ( 'NONE',  ( 0.000000000000000000, 81.90746397400387480, 3.894527615418187150 ) ) ;
#41299=DIRECTION ( 'NONE',  ( 0.000000000000000000, 0.000000000000000000, 1.000000000000000000 ) ) ;
#41306=FACE_OUTER_BOUND ( 'NONE', #41214, .T. ) ;
#41308=EDGE_CURVE ( 'NONE', #6665, #13155, #5575, .T. ) ;
#41311=ORIENTED_EDGE ( 'NONE', *, *, #37032, .F. ) ;
#41313=CIRCLE ( 'NONE', #15519, 31.99999999999998934 ) ;
#41316=ORIENTED_EDGE ( 'NONE', *, *, #12779, .F. ) ;
#41318=LINE ( 'NONE', #33951, #39451 ) ;
#41320=ORIENTED_EDGE ( 'NONE', *, *, #2409, .F. ) ;
#41325=ORIENTED_EDGE ( 'NONE', *, *, #39518, .F. ) ;
#41327=AXIS2_PLACEMENT_3D ( 'NONE', #9903, #17473, #29223 ) ;
#41331=DIRECTION ( 'NONE',  ( 0.000000000000000000, 0.000000000000000000, 1.000000000000000000 ) ) ;
#41337=DIRECTION ( 'NONE',  ( 0.000000000000000000, -0.9969173337331271867, -0.07845909572785568498 ) ) ;
#41351=DIRECTION ( 'NONE',  ( 0.000000000000000000, 0.000000000000000000, 1.000000000000000000 ) ) ;
#41353=DIRECTION ( 'NONE',  ( 0.000000000000000000, 0.000000000000000000, 1.000000000000000000 ) ) ;
#41359=DIRECTION ( 'NONE',  ( 0.000000000000000000, -0.1564344650402381132, 0.9876883405951365491 ) ) ;
#41361=VECTOR ( 'NONE', #19272, 1000.000000000000000 ) ;
#41374=ADVANCED_FACE ( 'NONE', ( #34437 ), #46449, .T. ) ;
#41387=EDGE_CURVE ( 'NONE', #38308, #3149, #21209, .T. ) ;
#41388=DIRECTION ( 'NONE',  ( 0.000000000000000000, -0.1564344650402170744, -0.9876883405951399908 ) ) ;
#41391=DIRECTION ( 'NONE',  ( -1.000000000000000000, 0.000000000000000000, 0.000000000000000000 ) ) ;
#41394=ORIENTED_EDGE ( 'NONE', *, *, #37181, .F. ) ;
#41403=ORIENTED_EDGE ( 'NONE', *, *, #48081, .F. ) ;
#41406=DIRECTION ( 'NONE',  ( -1.000000000000000000, 0.000000000000000000, 0.000000000000000000 ) ) ;
#41416=LINE ( 'NONE', #7640, #17003 ) ;
#41424=VECTOR ( 'NONE', #44211, 1000.000000000000000 ) ;
#41425=CARTESIAN_POINT ( 'NONE',  ( 5.000000000000002665, 21.60688246758586217, 79.10210256391376049 ) ) ;
#41426=CIRCLE ( 'NONE', #23450, 82.00000000000000000 ) ;
#41427=ORIENTED_EDGE ( 'NONE', *, *, #7177, .F. ) ;
#41428=DIRECTION ( 'NONE',  ( 0.000000000000000000, 0.6494480483301849905, -0.7604059656000299317 ) ) ;
#41429=VECTOR ( 'NONE', #40300, 1000.000000000000000 ) ;
#41434=AXIS2_PLACEMENT_3D ( 'NONE', #45534, #11774, #4904 ) ;
#41435=EDGE_CURVE ( 'NONE', #41545, #15919, #14977, .T. ) ;
#41438=ORIENTED_EDGE ( 'NONE', *, *, #17789, .T. ) ;
#41440=DIRECTION ( 'NONE',  ( 1.000000000000000000, -0.000000000000000000, -0.000000000000000000 ) ) ;
#41445=EDGE_CURVE ( 'NONE', #23147, #16520, #14164, .T. ) ;
#41446=EDGE_CURVE ( 'NONE', #27599, #14155, #34483, .T. ) ;
#41450=CIRCLE ( 'NONE', #21105, 82.00000000000000000 ) ;
#41457=CARTESIAN_POINT ( 'NONE',  ( 10.00000000000000000, 76.41127070299292257, -12.93880638057232346 ) ) ;
#41462=CARTESIAN_POINT ( 'NONE',  ( 10.00000000000000000, -46.54456581323847786, 59.03342792756247093 ) ) ;
#41466=CARTESIAN_POINT ( 'NONE',  ( 0.000000000000000000, -31.46837873495025306, 68.27212725128265447 ) ) ;
#41469=AXIS2_PLACEMENT_3D ( 'NONE', #3960, #15230, #22797 ) ;
#41470=DIRECTION ( 'NONE',  ( 0.000000000000000000, 0.000000000000000000, 1.000000000000000000 ) ) ;
#41473=CARTESIAN_POINT ( 'NONE',  ( 10.00000000000000000, 26.01480285779933510, -70.53064760720289428 ) ) ;
#41479=LINE ( 'NONE', #15052, #29387 ) ;
#41480=CARTESIAN_POINT ( 'NONE',  ( 0.000000000000000000, 68.27212725128275395, 31.46837873495001503 ) ) ;
#41487=AXIS2_PLACEMENT_3D ( 'NONE', #26538, #15040, #6967 ) ;
#41494=EDGE_CURVE ( 'NONE', #46638, #28147, #2850, .T. ) ;
#41504=ORIENTED_EDGE ( 'NONE', *, *, #35590, .T. ) ;
#41506=EDGE_CURVE ( 'NONE', #3764, #44761, #17295, .T. ) ;
#41512=VERTEX_POINT ( 'NONE', #17777 ) ;
#41518=DIRECTION ( 'NONE',  ( 0.000000000000000000, 0.000000000000000000, 1.000000000000000000 ) ) ;
#41532=DIRECTION ( 'NONE',  ( 0.000000000000000000, 0.8910065241883657894, 0.4539904997395510788 ) ) ;
#41535=DIRECTION ( 'NONE',  ( -1.000000000000000000, -0.000000000000000000, -0.000000000000000000 ) ) ;
#41542=CYLINDRICAL_SURFACE ( 'NONE', #28666, 31.99999999999998579 ) ;
#41545=VERTEX_POINT ( 'NONE', #36139 ) ;
#41549=EDGE_CURVE ( 'NONE', #32278, #33790, #39338, .T. ) ;
#41550=ORIENTED_EDGE ( 'NONE', *, *, #12719, .F. ) ;
#41553=ORIENTED_EDGE ( 'NONE', *, *, #11780, .T. ) ;
#41555=AXIS2_PLACEMENT_3D ( 'NONE', #32504, #10217, #13010 ) ;
#41557=FACE_OUTER_BOUND ( 'NONE', #2898, .T. ) ;
#41560=VERTEX_POINT ( 'NONE', #6064 ) ;
#41566=CARTESIAN_POINT ( 'NONE',  ( 10.00000000000000000, 0.000000000000000000, 0.000000000000000000 ) ) ;
#41574=VERTEX_POINT ( 'NONE', #10695 ) ;
#41578=CARTESIAN_POINT ( 'NONE',  ( 10.00000000000000000, 54.21277698773675979, 55.38113227695801299 ) ) ;
#41579=VERTEX_POINT ( 'NONE', #40781 ) ;
#41582=LINE ( 'NONE', #42070, #39971 ) ;
#41583=ORIENTED_EDGE ( 'NONE', *, *, #11746, .F. ) ;
#41584=VERTEX_POINT ( 'NONE', #11647 ) ;
#41585=CYLINDRICAL_SURFACE ( 'NONE', #24421, 31.99999999999999289 ) ;
#41588=DIRECTION ( 'NONE',  ( 0.000000000000000000, 0.3826834323650905589, -0.9238795325112864054 ) ) ;
#41593=CARTESIAN_POINT ( 'NONE',  ( 10.00000000000000000, -46.53671651293907274, -59.03961581697448935 ) ) ;
#41595=CARTESIAN_POINT ( 'NONE',  ( 10.00000000000000000, 0.000000000000000000, 0.000000000000000000 ) ) ;
#41596=DIRECTION ( 'NONE',  ( -1.000000000000000000, 0.000000000000000000, 0.000000000000000000 ) ) ;
#41608=ORIENTED_EDGE ( 'NONE', *, *, #36679, .T. ) ;
#41610=EDGE_CURVE ( 'NONE', #25536, #38965, #2481, .T. ) ;
#41615=ORIENTED_EDGE ( 'NONE', *, *, #23902, .F. ) ;
#41616=VERTEX_POINT ( 'NONE', #29289 ) ;
#41624=ORIENTED_EDGE ( 'NONE', *, *, #40653, .F. ) ;
#41625=DIRECTION ( 'NONE',  ( 1.000000000000000000, -0.000000000000000000, -0.000000000000000000 ) ) ;
#41635=CARTESIAN_POINT ( 'NONE',  ( 0.000000000000000000, -70.53064760720336324, 26.01480285779810231 ) ) ;
#41640=ORIENTED_EDGE ( 'NONE', *, *, #5478, .T. ) ;
#41645=DIRECTION ( 'NONE',  ( -1.000000000000000000, 0.000000000000000000, 0.000000000000000000 ) ) ;
#41646=FACE_OUTER_BOUND ( 'NONE', #26554, .T. ) ;
#41647=CARTESIAN_POINT ( 'NONE',  ( 10.00000000000000000, 62.50884508063427347, 41.76106447765511831 ) ) ;
#41648=EDGE_CURVE ( 'NONE', #9073, #44497, #26715, .T. ) ;
#41665=CARTESIAN_POINT ( 'NONE',  ( 10.00000000000000000, 0.000000000000000000, 0.000000000000000000 ) ) ;
#41670=DIRECTION ( 'NONE',  ( 0.000000000000000000, 0.8526401643540897357, 0.5224985647159531288 ) ) ;
#41682=ORIENTED_EDGE ( 'NONE', *, *, #47891, .T. ) ;
#41685=DIRECTION ( 'NONE',  ( 1.000000000000000000, 0.000000000000000000, 0.000000000000000000 ) ) ;
#41690=ORIENTED_EDGE ( 'NONE', *, *, #24211, .T. ) ;
#41692=ORIENTED_EDGE ( 'NONE', *, *, #42095, .F. ) ;
#41693=ORIENTED_EDGE ( 'NONE', *, *, #17706, .F. ) ;
#41694=AXIS2_PLACEMENT_3D ( 'NONE', #2154, #39613, #32021 ) ;
#41697=AXIS2_PLACEMENT_3D ( 'NONE', #4937, #31391, #34792 ) ;
#41699=CIRCLE ( 'NONE', #1020, 31.99999999999998579 ) ;
#41702=ORIENTED_EDGE ( 'NONE', *, *, #23260, .F. ) ;
#41706=DIRECTION ( 'NONE',  ( -1.000000000000000000, -0.000000000000000000, 0.000000000000000000 ) ) ;
#41728=AXIS2_PLACEMENT_3D ( 'NONE', #39019, #27285, #39254 ) ;
#41729=EDGE_CURVE ( 'NONE', #3853, #38187, #15011, .T. ) ;
#41737=EDGE_CURVE ( 'NONE', #44507, #14647, #7965, .T. ) ;
#41738=DIRECTION ( 'NONE',  ( -1.000000000000000000, 0.000000000000000000, 0.000000000000000000 ) ) ;
#41752=CARTESIAN_POINT ( 'NONE',  ( 10.00000000000000000, -58.39081064771787766, 50.95692526931307498 ) ) ;
#41756=ORIENTED_EDGE ( 'NONE', *, *, #17521, .T. ) ;
#41765=CARTESIAN_POINT ( 'NONE',  ( 10.00000000000000000, 46.21855187248629449, 62.20884554314036308 ) ) ;
#41776=CIRCLE ( 'NONE', #44139, 82.00000000000000000 ) ;
#41780=CARTESIAN_POINT ( 'NONE',  ( 5.000000000000002665, -21.60688246758530440, -79.10210256391390260 ) ) ;
#41788=CARTESIAN_POINT ( 'NONE',  ( 10.00000000000000000, -58.39081064771713869, -50.95692526931392052 ) ) ;
#41789=CARTESIAN_POINT ( 'NONE',  ( 10.00000000000000000, 71.27951684758026829, 30.41916302227139113 ) ) ;
#41795=AXIS2_PLACEMENT_3D ( 'NONE', #42742, #38331, #24356 ) ;
#41796=VERTEX_POINT ( 'NONE', #21328 ) ;
#41799=ORIENTED_EDGE ( 'NONE', *, *, #36664, .T. ) ;
#41808=AXIS2_PLACEMENT_3D ( 'NONE', #39285, #31964, #28041 ) ;
#41813=CARTESIAN_POINT ( 'NONE',  ( 10.00000000000000000, 0.000000000000000000, 0.000000000000000000 ) ) ;
#41821=DIRECTION ( 'NONE',  ( 0.000000000000000000, 0.000000000000000000, 1.000000000000000000 ) ) ;
#41823=DIRECTION ( 'NONE',  ( 1.000000000000000000, 0.000000000000000000, 0.000000000000000000 ) ) ;
#41826=EDGE_LOOP ( 'NONE', ( #2656, #12092, #20516, #25045 ) ) ;
#41830=EDGE_CURVE ( 'NONE', #12875, #36756, #21083, .T. ) ;
#41832=DIRECTION ( 'NONE',  ( 0.000000000000000000, 0.000000000000000000, 1.000000000000000000 ) ) ;
#41833=VERTEX_POINT ( 'NONE', #28692 ) ;
#41836=CARTESIAN_POINT ( 'NONE',  ( 0.000000000000000000, -62.50329211542465657, 41.76937507738766442 ) ) ;
#41837=DIRECTION ( 'NONE',  ( 0.000000000000000000, 0.000000000000000000, 1.000000000000000000 ) ) ;
#41838=CARTESIAN_POINT ( 'NONE',  ( 10.00000000000000000, -23.16143007188481207, 73.95703589263968070 ) ) ;
#41840=DIRECTION ( 'NONE',  ( 1.000000000000000000, 0.000000000000000000, 0.000000000000000000 ) ) ;
#41843=DIRECTION ( 'NONE',  ( -1.000000000000000000, -0.000000000000000000, -0.000000000000000000 ) ) ;
#41844=CIRCLE ( 'NONE', #26213, 32.00000000000000000 ) ;
#41848=CIRCLE ( 'NONE', #24618, 31.99999999999998934 ) ;
#41850=CARTESIAN_POINT ( 'NONE',  ( 10.00000000000000000, -14.67089635893764665, 73.72996012237435082 ) ) ;
#41852=DIRECTION ( 'NONE',  ( -1.000000000000000000, -0.000000000000000000, -0.000000000000000000 ) ) ;
#41853=EDGE_CURVE ( 'NONE', #45623, #11599, #11041, .T. ) ;
#41865=EDGE_LOOP ( 'NONE', ( #7585, #24674, #47492, #44862 ) ) ;
#41868=CARTESIAN_POINT ( 'NONE',  ( 0.000000000000000000, -41.76937507738831812, 62.50329211542423025 ) ) ;
#41869=EDGE_LOOP ( 'NONE', ( #39653, #15451, #29763, #19628 ) ) ;
#41870=EDGE_LOOP ( 'NONE', ( #34236, #11631, #33659, #2493 ) ) ;
#41871=ORIENTED_EDGE ( 'NONE', *, *, #43543, .F. ) ;
#41873=VERTEX_POINT ( 'NONE', #6654 ) ;
#41874=AXIS2_PLACEMENT_3D ( 'NONE', #21351, #32618, #10598 ) ;
#41876=ORIENTED_EDGE ( 'NONE', *, *, #17819, .F. ) ;
#41878=DIRECTION ( 'NONE',  ( 0.000000000000000000, 0.000000000000000000, 1.000000000000000000 ) ) ;
#41887=FACE_OUTER_BOUND ( 'NONE', #40585, .T. ) ;
#41888=CARTESIAN_POINT ( 'NONE',  ( 0.000000000000000000, 71.21200624218852226, -40.65526001592539984 ) ) ;
#41897=EDGE_CURVE ( 'NONE', #36459, #7382, #32591, .T. ) ;
#41914=CIRCLE ( 'NONE', #5960, 77.49899999999999523 ) ;
#41918=CIRCLE ( 'NONE', #33293, 82.00000000000000000 ) ;
#41926=DIRECTION ( 'NONE',  ( -1.000000000000000000, 0.000000000000000000, 0.000000000000000000 ) ) ;
#41938=CYLINDRICAL_SURFACE ( 'NONE', #1587, 31.99999999999999289 ) ;
#41941=VECTOR ( 'NONE', #46783, 1000.000000000000000 ) ;
#41942=CARTESIAN_POINT ( 'NONE',  ( 10.00000000000000000, 46.54456581323805153, 59.03342792756280488 ) ) ;
#41943=CARTESIAN_POINT ( 'NONE',  ( 0.000000000000000000, 0.000000000000000000, 0.000000000000000000 ) ) ;
#41949=CARTESIAN_POINT ( 'NONE',  ( 10.00000000000000000, -77.49459641780886443, -0.8261519478439277586 ) ) ;
#41963=LINE ( 'NONE', #9141, #35220 ) ;
#41968=CARTESIAN_POINT ( 'NONE',  ( 10.00000000000000000, 34.44570377933598593, 69.42325613327452061 ) ) ;
#41969=EDGE_CURVE ( 'NONE', #46575, #40440, #47793, .T. ) ;
#41971=CIRCLE ( 'NONE', #40390, 31.99999999999999289 ) ;
#41979=ORIENTED_EDGE ( 'NONE', *, *, #20115, .T. ) ;
#41989=AXIS2_PLACEMENT_3D ( 'NONE', #26761, #42171, #22605 ) ;
#41994=VECTOR ( 'NONE', #27157, 1000.000000000000000 ) ;
#42000=VERTEX_POINT ( 'NONE', #34267 ) ;
#42003=FACE_OUTER_BOUND ( 'NONE', #42952, .T. ) ;
#42004=VERTEX_POINT ( 'NONE', #23024 ) ;
#42013=CARTESIAN_POINT ( 'NONE',  ( 10.00000000000000000, 0.000000000000000000, 0.000000000000000000 ) ) ;
#42019=DIRECTION ( 'NONE',  ( 0.000000000000000000, -0.8526401643540970632, 0.5224985647159411384 ) ) ;
#42023=DIRECTION ( 'NONE',  ( 0.000000000000000000, 0.9969173337331282969, -0.07845909572784179331 ) ) ;
#42028=CYLINDRICAL_SURFACE ( 'NONE', #33422, 77.49899999999999523 ) ;
#42030=ORIENTED_EDGE ( 'NONE', *, *, #18608, .F. ) ;
#42035=DIRECTION ( 'NONE',  ( -1.000000000000000000, 0.000000000000000000, 0.000000000000000000 ) ) ;
#42036=ORIENTED_EDGE ( 'NONE', *, *, #8871, .F. ) ;
#42042=EDGE_LOOP ( 'NONE', ( #18237, #35005, #19861, #31338 ) ) ;
#42052=CIRCLE ( 'NONE', #2184, 77.49900000000002365 ) ;
#42057=VERTEX_POINT ( 'NONE', #45294 ) ;
#42064=CYLINDRICAL_SURFACE ( 'NONE', #23664, 31.99999999999999289 ) ;
#42070=CARTESIAN_POINT ( 'NONE',  ( 10.00000000000000000, -49.70050353004846500, -59.46389618802017907 ) ) ;
#42073=ORIENTED_EDGE ( 'NONE', *, *, #25018, .T. ) ;
#42083=EDGE_CURVE ( 'NONE', #33821, #43090, #43958, .T. ) ;
#42084=DIRECTION ( 'NONE',  ( 0.000000000000000000, -0.9876883405951394357, 0.1564344650402205716 ) ) ;
#42089=ORIENTED_EDGE ( 'NONE', *, *, #11509, .F. ) ;
#42093=EDGE_LOOP ( 'NONE', ( #44824, #8264, #40428, #12530 ) ) ;
#42094=EDGE_CURVE ( 'NONE', #3743, #10782, #15048, .T. ) ;
#42095=EDGE_CURVE ( 'NONE', #37633, #23915, #36891, .T. ) ;
#42099=ORIENTED_EDGE ( 'NONE', *, *, #12961, .F. ) ;
#42100=ORIENTED_EDGE ( 'NONE', *, *, #28732, .F. ) ;
#42103=ADVANCED_FACE ( 'NONE', ( #31108 ), #20076, .T. ) ;
#42107=LINE ( 'NONE', #38432, #13753 ) ;
#42118=CARTESIAN_POINT ( 'NONE',  ( 10.00000000000000000, 0.000000000000000000, 0.000000000000000000 ) ) ;
#42119=DIRECTION ( 'NONE',  ( 0.000000000000000000, 0.000000000000000000, 1.000000000000000000 ) ) ;
#42142=DIRECTION ( 'NONE',  ( 0.000000000000000000, 0.000000000000000000, 1.000000000000000000 ) ) ;
#42146=LINE ( 'NONE', #23304, #16633 ) ;
#42147=FACE_OUTER_BOUND ( 'NONE', #15927, .T. ) ;
#42150=CIRCLE ( 'NONE', #15560, 32.00000000000000711 ) ;
#42155=ORIENTED_EDGE ( 'NONE', *, *, #26060, .F. ) ;
#42162=ORIENTED_EDGE ( 'NONE', *, *, #6221, .T. ) ;
#42167=ADVANCED_FACE ( 'NONE', ( #27669 ), #42844, .T. ) ;
#42171=DIRECTION ( 'NONE',  ( -1.000000000000000000, -0.000000000000000000, -0.000000000000000000 ) ) ;
#42173=VERTEX_POINT ( 'NONE', #34757 ) ;
#42179=ORIENTED_EDGE ( 'NONE', *, *, #42899, .F. ) ;
#42183=CARTESIAN_POINT ( 'NONE',  ( 10.00000000000000000, 59.03342792756328095, -46.54456581323744757 ) ) ;
#42184=ADVANCED_FACE ( 'NONE', ( #24469 ), #24000, .T. ) ;
#42193=VECTOR ( 'NONE', #22672, 1000.000000000000000 ) ;
#42194=ORIENTED_EDGE ( 'NONE', *, *, #18152, .T. ) ;
#42206=EDGE_CURVE ( 'NONE', #33821, #32703, #24944, .T. ) ;
#42207=ORIENTED_EDGE ( 'NONE', *, *, #36938, .T. ) ;
#42212=VECTOR ( 'NONE', #41440, 1000.000000000000000 ) ;
#42222=DIRECTION ( 'NONE',  ( -1.000000000000000000, -0.000000000000000000, 0.000000000000000000 ) ) ;
#42224=AXIS2_PLACEMENT_3D ( 'NONE', #29710, #37541, #15752 ) ;
#42225=DIRECTION ( 'NONE',  ( 0.000000000000000000, 0.000000000000000000, 1.000000000000000000 ) ) ;
#42227=VERTEX_POINT ( 'NONE', #21989 ) ;
#42230=CARTESIAN_POINT ( 'NONE',  ( 10.00000000000000000, 62.50329211542494789, -41.76937507738723099 ) ) ;
#42231=VERTEX_POINT ( 'NONE', #21524 ) ;
#42236=CARTESIAN_POINT ( 'NONE',  ( 10.00000000000000000, -23.16143007188376757, -73.95703589263997912 ) ) ;
#42237=CARTESIAN_POINT ( 'NONE',  ( 0.000000000000000000, -12.93880638057258814, -76.41127070299285151 ) ) ;
#42242=FACE_OUTER_BOUND ( 'NONE', #42655, .T. ) ;
#42247=DIRECTION ( 'NONE',  ( 1.000000000000000000, 0.000000000000000000, 0.000000000000000000 ) ) ;
#42251=ADVANCED_FACE ( 'NONE', ( #36677 ), #32302, .T. ) ;
#42255=EDGE_CURVE ( 'NONE', #30674, #16029, #32541, .T. ) ;
#42262=ORIENTED_EDGE ( 'NONE', *, *, #6507, .T. ) ;
#42268=ORIENTED_EDGE ( 'NONE', *, *, #9821, .T. ) ;
#42273=EDGE_CURVE ( 'NONE', #13379, #19466, #21752, .T. ) ;
#42278=CYLINDRICAL_SURFACE ( 'NONE', #1926, 82.00000000000000000 ) ;
#42282=CARTESIAN_POINT ( 'NONE',  ( 10.00000000000000000, 72.35432306680455383, 20.40083707023012494 ) ) ;
#42288=EDGE_LOOP ( 'NONE', ( #38694, #3698, #9036, #18803 ) ) ;
#42300=ORIENTED_EDGE ( 'NONE', *, *, #24401, .T. ) ;
#42302=VERTEX_POINT ( 'NONE', #43789 ) ;
#42307=CIRCLE ( 'NONE', #17994, 77.49900000000000944 ) ;
#42308=LINE ( 'NONE', #8521, #22074 ) ;
#42322=CIRCLE ( 'NONE', #47750, 31.99999999999999289 ) ;
#42323=LINE ( 'NONE', #8779, #15203 ) ;
#42327=EDGE_LOOP ( 'NONE', ( #12636, #12446, #502, #27917 ) ) ;
#42336=CARTESIAN_POINT ( 'NONE',  ( 10.00000000000000000, -39.78640506895653317, 66.50666863321987421 ) ) ;
#42339=ORIENTED_EDGE ( 'NONE', *, *, #10847, .F. ) ;
#42341=ORIENTED_EDGE ( 'NONE', *, *, #43061, .F. ) ;
#42345=ORIENTED_EDGE ( 'NONE', *, *, #39810, .F. ) ;
#42348=CARTESIAN_POINT ( 'NONE',  ( 10.00000000000000000, 71.21200624218795383, 40.65526001592638039 ) ) ;
#42351=VERTEX_POINT ( 'NONE', #41578 ) ;
#42353=ORIENTED_EDGE ( 'NONE', *, *, #1723, .F. ) ;
#42354=EDGE_CURVE ( 'NONE', #25698, #10994, #36923, .T. ) ;
#42355=AXIS2_PLACEMENT_3D ( 'NONE', #7984, #653, #15582 ) ;
#42365=VECTOR ( 'NONE', #18384, 1000.000000000000000 ) ;
#42375=FACE_OUTER_BOUND ( 'NONE', #30006, .T. ) ;
#42376=CARTESIAN_POINT ( 'NONE',  ( 10.00000000000000000, 18.89407956138256139, 75.16055320797038064 ) ) ;
#42379=EDGE_CURVE ( 'NONE', #37110, #40588, #6478, .T. ) ;
#42385=VERTEX_POINT ( 'NONE', #37414 ) ;
#42387=ORIENTED_EDGE ( 'NONE', *, *, #19769, .T. ) ;
#42388=CARTESIAN_POINT ( 'NONE',  ( 10.00000000000000000, 58.39081064771823293, -50.95692526931266286 ) ) ;
#42389=AXIS2_PLACEMENT_3D ( 'NONE', #37914, #26900, #41351 ) ;
#42393=ADVANCED_FACE ( 'NONE', ( #25905 ), #4387, .T. ) ;
#42395=CIRCLE ( 'NONE', #32232, 31.99999999999999289 ) ;
#42399=VERTEX_POINT ( 'NONE', #19511 ) ;
#42405=CARTESIAN_POINT ( 'NONE',  ( 10.00000000000000000, 78.73519480814985627, -22.90783923731548910 ) ) ;
#42410=ORIENTED_EDGE ( 'NONE', *, *, #36623, .T. ) ;
#42416=ORIENTED_EDGE ( 'NONE', *, *, #31157, .F. ) ;
#42419=CARTESIAN_POINT ( 'NONE',  ( 0.000000000000000000, 56.15606465354959198, 59.75363087400094741 ) ) ;
#42420=AXIS2_PLACEMENT_3D ( 'NONE', #22258, #14184, #11245 ) ;
#42422=DIRECTION ( 'NONE',  ( -1.000000000000000000, 0.000000000000000000, -0.000000000000000000 ) ) ;
#42428=AXIS2_PLACEMENT_3D ( 'NONE', #12350, #823, #15767 ) ;
#42429=DIRECTION ( 'NONE',  ( -1.000000000000000000, 0.000000000000000000, 0.000000000000000000 ) ) ;
#42442=AXIS2_PLACEMENT_3D ( 'NONE', #12699, #45490, #20034 ) ;
#42444=CARTESIAN_POINT ( 'NONE',  ( 10.00000000000000000, 74.65491531819118620, -8.830959090342659579 ) ) ;
#42445=CIRCLE ( 'NONE', #44805, 77.49900000000002365 ) ;
#42446=ORIENTED_EDGE ( 'NONE', *, *, #21723, .T. ) ;
#42449=DIRECTION ( 'NONE',  ( -1.000000000000000000, 0.000000000000000000, 0.000000000000000000 ) ) ;
#42451=EDGE_CURVE ( 'NONE', #33614, #25524, #38527, .T. ) ;
#42453=VERTEX_POINT ( 'NONE', #7307 ) ;
#42458=EDGE_CURVE ( 'NONE', #4911, #32425, #4142, .T. ) ;
#42459=DIRECTION ( 'NONE',  ( -1.000000000000000000, 0.000000000000000000, 0.000000000000000000 ) ) ;
#42468=DIRECTION ( 'NONE',  ( 0.000000000000000000, 0.000000000000000000, 1.000000000000000000 ) ) ;
#42469=DIRECTION ( 'NONE',  ( 0.000000000000000000, 0.000000000000000000, 1.000000000000000000 ) ) ;
#42471=EDGE_LOOP ( 'NONE', ( #36216, #36743, #10230, #16308 ) ) ;
#42472=CIRCLE ( 'NONE', #6628, 82.00000000000000000 ) ;
#42475=EDGE_LOOP ( 'NONE', ( #21462, #29264, #5169, #15457 ) ) ;
#42476=CARTESIAN_POINT ( 'NONE',  ( 0.000000000000000000, -44.99326035066006568, -68.55367621811190304 ) ) ;
#42479=AXIS2_PLACEMENT_3D ( 'NONE', #30185, #45106, #41670 ) ;
#42491=DIRECTION ( 'NONE',  ( 0.000000000000000000, 0.3090169943749482839, -0.9510565162951533091 ) ) ;
#42493=DIRECTION ( 'NONE',  ( 0.000000000000000000, 0.5877852522924684742, 0.8090169943749506709 ) ) ;
#42515=AXIS2_PLACEMENT_3D ( 'NONE', #32803, #36488, #6641 ) ;
#42517=EDGE_CURVE ( 'NONE', #13398, #361, #2548, .T. ) ;
#42522=EDGE_LOOP ( 'NONE', ( #26392, #37876, #40379, #18918 ) ) ;
#42523=CIRCLE ( 'NONE', #44858, 82.00000000000000000 ) ;
#42530=ORIENTED_EDGE ( 'NONE', *, *, #47613, .T. ) ;
#42532=LINE ( 'NONE', #24650, #9248 ) ;
#42538=ORIENTED_EDGE ( 'NONE', *, *, #1187, .F. ) ;
#42543=AXIS2_PLACEMENT_3D ( 'NONE', #19300, #37665, #15408 ) ;
#42545=CIRCLE ( 'NONE', #22203, 12.50000000000000000 ) ;
#42546=ORIENTED_EDGE ( 'NONE', *, *, #23929, .F. ) ;
#42551=VERTEX_POINT ( 'NONE', #34949 ) ;
#42555=AXIS2_PLACEMENT_3D ( 'NONE', #25513, #29669, #22341 ) ;
#42558=EDGE_CURVE ( 'NONE', #41796, #36392, #30812, .T. ) ;
#42564=CARTESIAN_POINT ( 'NONE',  ( 10.00000000000000000, 0.000000000000000000, 0.000000000000000000 ) ) ;
#42565=DIRECTION ( 'NONE',  ( 0.000000000000000000, 0.000000000000000000, 1.000000000000000000 ) ) ;
#42576=ORIENTED_EDGE ( 'NONE', *, *, #44281, .T. ) ;
#42579=VECTOR ( 'NONE', #23224, 1000.000000000000000 ) ;
#42580=LINE ( 'NONE', #4638, #37093 ) ;
#42582=CIRCLE ( 'NONE', #12884, 31.99999999999999645 ) ;
#42588=CIRCLE ( 'NONE', #12898, 31.99999999999999645 ) ;
#42589=CARTESIAN_POINT ( 'NONE',  ( 0.000000000000000000, -66.50666863322028632, 39.78640506895582973 ) ) ;
#42591=ORIENTED_EDGE ( 'NONE', *, *, #28946, .T. ) ;
#42592=ORIENTED_EDGE ( 'NONE', *, *, #1583, .T. ) ;
#42596=ADVANCED_FACE ( 'NONE', ( #28096 ), #42064, .T. ) ;
#42598=ORIENTED_EDGE ( 'NONE', *, *, #13830, .T. ) ;
#42601=DIRECTION ( 'NONE',  ( -1.000000000000000000, -0.000000000000000000, -0.000000000000000000 ) ) ;
#42603=DIRECTION ( 'NONE',  ( 0.000000000000000000, 0.000000000000000000, 1.000000000000000000 ) ) ;
#42611=VERTEX_POINT ( 'NONE', #1430 ) ;
#42616=DIRECTION ( 'NONE',  ( -1.000000000000000000, -0.000000000000000000, -0.000000000000000000 ) ) ;
#42618=CARTESIAN_POINT ( 'NONE',  ( -10.00000000000000000, 0.000000000000000000, 0.000000000000000000 ) ) ;
#42629=DIRECTION ( 'NONE',  ( 0.000000000000000000, 0.000000000000000000, 1.000000000000000000 ) ) ;
#42633=CIRCLE ( 'NONE', #24630, 77.49899999999999523 ) ;
#42636=DIRECTION ( 'NONE',  ( -1.000000000000000000, -0.000000000000000000, -0.000000000000000000 ) ) ;
#42649=CARTESIAN_POINT ( 'NONE',  ( 0.000000000000000000, 51.03279382321088065, 55.19960302592086521 ) ) ;
#42650=VERTEX_POINT ( 'NONE', #28812 ) ;
#42651=( NAMED_UNIT ( * ) PLANE_ANGLE_UNIT ( ) SI_UNIT ( $, .RADIAN. ) );
#42653=VECTOR ( 'NONE', #33375, 1000.000000000000000 ) ;
#42655=EDGE_LOOP ( 'NONE', ( #48420, #19917, #36478, #43953 ) ) ;
#42656=CYLINDRICAL_SURFACE ( 'NONE', #27412, 31.99999999999998579 ) ;
#42657=ORIENTED_EDGE ( 'NONE', *, *, #23585, .T. ) ;
#42658=CYLINDRICAL_SURFACE ( 'NONE', #434, 31.99999999999999289 ) ;
#42666=DIRECTION ( 'NONE',  ( 0.000000000000000000, 0.000000000000000000, 1.000000000000000000 ) ) ;
#42669=CARTESIAN_POINT ( 'NONE',  ( 0.000000000000000000, 74.74816331893477184, -33.71516098798660011 ) ) ;
#42670=VERTEX_POINT ( 'NONE', #24667 ) ;
#42673=DIRECTION ( 'NONE',  ( 1.000000000000000000, 0.000000000000000000, 0.000000000000000000 ) ) ;
#42679=ORIENTED_EDGE ( 'NONE', *, *, #36242, .F. ) ;
#42682=DIRECTION ( 'NONE',  ( 0.000000000000000000, 0.000000000000000000, 1.000000000000000000 ) ) ;
#42689=DIRECTION ( 'NONE',  ( -1.000000000000000000, 0.000000000000000000, 0.000000000000000000 ) ) ;
#42692=DIRECTION ( 'NONE',  ( 1.000000000000000000, 0.000000000000000000, 0.000000000000000000 ) ) ;
#42695=AXIS2_PLACEMENT_3D ( 'NONE', #34752, #8799, #16173 ) ;
#42705=EDGE_LOOP ( 'NONE', ( #38983, #13870, #45853, #33702 ) ) ;
#42706=CIRCLE ( 'NONE', #46622, 31.99999999999999645 ) ;
#42707=EDGE_LOOP ( 'NONE', ( #18729, #21497, #40810, #6065 ) ) ;
#42712=LINE ( 'NONE', #27298, #26564 ) ;
#42719=ADVANCED_FACE ( 'NONE', ( #32492 ), #7014, .T. ) ;
#42722=DIRECTION ( 'NONE',  ( 0.000000000000000000, -0.1564344650402381132, 0.9876883405951365491 ) ) ;
#42725=ORIENTED_EDGE ( 'NONE', *, *, #42839, .F. ) ;
#42726=ORIENTED_EDGE ( 'NONE', *, *, #41435, .F. ) ;
#42741=FACE_OUTER_BOUND ( 'NONE', #23485, .T. ) ;
#42742=CARTESIAN_POINT ( 'NONE',  ( -10.00000000000000000, 0.000000000000000000, 0.000000000000000000 ) ) ;
#42744=LINE ( 'NONE', #5296, #47306 ) ;
#42748=CARTESIAN_POINT ( 'NONE',  ( 10.00000000000000000, 0.000000000000000000, 0.000000000000000000 ) ) ;
#42751=CARTESIAN_POINT ( 'NONE',  ( 0.000000000000000000, 0.000000000000000000, 0.000000000000000000 ) ) ;
#42752=CYLINDRICAL_SURFACE ( 'NONE', #39698, 82.00000000000000000 ) ;
#42755=CARTESIAN_POINT ( 'NONE',  ( 10.00000000000000000, 0.000000000000000000, 0.000000000000000000 ) ) ;
#42756=CARTESIAN_POINT ( 'NONE',  ( 0.000000000000000000, -80.28980883073769803, 16.65972982744906261 ) ) ;
#42758=DIRECTION ( 'NONE',  ( -1.000000000000000000, 0.000000000000000000, -0.000000000000000000 ) ) ;
#42760=CARTESIAN_POINT ( 'NONE',  ( 10.00000000000000000, -77.49459641780886443, -0.8261519478439277586 ) ) ;
#42763=VECTOR ( 'NONE', #33872, 1000.000000000000000 ) ;
#42768=DIRECTION ( 'NONE',  ( 0.000000000000000000, 0.000000000000000000, 1.000000000000000000 ) ) ;
#42771=DIRECTION ( 'NONE',  ( -1.000000000000000000, -0.000000000000000000, 0.000000000000000000 ) ) ;
#42774=VERTEX_POINT ( 'NONE', #22669 ) ;
#42778=DIRECTION ( 'NONE',  ( 0.000000000000000000, -0.07845909572783053842, -0.9969173337331290741 ) ) ;
#42782=DIRECTION ( 'NONE',  ( -1.000000000000000000, -0.000000000000000000, -0.000000000000000000 ) ) ;
#42783=EDGE_LOOP ( 'NONE', ( #10830, #26579, #44339, #16043 ) ) ;
#42786=ORIENTED_EDGE ( 'NONE', *, *, #3136, .T. ) ;
#42795=EDGE_LOOP ( 'NONE', ( #33549, #22473, #3145, #24809 ) ) ;
#42802=CARTESIAN_POINT ( 'NONE',  ( 10.00000000000000000, 51.29473840253223926, 63.97538442413446091 ) ) ;
#42804=DIRECTION ( 'NONE',  ( -1.000000000000000000, 0.000000000000000000, 0.000000000000000000 ) ) ;
#42809=CARTESIAN_POINT ( 'NONE',  ( 5.000000000000000000, 51.29473840253317718, -63.97538442413369353 ) ) ;
#42813=ORIENTED_EDGE ( 'NONE', *, *, #25354, .T. ) ;
#42815=DIRECTION ( 'NONE',  ( -1.000000000000000000, -0.000000000000000000, 0.000000000000000000 ) ) ;
#42819=EDGE_LOOP ( 'NONE', ( #9181, #11186, #46122, #32983 ) ) ;
#42820=ORIENTED_EDGE ( 'NONE', *, *, #20169, .F. ) ;
#42822=ADVANCED_FACE ( 'NONE', ( #26828 ), #3335, .T. ) ;
#42833=ORIENTED_EDGE ( 'NONE', *, *, #11344, .F. ) ;
#42838=DIRECTION ( 'NONE',  ( -1.000000000000000000, 0.000000000000000000, 0.000000000000000000 ) ) ;
#42839=EDGE_CURVE ( 'NONE', #18610, #20071, #6509, .T. ) ;
#42842=CARTESIAN_POINT ( 'NONE',  ( 10.00000000000000000, 0.000000000000000000, 0.000000000000000000 ) ) ;
#42844=CYLINDRICAL_SURFACE ( 'NONE', #25956, 31.99999999999999289 ) ;
#42846=CYLINDRICAL_SURFACE ( 'NONE', #38414, 32.00000000000000000 ) ;
#42849=CARTESIAN_POINT ( 'NONE',  ( 5.000000000000002665, 2.543863470249527303, -81.96053171279901051 ) ) ;
#42850=FACE_OUTER_BOUND ( 'NONE', #12117, .T. ) ;
#42851=DIRECTION ( 'NONE',  ( -1.000000000000000000, 0.000000000000000000, 0.000000000000000000 ) ) ;
#42857=ORIENTED_EDGE ( 'NONE', *, *, #8871, .T. ) ;
#42858=DIRECTION ( 'NONE',  ( 1.000000000000000000, 0.000000000000000000, 0.000000000000000000 ) ) ;
#42862=CARTESIAN_POINT ( 'NONE',  ( 0.000000000000000000, 0.000000000000000000, 0.000000000000000000 ) ) ;
#42865=ADVANCED_FACE ( 'NONE', ( #37116 ), #48374, .T. ) ;
#42868=DIRECTION ( 'NONE',  ( 0.000000000000000000, 0.5877852522924743583, -0.8090169943749466741 ) ) ;
#42878=EDGE_CURVE ( 'NONE', #747, #6258, #1611, .T. ) ;
#42879=FACE_OUTER_BOUND ( 'NONE', #16345, .T. ) ;
#42885=EDGE_CURVE ( 'NONE', #35650, #46082, #233, .T. ) ;
#42895=ORIENTED_EDGE ( 'NONE', *, *, #46743, .T. ) ;
#42899=EDGE_CURVE ( 'NONE', #29274, #828, #4173, .T. ) ;
#42900=VECTOR ( 'NONE', #29055, 1000.000000000000000 ) ;
#42901=DIRECTION ( 'NONE',  ( 1.000000000000000000, 0.000000000000000000, 0.000000000000000000 ) ) ;
#42902=ORIENTED_EDGE ( 'NONE', *, *, #23600, .T. ) ;
#42906=CARTESIAN_POINT ( 'NONE',  ( 10.00000000000000000, 0.000000000000000000, 0.000000000000000000 ) ) ;
#42908=LINE ( 'NONE', #20368, #38134 ) ;
#42909=ORIENTED_EDGE ( 'NONE', *, *, #12830, .T. ) ;
#42910=ORIENTED_EDGE ( 'NONE', *, *, #34640, .T. ) ;
#42912=EDGE_LOOP ( 'NONE', ( #10523, #16824, #11404, #27941 ) ) ;
#42913=FACE_OUTER_BOUND ( 'NONE', #8194, .T. ) ;
#42926=DIRECTION ( 'NONE',  ( 1.000000000000000000, -0.000000000000000000, -0.000000000000000000 ) ) ;
#42936=AXIS2_PLACEMENT_3D ( 'NONE', #41566, #34206, #444 ) ;
#42945=EDGE_CURVE ( 'NONE', #34021, #1544, #8948, .T. ) ;
#42950=DIRECTION ( 'NONE',  ( -1.000000000000000000, 0.000000000000000000, 0.000000000000000000 ) ) ;
#42951=VERTEX_POINT ( 'NONE', #20435 ) ;
#42952=EDGE_LOOP ( 'NONE', ( #40322, #895, #23025, #4888 ) ) ;
#42958=CARTESIAN_POINT ( 'NONE',  ( 0.000000000000000000, 0.000000000000000000, 0.000000000000000000 ) ) ;
#42959=CYLINDRICAL_SURFACE ( 'NONE', #37641, 77.49899999999999523 ) ;
#42963=CIRCLE ( 'NONE', #39857, 77.49900000000000944 ) ;
#42967=CIRCLE ( 'NONE', #14061, 31.99999999999999289 ) ;
#42976=CARTESIAN_POINT ( 'NONE',  ( 10.00000000000000000, 68.55367621811204515, -44.99326035065983120 ) ) ;
#42983=DIRECTION ( 'NONE',  ( 0.000000000000000000, 0.000000000000000000, 1.000000000000000000 ) ) ;
#43002=ORIENTED_EDGE ( 'NONE', *, *, #44583, .T. ) ;
#43006=ORIENTED_EDGE ( 'NONE', *, *, #26562, .T. ) ;
#43010=EDGE_LOOP ( 'NONE', ( #32137, #20047, #20807, #898 ) ) ;
#43011=ORIENTED_EDGE ( 'NONE', *, *, #30065, .T. ) ;
#43014=ADVANCED_FACE ( 'NONE', ( #45924 ), #8692, .T. ) ;
#43019=VERTEX_POINT ( 'NONE', #13350 ) ;
#43023=CARTESIAN_POINT ( 'NONE',  ( 10.00000000000000000, 0.000000000000000000, 2.500000000000000000 ) ) ;
#43029=CARTESIAN_POINT ( 'NONE',  ( 0.000000000000000000, 77.16300072079660310, 27.74655509720696500 ) ) ;
#43033=AXIS2_PLACEMENT_3D ( 'NONE', #27358, #34434, #30796 ) ;
#43036=AXIS2_PLACEMENT_3D ( 'NONE', #9057, #1713, #12981 ) ;
#43043=DIRECTION ( 'NONE',  ( 0.000000000000000000, 0.9969173337331281859, -0.07845909572784180719 ) ) ;
#43045=ADVANCED_FACE ( 'NONE', ( #28269 ), #9665, .T. ) ;
#43048=DIRECTION ( 'NONE',  ( 0.000000000000000000, 0.000000000000000000, 1.000000000000000000 ) ) ;
#43052=EDGE_LOOP ( 'NONE', ( #691, #17418, #21002, #6110 ) ) ;
#43054=CARTESIAN_POINT ( 'NONE',  ( 0.000000000000000000, -44.88180994100421373, 63.18004540533011948 ) ) ;
#43055=CARTESIAN_POINT ( 'NONE',  ( 10.00000000000000000, 2.956366410620650420, 75.11725578898469280 ) ) ;
#43059=ORIENTED_EDGE ( 'NONE', *, *, #27905, .F. ) ;
#43061=EDGE_CURVE ( 'NONE', #37949, #24526, #44065, .T. ) ;
#43073=AXIS2_PLACEMENT_3D ( 'NONE', #19514, #30086, #34454 ) ;
#43076=ORIENTED_EDGE ( 'NONE', *, *, #8611, .F. ) ;
#43079=DIRECTION ( 'NONE',  ( 0.000000000000000000, 0.000000000000000000, 1.000000000000000000 ) ) ;
#43080=ORIENTED_EDGE ( 'NONE', *, *, #39531, .F. ) ;
#43082=ORIENTED_EDGE ( 'NONE', *, *, #41549, .F. ) ;
#43083=DIRECTION ( 'NONE',  ( -1.000000000000000000, -0.000000000000000000, -0.000000000000000000 ) ) ;
#43086=ORIENTED_EDGE ( 'NONE', *, *, #43676, .F. ) ;
#43088=DIRECTION ( 'NONE',  ( -1.000000000000000000, 0.000000000000000000, -0.000000000000000000 ) ) ;
#43090=VERTEX_POINT ( 'NONE', #28987 ) ;
#43106=CYLINDRICAL_SURFACE ( 'NONE', #10769, 77.49899999999999523 ) ;
#43108=AXIS2_PLACEMENT_3D ( 'NONE', #32767, #2669, #17127 ) ;
#43111=EDGE_CURVE ( 'NONE', #31962, #23138, #6250, .T. ) ;
#43113=ADVANCED_FACE ( 'NONE', ( #5769 ), #43461, .T. ) ;
#43115=AXIS2_PLACEMENT_3D ( 'NONE', #9776, #42601, #27666 ) ;
#43119=ORIENTED_EDGE ( 'NONE', *, *, #34080, .F. ) ;
#43120=ORIENTED_EDGE ( 'NONE', *, *, #45379, .F. ) ;
#43121=EDGE_CURVE ( 'NONE', #30853, #21451, #32340, .T. ) ;
#43123=ORIENTED_EDGE ( 'NONE', *, *, #36779, .F. ) ;
#43129=CARTESIAN_POINT ( 'NONE',  ( 10.00000000000000000, -41.76937507738745836, -62.50329211542482710 ) ) ;
#43132=ORIENTED_EDGE ( 'NONE', *, *, #34655, .T. ) ;
#43141=CARTESIAN_POINT ( 'NONE',  ( 0.000000000000000000, 81.90746397400393164, -3.894527615416986333 ) ) ;
#43143=DIRECTION ( 'NONE',  ( -1.000000000000000000, 0.000000000000000000, 0.000000000000000000 ) ) ;
#43144=CARTESIAN_POINT ( 'NONE',  ( 10.00000000000000000, 10.30890764327382847, 81.34940948281339956 ) ) ;
#43148=CYLINDRICAL_SURFACE ( 'NONE', #33285, 31.99999999999999289 ) ;
#43149=ORIENTED_EDGE ( 'NONE', *, *, #27640, .F. ) ;
#43152=CARTESIAN_POINT ( 'NONE',  ( 5.000000000000000000, -50.23322058963393744, 64.81221759200325039 ) ) ;
#43158=DIRECTION ( 'NONE',  ( 0.000000000000000000, 0.000000000000000000, 1.000000000000000000 ) ) ;
#43164=CARTESIAN_POINT ( 'NONE',  ( 10.00000000000000000, 36.72794159290241822, 65.59268652807223532 ) ) ;
#43166=DIRECTION ( 'NONE',  ( -1.000000000000000000, -0.000000000000000000, 0.000000000000000000 ) ) ;
#43170=CARTESIAN_POINT ( 'NONE',  ( 10.00000000000000000, -8.840884882375609877, 74.65374052328647281 ) ) ;
#43173=CYLINDRICAL_SURFACE ( 'NONE', #43304, 82.00000000000000000 ) ;
#43186=AXIS2_PLACEMENT_3D ( 'NONE', #7801, #45744, #12223 ) ;
#43187=ORIENTED_EDGE ( 'NONE', *, *, #23640, .T. ) ;
#43190=DIRECTION ( 'NONE',  ( -1.000000000000000000, 0.000000000000000000, -0.000000000000000000 ) ) ;
#43192=DIRECTION ( 'NONE',  ( 0.000000000000000000, 0.000000000000000000, 1.000000000000000000 ) ) ;
#43195=AXIS2_PLACEMENT_3D ( 'NONE', #17671, #23879, #36273 ) ;
#43200=AXIS2_PLACEMENT_3D ( 'NONE', #34699, #38884, #35184 ) ;
#43203=DIRECTION ( 'NONE',  ( -1.000000000000000000, 0.000000000000000000, 0.000000000000000000 ) ) ;
#43205=DIRECTION ( 'NONE',  ( 0.000000000000000000, 0.000000000000000000, 1.000000000000000000 ) ) ;
#43211=DIRECTION ( 'NONE',  ( 0.000000000000000000, 0.000000000000000000, 1.000000000000000000 ) ) ;
#43217=DIRECTION ( 'NONE',  ( 0.000000000000000000, 0.000000000000000000, 1.000000000000000000 ) ) ;
#43218=DIRECTION ( 'NONE',  ( 0.000000000000000000, 0.000000000000000000, 1.000000000000000000 ) ) ;
#43226=EDGE_CURVE ( 'NONE', #12437, #24420, #26533, .T. ) ;
#43233=CIRCLE ( 'NONE', #30721, 82.00000000000000000 ) ;
#43246=VERTEX_POINT ( 'NONE', #22384 ) ;
#43251=DIRECTION ( 'NONE',  ( -1.000000000000000000, 0.000000000000000000, -0.000000000000000000 ) ) ;
#43256=EDGE_LOOP ( 'NONE', ( #1088, #14342, #24994, #27120 ) ) ;
#43258=ORIENTED_EDGE ( 'NONE', *, *, #22101, .T. ) ;
#43262=EDGE_CURVE ( 'NONE', #25818, #1310, #41233, .T. ) ;
#43267=EDGE_CURVE ( 'NONE', #18503, #28263, #44171, .T. ) ;
#43269=DIRECTION ( 'NONE',  ( -1.000000000000000000, -0.000000000000000000, 0.000000000000000000 ) ) ;
#43270=DIRECTION ( 'NONE',  ( -1.000000000000000000, 0.000000000000000000, 0.000000000000000000 ) ) ;
#43273=ORIENTED_EDGE ( 'NONE', *, *, #21664, .F. ) ;
#43278=CARTESIAN_POINT ( 'NONE',  ( 10.00000000000000000, 73.73191006444551476, 14.66109333815590254 ) ) ;
#43288=AXIS2_PLACEMENT_3D ( 'NONE', #43472, #24136, #43218 ) ;
#43291=CARTESIAN_POINT ( 'NONE',  ( 0.000000000000000000, -51.29473840253270112, 63.97538442413407012 ) ) ;
#43297=ORIENTED_EDGE ( 'NONE', *, *, #31750, .T. ) ;
#43304=AXIS2_PLACEMENT_3D ( 'NONE', #22689, #4099, #425 ) ;
#43307=VECTOR ( 'NONE', #45362, 1000.000000000000000 ) ;
#43310=EDGE_LOOP ( 'NONE', ( #39023, #30128, #24511, #18430 ) ) ;
#43312=ORIENTED_EDGE ( 'NONE', *, *, #11111, .T. ) ;
#43313=ORIENTED_EDGE ( 'NONE', *, *, #23288, .F. ) ;
#43318=ORIENTED_EDGE ( 'NONE', *, *, #1723, .T. ) ;
#43320=ORIENTED_EDGE ( 'NONE', *, *, #18537, .F. ) ;
#43321=CIRCLE ( 'NONE', #5016, 82.00000000000000000 ) ;
#43346=LINE ( 'NONE', #21285, #43496 ) ;
#43350=CARTESIAN_POINT ( 'NONE',  ( 10.00000000000000000, 0.000000000000000000, 0.000000000000000000 ) ) ;
#43352=AXIS2_PLACEMENT_3D ( 'NONE', #40718, #22599, #4254 ) ;
#43363=DIRECTION ( 'NONE',  ( 0.000000000000000000, 0.000000000000000000, 1.000000000000000000 ) ) ;
#43373=ORIENTED_EDGE ( 'NONE', *, *, #38815, .F. ) ;
#43374=DIRECTION ( 'NONE',  ( -1.000000000000000000, 0.000000000000000000, 0.000000000000000000 ) ) ;
#43376=DIRECTION ( 'NONE',  ( -1.000000000000000000, -0.000000000000000000, 0.000000000000000000 ) ) ;
#43379=DIRECTION ( 'NONE',  ( 0.000000000000000000, 0.000000000000000000, 1.000000000000000000 ) ) ;
#43380=ORIENTED_EDGE ( 'NONE', *, *, #2335, .F. ) ;
#43386=CARTESIAN_POINT ( 'NONE',  ( 0.000000000000000000, 50.95692526931328104, 58.39081064771769292 ) ) ;
#43387=DIRECTION ( 'NONE',  ( -1.000000000000000000, -0.000000000000000000, -0.000000000000000000 ) ) ;
#43391=CARTESIAN_POINT ( 'NONE',  ( -10.00000000000000000, 0.000000000000000000, 0.000000000000000000 ) ) ;
#43394=EDGE_CURVE ( 'NONE', #14647, #1729, #8411, .T. ) ;
#43401=CYLINDRICAL_SURFACE ( 'NONE', #40967, 77.49899999999999523 ) ;
#43409=DIRECTION ( 'NONE',  ( 0.000000000000000000, 0.9510565162951544194, -0.3090169943749448422 ) ) ;
#43411=DIRECTION ( 'NONE',  ( -1.000000000000000000, 0.000000000000000000, 0.000000000000000000 ) ) ;
#43414=CIRCLE ( 'NONE', #25419, 31.99999999999998579 ) ;
#43416=DIRECTION ( 'NONE',  ( -1.000000000000000000, 0.000000000000000000, 0.000000000000000000 ) ) ;
#43425=CARTESIAN_POINT ( 'NONE',  ( 10.00000000000000000, -35.91791733033426226, -68.67312586195033930 ) ) ;
#43426=ORIENTED_EDGE ( 'NONE', *, *, #27156, .T. ) ;
#43429=VECTOR ( 'NONE', #36022, 1000.000000000000000 ) ;
#43431=CIRCLE ( 'NONE', #25445, 77.49900000000000944 ) ;
#43434=CIRCLE ( 'NONE', #16845, 77.49900000000000944 ) ;
#43438=ORIENTED_EDGE ( 'NONE', *, *, #14320, .T. ) ;
#43440=DIRECTION ( 'NONE',  ( -1.000000000000000000, -0.000000000000000000, -0.000000000000000000 ) ) ;
#43442=VERTEX_POINT ( 'NONE', #4737 ) ;
#43446=ORIENTED_EDGE ( 'NONE', *, *, #44687, .T. ) ;
#43449=DIRECTION ( 'NONE',  ( -1.000000000000000000, 0.000000000000000000, 0.000000000000000000 ) ) ;
#43461=CYLINDRICAL_SURFACE ( 'NONE', #19039, 77.49899999999999523 ) ;
#43463=CARTESIAN_POINT ( 'NONE',  ( 10.00000000000000000, -46.53671651293907274, -59.03961581697448935 ) ) ;
#43467=ORIENTED_EDGE ( 'NONE', *, *, #30008, .T. ) ;
#43468=VERTEX_POINT ( 'NONE', #29595 ) ;
#43472=CARTESIAN_POINT ( 'NONE',  ( -10.00000000000000000, 0.000000000000000000, 0.000000000000000000 ) ) ;
#43474=CARTESIAN_POINT ( 'NONE',  ( 0.000000000000000000, 8.840884882376133902, -74.65374052328640175 ) ) ;
#43476=CYLINDRICAL_SURFACE ( 'NONE', #3671, 82.00000000000000000 ) ;
#43490=ORIENTED_EDGE ( 'NONE', *, *, #12544, .T. ) ;
#43493=CARTESIAN_POINT ( 'NONE',  ( 10.00000000000000000, -62.50884508063453637, 41.76106447765467777 ) ) ;
#43494=CARTESIAN_POINT ( 'NONE',  ( 0.000000000000000000, 39.47590169984846398, 71.87247863392428826 ) ) ;
#43495=VERTEX_POINT ( 'NONE', #9367 ) ;
#43496=VECTOR ( 'NONE', #24739, 1000.000000000000000 ) ;
#43499=ORIENTED_EDGE ( 'NONE', *, *, #39518, .T. ) ;
#43501=DIRECTION ( 'NONE',  ( -1.000000000000000000, -0.000000000000000000, -0.000000000000000000 ) ) ;
#43502=DIRECTION ( 'NONE',  ( 0.000000000000000000, 0.1564344650402244852, 0.9876883405951387696 ) ) ;
#43511=ADVANCED_FACE ( 'NONE', ( #2049 ), #43401, .T. ) ;
#43516=DIRECTION ( 'NONE',  ( 0.000000000000000000, 0.3826834323650841752, 0.9238795325112891810 ) ) ;
#43536=VERTEX_POINT ( 'NONE', #9857 ) ;
#43543=EDGE_CURVE ( 'NONE', #26599, #39866, #2265, .T. ) ;
#43544=VERTEX_POINT ( 'NONE', #36282 ) ;
#43547=ORIENTED_EDGE ( 'NONE', *, *, #13995, .F. ) ;
#43555=ORIENTED_EDGE ( 'NONE', *, *, #32459, .F. ) ;
#43558=CARTESIAN_POINT ( 'NONE',  ( 10.00000000000000000, -41.19522573413780009, 65.64334221924896440 ) ) ;
#43559=AXIS2_PLACEMENT_3D ( 'NONE', #43754, #3605, #14869 ) ;
#43568=CIRCLE ( 'NONE', #9951, 77.49899999999999523 ) ;
#43578=AXIS2_PLACEMENT_3D ( 'NONE', #22143, #37560, #18479 ) ;
#43579=CARTESIAN_POINT ( 'NONE',  ( -10.00000000000000000, 0.000000000000000000, 0.000000000000000000 ) ) ;
#43580=DIRECTION ( 'NONE',  ( 0.000000000000000000, 0.000000000000000000, -1.000000000000000000 ) ) ;
#43582=DIRECTION ( 'NONE',  ( 0.000000000000000000, 0.000000000000000000, 1.000000000000000000 ) ) ;
#43586=CYLINDRICAL_SURFACE ( 'NONE', #30310, 82.00000000000000000 ) ;
#43589=CIRCLE ( 'NONE', #22482, 32.00000000000000000 ) ;
#43590=EDGE_CURVE ( 'NONE', #25422, #18426, #20882, .T. ) ;
#43600=ORIENTED_EDGE ( 'NONE', *, *, #12280, .T. ) ;
#43606=AXIS2_PLACEMENT_3D ( 'NONE', #25369, #14364, #21705 ) ;
#43613=ORIENTED_EDGE ( 'NONE', *, *, #47840, .F. ) ;
#43620=CARTESIAN_POINT ( 'NONE',  ( 10.00000000000000000, 0.000000000000000000, 0.000000000000000000 ) ) ;
#43622=LINE ( 'NONE', #10086, #9206 ) ;
#43623=ORIENTED_EDGE ( 'NONE', *, *, #17683, .F. ) ;
#43624=ORIENTED_EDGE ( 'NONE', *, *, #36527, .F. ) ;
#43628=DIRECTION ( 'NONE',  ( -1.000000000000000000, -0.000000000000000000, 0.000000000000000000 ) ) ;
#43637=ORIENTED_EDGE ( 'NONE', *, *, #11406, .F. ) ;
#43638=DIRECTION ( 'NONE',  ( 0.000000000000000000, -0.9876883405951393247, 0.1564344650402207382 ) ) ;
#43640=CARTESIAN_POINT ( 'NONE',  ( 0.000000000000000000, 0.000000000000000000, 0.000000000000000000 ) ) ;
#43642=ORIENTED_EDGE ( 'NONE', *, *, #18152, .F. ) ;
#43646=ORIENTED_EDGE ( 'NONE', *, *, #25614, .F. ) ;
#43648=VERTEX_POINT ( 'NONE', #19058 ) ;
#43651=EDGE_LOOP ( 'NONE', ( #29649, #4004, #22633, #17517 ) ) ;
#43653=EDGE_CURVE ( 'NONE', #40145, #11579, #46455, .T. ) ;
#43655=EDGE_CURVE ( 'NONE', #10143, #270, #21423, .T. ) ;
#43657=VERTEX_POINT ( 'NONE', #4399 ) ;
#43660=ORIENTED_EDGE ( 'NONE', *, *, #31435, .T. ) ;
#43661=AXIS2_PLACEMENT_3D ( 'NONE', #15079, #26339, #41272 ) ;
#43663=EDGE_CURVE ( 'NONE', #28709, #39014, #11248, .T. ) ;
#43665=CARTESIAN_POINT ( 'NONE',  ( 10.00000000000000000, 56.15606465355042332, -59.75363087400016582 ) ) ;
#43666=ORIENTED_EDGE ( 'NONE', *, *, #26749, .T. ) ;
#43669=DIRECTION ( 'NONE',  ( 0.000000000000000000, 0.9876883405951371042, 0.1564344650402346437 ) ) ;
#43676=EDGE_CURVE ( 'NONE', #13460, #1544, #33171, .T. ) ;
#43677=ORIENTED_EDGE ( 'NONE', *, *, #2526, .F. ) ;
#43687=DIRECTION ( 'NONE',  ( 1.000000000000000000, 0.000000000000000000, 0.000000000000000000 ) ) ;
#43702=EDGE_CURVE ( 'NONE', #26319, #14647, #39436, .T. ) ;
#43703=CARTESIAN_POINT ( 'NONE',  ( -10.00000000000000000, 0.000000000000000000, 0.000000000000000000 ) ) ;
#43709=EDGE_CURVE ( 'NONE', #21451, #30509, #34728, .T. ) ;
#43717=DIRECTION ( 'NONE',  ( -1.000000000000000000, -0.000000000000000000, -0.000000000000000000 ) ) ;
#43728=CARTESIAN_POINT ( 'NONE',  ( 5.000000000000002665, -81.90746397400393164, 3.894527615417586741 ) ) ;
#43731=CYLINDRICAL_SURFACE ( 'NONE', #22526, 82.00000000000000000 ) ;
#43732=DIRECTION ( 'NONE',  ( 0.000000000000000000, 0.000000000000000000, 1.000000000000000000 ) ) ;
#43740=CARTESIAN_POINT ( 'NONE',  ( 0.000000000000000000, -74.65491531819124305, 8.830959090342128448 ) ) ;
#43747=ORIENTED_EDGE ( 'NONE', *, *, #22697, .T. ) ;
#43748=FACE_OUTER_BOUND ( 'NONE', #37877, .T. ) ;
#43750=DIRECTION ( 'NONE',  ( 0.000000000000000000, 0.7604059656000277112, 0.6494480483301875440 ) ) ;
#43751=CARTESIAN_POINT ( 'NONE',  ( 10.00000000000000000, -50.95692526931372157, 58.39081064771733054 ) ) ;
#43753=CYLINDRICAL_SURFACE ( 'NONE', #44302, 77.49899999999999523 ) ;
#43754=CARTESIAN_POINT ( 'NONE',  ( 10.00000000000000000, 65.58780272294076497, 36.73666225445916211 ) ) ;
#43755=EDGE_CURVE ( 'NONE', #15196, #13603, #25346, .T. ) ;
#43758=DIRECTION ( 'NONE',  ( 0.000000000000000000, -0.7604059656000369261, 0.6494480483301766638 ) ) ;
#43762=DIRECTION ( 'NONE',  ( 0.000000000000000000, -0.7604059656000228262, -0.6494480483301932061 ) ) ;
#43764=ADVANCED_FACE ( 'NONE', ( #3066 ), #32932, .T. ) ;
#43769=EDGE_CURVE ( 'NONE', #11292, #20770, #26963, .T. ) ;
#43772=ORIENTED_EDGE ( 'NONE', *, *, #38071, .F. ) ;
#43773=DIRECTION ( 'NONE',  ( 1.000000000000000000, -0.000000000000000000, -0.000000000000000000 ) ) ;
#43774=ORIENTED_EDGE ( 'NONE', *, *, #12280, .F. ) ;
#43775=EDGE_LOOP ( 'NONE', ( #40920, #40338, #45524, #89 ) ) ;
#43783=FACE_OUTER_BOUND ( 'NONE', #45585, .T. ) ;
#43787=CIRCLE ( 'NONE', #22688, 77.49899999999999523 ) ;
#43789=CARTESIAN_POINT ( 'NONE',  ( 0.000000000000000000, -22.90783923731575911, -78.73519480814978522 ) ) ;
#43794=AXIS2_PLACEMENT_3D ( 'NONE', #29237, #32436, #22125 ) ;
#43799=ORIENTED_EDGE ( 'NONE', *, *, #44924, .F. ) ;
#43801=CARTESIAN_POINT ( 'NONE',  ( 0.000000000000000000, -71.91182617369207719, 28.89263327155721228 ) ) ;
#43803=VERTEX_POINT ( 'NONE', #3308 ) ;
#43805=CARTESIAN_POINT ( 'NONE',  ( 0.000000000000000000, -27.74655509720617275, -77.16300072079690153 ) ) ;
#43810=DIRECTION ( 'NONE',  ( -1.000000000000000000, 0.000000000000000000, 0.000000000000000000 ) ) ;
#43814=DIRECTION ( 'NONE',  ( 0.000000000000000000, 0.9969173337331281859, -0.07845909572784168229 ) ) ;
#43824=VECTOR ( 'NONE', #29428, 1000.000000000000000 ) ;
#43832=DIRECTION ( 'NONE',  ( 0.000000000000000000, 0.9876883405951383255, -0.1564344650402276216 ) ) ;
#43833=VERTEX_POINT ( 'NONE', #15791 ) ;
#43837=EDGE_CURVE ( 'NONE', #14170, #43657, #2686, .T. ) ;
#43842=ORIENTED_EDGE ( 'NONE', *, *, #3235, .T. ) ;
#43843=LINE ( 'NONE', #36258, #44970 ) ;
#43853=VERTEX_POINT ( 'NONE', #847 ) ;
#43854=AXIS2_PLACEMENT_3D ( 'NONE', #25114, #28567, #40064 ) ;
#43857=ORIENTED_EDGE ( 'NONE', *, *, #2245, .F. ) ;
#43867=VERTEX_POINT ( 'NONE', #12140 ) ;
#43868=ADVANCED_FACE ( 'NONE', ( #23367 ), #38302, .T. ) ;
#43876=DIRECTION ( 'NONE',  ( 0.000000000000000000, 0.000000000000000000, 1.000000000000000000 ) ) ;
#43879=DIRECTION ( 'NONE',  ( -1.000000000000000000, 0.000000000000000000, 0.000000000000000000 ) ) ;
#43895=AXIS2_PLACEMENT_3D ( 'NONE', #4807, #12405, #27825 ) ;
#43901=CYLINDRICAL_SURFACE ( 'NONE', #36222, 31.99999999999999289 ) ;
#43906=ORIENTED_EDGE ( 'NONE', *, *, #29111, .T. ) ;
#43908=ORIENTED_EDGE ( 'NONE', *, *, #38296, .F. ) ;
#43911=DIRECTION ( 'NONE',  ( 1.000000000000000000, 0.000000000000000000, 0.000000000000000000 ) ) ;
#43921=DIRECTION ( 'NONE',  ( 0.000000000000000000, 0.000000000000000000, 1.000000000000000000 ) ) ;
#43925=DIRECTION ( 'NONE',  ( 0.000000000000000000, -0.7604059656000368150, 0.6494480483301767748 ) ) ;
#43933=CARTESIAN_POINT ( 'NONE',  ( 10.00000000000000000, -24.73286445877757345, 73.44644590900053061 ) ) ;
#43938=VERTEX_POINT ( 'NONE', #9188 ) ;
#43942=CARTESIAN_POINT ( 'NONE',  ( 10.00000000000000000, 36.73666225445988687, -65.58780272294035285 ) ) ;
#43953=ORIENTED_EDGE ( 'NONE', *, *, #29796, .T. ) ;
#43954=AXIS2_PLACEMENT_3D ( 'NONE', #28479, #46840, #2762 ) ;
#43957=DIRECTION ( 'NONE',  ( 0.000000000000000000, 0.000000000000000000, 1.000000000000000000 ) ) ;
#43958=CIRCLE ( 'NONE', #19694, 12.50000000000000000 ) ;
#43963=ORIENTED_EDGE ( 'NONE', *, *, #12620, .T. ) ;
#43969=VERTEX_POINT ( 'NONE', #47367 ) ;
#43984=DIRECTION ( 'NONE',  ( -1.000000000000000000, 0.000000000000000000, -0.000000000000000000 ) ) ;
#43992=DIRECTION ( 'NONE',  ( 0.000000000000000000, -0.8910065241883627918, -0.4539904997395567965 ) ) ;
#43998=CIRCLE ( 'NONE', #20538, 82.00000000000000000 ) ;
#44000=DIRECTION ( 'NONE',  ( -1.000000000000000000, 0.000000000000000000, 0.000000000000000000 ) ) ;
#44004=CIRCLE ( 'NONE', #1809, 32.00000000000000000 ) ;
#44008=EDGE_CURVE ( 'NONE', #28263, #38490, #24579, .T. ) ;
#44010=AXIS2_PLACEMENT_3D ( 'NONE', #34599, #19670, #7941 ) ;
#44012=FACE_OUTER_BOUND ( 'NONE', #46088, .T. ) ;
#44013=ORIENTED_EDGE ( 'NONE', *, *, #12719, .T. ) ;
#44015=EDGE_CURVE ( 'NONE', #45284, #8653, #6615, .T. ) ;
#44018=CIRCLE ( 'NONE', #8835, 82.00000000000000000 ) ;
#44022=CARTESIAN_POINT ( 'NONE',  ( 0.000000000000000000, 2.543863470248389103, 81.96053171279903893 ) ) ;
#44024=EDGE_CURVE ( 'NONE', #6313, #18399, #6247, .T. ) ;
#44034=EDGE_LOOP ( 'NONE', ( #2869, #15399, #29522, #39017 ) ) ;
#44035=DIRECTION ( 'NONE',  ( 0.000000000000000000, -0.8526401643540860720, -0.5224985647159590130 ) ) ;
#44045=ORIENTED_EDGE ( 'NONE', *, *, #23150, .T. ) ;
#44050=CARTESIAN_POINT ( 'NONE',  ( 10.00000000000000000, 71.21200624218852226, -40.65526001592539984 ) ) ;
#44054=DIRECTION ( 'NONE',  ( 1.000000000000000000, 0.000000000000000000, 0.000000000000000000 ) ) ;
#44063=EDGE_LOOP ( 'NONE', ( #20794, #5297, #17557, #29212 ) ) ;
#44065=CIRCLE ( 'NONE', #22961, 82.00000000000000000 ) ;
#44070=ORIENTED_EDGE ( 'NONE', *, *, #2529, .T. ) ;
#44074=DIRECTION ( 'NONE',  ( -1.000000000000000000, -0.000000000000000000, -0.000000000000000000 ) ) ;
#44080=VECTOR ( 'NONE', #27481, 1000.000000000000000 ) ;
#44086=VERTEX_POINT ( 'NONE', #9418 ) ;
#44094=AXIS2_PLACEMENT_3D ( 'NONE', #16192, #46282, #31122 ) ;
#44095=DIRECTION ( 'NONE',  ( 0.000000000000000000, 0.6494480483301848794, -0.7604059656000299317 ) ) ;
#44096=ORIENTED_EDGE ( 'NONE', *, *, #47846, .T. ) ;
#44101=LINE ( 'NONE', #26234, #24433 ) ;
#44109=CARTESIAN_POINT ( 'NONE',  ( 10.00000000000000000, -69.42325613327415113, -34.44570377933673910 ) ) ;
#44112=FACE_OUTER_BOUND ( 'NONE', #33261, .T. ) ;
#44115=ORIENTED_EDGE ( 'NONE', *, *, #14519, .F. ) ;
#44119=DIRECTION ( 'NONE',  ( -1.000000000000000000, 0.000000000000000000, 0.000000000000000000 ) ) ;
#44123=EDGE_CURVE ( 'NONE', #27602, #26319, #9757, .T. ) ;
#44128=DIRECTION ( 'NONE',  ( 0.000000000000000000, 0.000000000000000000, 1.000000000000000000 ) ) ;
#44135=EDGE_LOOP ( 'NONE', ( #9705, #15736, #45909, #7989 ) ) ;
#44139=AXIS2_PLACEMENT_3D ( 'NONE', #29445, #22084, #47550 ) ;
#44141=CARTESIAN_POINT ( 'NONE',  ( 10.00000000000000000, -51.02545421589285723, -55.20638768913812555 ) ) ;
#44146=DIRECTION ( 'NONE',  ( 0.000000000000000000, -0.2334453638558922628, -0.9723699203976798877 ) ) ;
#44153=AXIS2_PLACEMENT_3D ( 'NONE', #38449, #45807, #8578 ) ;
#44154=EDGE_CURVE ( 'NONE', #13155, #17581, #41848, .T. ) ;
#44156=EDGE_CURVE ( 'NONE', #31426, #33111, #39513, .T. ) ;
#44158=CARTESIAN_POINT ( 'NONE',  ( 10.00000000000000000, -40.65526001592565564, -71.21200624218839437 ) ) ;
#44159=CARTESIAN_POINT ( 'NONE',  ( 5.000000000000002665, 39.47590169984846398, 71.87247863392428826 ) ) ;
#44161=ORIENTED_EDGE ( 'NONE', *, *, #22149, .T. ) ;
#44166=DIRECTION ( 'NONE',  ( -1.000000000000000000, -0.000000000000000000, -0.000000000000000000 ) ) ;
#44168=DIRECTION ( 'NONE',  ( -1.000000000000000000, 0.000000000000000000, 0.000000000000000000 ) ) ;
#44171=LINE ( 'NONE', #15037, #34660 ) ;
#44180=DIRECTION ( 'NONE',  ( 0.000000000000000000, -0.9723699203976740035, -0.2334453638559160216 ) ) ;
#44181=CARTESIAN_POINT ( 'NONE',  ( 10.00000000000000178, 1.530808498934191521E-15, -12.50000000000000000 ) ) ;
#44183=CIRCLE ( 'NONE', #1996, 31.99999999999999645 ) ;
#44184=CIRCLE ( 'NONE', #32482, 32.00000000000000000 ) ;
#44187=ORIENTED_EDGE ( 'NONE', *, *, #442, .T. ) ;
#44188=LINE ( 'NONE', #41251, #8997 ) ;
#44190=DIRECTION ( 'NONE',  ( -1.000000000000000000, -0.000000000000000000, -0.000000000000000000 ) ) ;
#44200=AXIS2_PLACEMENT_3D ( 'NONE', #32324, #21053, #10529 ) ;
#44207=FACE_OUTER_BOUND ( 'NONE', #23719, .T. ) ;
#44208=CARTESIAN_POINT ( 'NONE',  ( 10.00000000000000000, -76.69515212746036070, 29.01471420065537643 ) ) ;
#44211=DIRECTION ( 'NONE',  ( -1.000000000000000000, 0.000000000000000000, 0.000000000000000000 ) ) ;
#44216=EDGE_CURVE ( 'NONE', #16811, #9223, #44406, .T. ) ;
#44220=ORIENTED_EDGE ( 'NONE', *, *, #14369, .F. ) ;
#44221=EDGE_LOOP ( 'NONE', ( #48450, #31991, #28644, #7652 ) ) ;
#44224=ORIENTED_EDGE ( 'NONE', *, *, #18817, .T. ) ;
#44226=CIRCLE ( 'NONE', #23121, 31.99999999999999645 ) ;
#44240=CARTESIAN_POINT ( 'NONE',  ( 0.000000000000000000, 0.000000000000000000, 0.000000000000000000 ) ) ;
#44241=VECTOR ( 'NONE', #47809, 1000.000000000000000 ) ;
#44243=DIRECTION ( 'NONE',  ( 0.000000000000000000, 0.000000000000000000, 1.000000000000000000 ) ) ;
#44244=CIRCLE ( 'NONE', #26256, 31.99999999999999289 ) ;
#44246=CARTESIAN_POINT ( 'NONE',  ( 10.00000000000000000, 0.000000000000000000, 0.000000000000000000 ) ) ;
#44251=( NAMED_UNIT ( * ) SI_UNIT ( $, .STERADIAN. ) SOLID_ANGLE_UNIT ( ) );
#44255=CIRCLE ( 'NONE', #30994, 32.00000000000000000 ) ;
#44262=EDGE_CURVE ( 'NONE', #32517, #7731, #12335, .T. ) ;
#44268=ADVANCED_FACE ( 'NONE', ( #41229 ), #809, .T. ) ;
#44269=CIRCLE ( 'NONE', #15367, 31.99999999999999289 ) ;
#44281=EDGE_CURVE ( 'NONE', #10873, #2830, #15751, .T. ) ;
#44282=DIRECTION ( 'NONE',  ( -1.000000000000000000, -0.000000000000000000, 0.000000000000000000 ) ) ;
#44291=CIRCLE ( 'NONE', #33358, 31.99999999999999645 ) ;
#44296=FACE_OUTER_BOUND ( 'NONE', #44513, .T. ) ;
#44298=FACE_OUTER_BOUND ( 'NONE', #20248, .T. ) ;
#44299=LINE ( 'NONE', #10772, #3526 ) ;
#44301=CARTESIAN_POINT ( 'NONE',  ( 5.000000000000000000, -59.75363087400113926, 56.15606465354937882 ) ) ;
#44302=AXIS2_PLACEMENT_3D ( 'NONE', #13902, #36414, #6554 ) ;
#44308=ORIENTED_EDGE ( 'NONE', *, *, #8671, .T. ) ;
#44320=EDGE_CURVE ( 'NONE', #11204, #14124, #334, .T. ) ;
#44321=DIRECTION ( 'NONE',  ( -1.000000000000000000, 0.000000000000000000, 0.000000000000000000 ) ) ;
#44331=VERTEX_POINT ( 'NONE', #34106 ) ;
#44334=ORIENTED_EDGE ( 'NONE', *, *, #12286, .T. ) ;
#44339=ORIENTED_EDGE ( 'NONE', *, *, #27577, .T. ) ;
#44340=EDGE_CURVE ( 'NONE', #7999, #12683, #17577, .T. ) ;
#44342=ORIENTED_EDGE ( 'NONE', *, *, #25455, .F. ) ;
#44347=DIRECTION ( 'NONE',  ( 0.000000000000000000, 0.000000000000000000, -1.000000000000000000 ) ) ;
#44349=DIRECTION ( 'NONE',  ( -1.000000000000000000, 0.000000000000000000, -0.000000000000000000 ) ) ;
#44352=ORIENTED_EDGE ( 'NONE', *, *, #25464, .T. ) ;
#44353=EDGE_CURVE ( 'NONE', #4138, #2489, #8219, .T. ) ;
#44360=DIRECTION ( 'NONE',  ( 0.000000000000000000, 0.000000000000000000, 1.000000000000000000 ) ) ;
#44367=CARTESIAN_POINT ( 'NONE',  ( 10.00000000000000000, -36.72794159290197769, -65.59268652807249111 ) ) ;
#44369=FACE_OUTER_BOUND ( 'NONE', #31061, .T. ) ;
#44372=DIRECTION ( 'NONE',  ( 0.000000000000000000, 0.8526401643540935105, -0.5224985647159468005 ) ) ;
#44379=CARTESIAN_POINT ( 'NONE',  ( 10.00000000000000000, -12.93880638057369659, 76.41127070299266677 ) ) ;
#44383=CARTESIAN_POINT ( 'NONE',  ( 10.00000000000000000, 16.00000000000000000, -2.500000000000000000 ) ) ;
#44386=AXIS2_PLACEMENT_3D ( 'NONE', #29419, #2737, #14491 ) ;
#44395=ADVANCED_FACE ( 'NONE', ( #12810 ), #2261, .T. ) ;
#44399=DIRECTION ( 'NONE',  ( 0.000000000000000000, 0.000000000000000000, 1.000000000000000000 ) ) ;
#44405=CARTESIAN_POINT ( 'NONE',  ( 0.000000000000000000, -30.41916302227164337, 71.27951684758015460 ) ) ;
#44406=LINE ( 'NONE', #40731, #10566 ) ;
#44408=CYLINDRICAL_SURFACE ( 'NONE', #9400, 31.99999999999999289 ) ;
#44418=CARTESIAN_POINT ( 'NONE',  ( 10.00000000000000000, 73.73191006444572793, -14.66109333815486515 ) ) ;
#44420=LINE ( 'NONE', #28593, #36468 ) ;
#44421=ADVANCED_FACE ( 'NONE', ( #12568 ), #2044, .T. ) ;
#44422=DIRECTION ( 'NONE',  ( -1.000000000000000000, -0.000000000000000000, -0.000000000000000000 ) ) ;
#44423=FACE_OUTER_BOUND ( 'NONE', #21876, .T. ) ;
#44424=DIRECTION ( 'NONE',  ( -1.000000000000000000, 0.000000000000000000, 0.000000000000000000 ) ) ;
#44428=CARTESIAN_POINT ( 'NONE',  ( 0.000000000000000000, 75.54627589209970040, -17.28742895386005785 ) ) ;
#44432=ADVANCED_FACE ( 'NONE', ( #42913 ), #5959, .T. ) ;
#44435=ORIENTED_EDGE ( 'NONE', *, *, #30609, .F. ) ;
#44440=AXIS2_PLACEMENT_3D ( 'NONE', #34539, #23299, #42142 ) ;
#44447=VERTEX_POINT ( 'NONE', #24070 ) ;
#44452=CARTESIAN_POINT ( 'NONE',  ( 10.00000000000000000, 0.000000000000000000, 0.000000000000000000 ) ) ;
#44459=DIRECTION ( 'NONE',  ( 0.000000000000000000, -0.7071067811865536790, 0.7071067811865414665 ) ) ;
#44461=DIRECTION ( 'NONE',  ( 0.000000000000000000, 0.000000000000000000, -1.000000000000000000 ) ) ;
#44466=ADVANCED_FACE ( 'NONE', ( #47059 ), #39488, .T. ) ;
#44469=CARTESIAN_POINT ( 'NONE',  ( 0.000000000000000000, -78.73519480814971416, 22.90783923731600069 ) ) ;
#44473=ORIENTED_EDGE ( 'NONE', *, *, #48138, .T. ) ;
#44474=EDGE_CURVE ( 'NONE', #13774, #35650, #24535, .T. ) ;
#44475=DIRECTION ( 'NONE',  ( -1.000000000000000000, -0.000000000000000000, 0.000000000000000000 ) ) ;
#44492=AXIS2_PLACEMENT_3D ( 'NONE', #37885, #23192, #33716 ) ;
#44497=VERTEX_POINT ( 'NONE', #31672 ) ;
#44499=EDGE_CURVE ( 'NONE', #29028, #6991, #46590, .T. ) ;
#44500=VECTOR ( 'NONE', #33136, 1000.000000000000000 ) ;
#44504=CARTESIAN_POINT ( 'NONE',  ( 0.000000000000000000, -68.67312586194971402, -35.91791733033549860 ) ) ;
#44506=DIRECTION ( 'NONE',  ( 0.000000000000000000, 0.3826834323650841752, 0.9238795325112891810 ) ) ;
#44507=VERTEX_POINT ( 'NONE', #20624 ) ;
#44513=EDGE_LOOP ( 'NONE', ( #27164, #41504, #14466, #47297 ) ) ;
#44514=DIRECTION ( 'NONE',  ( 0.000000000000000000, 0.000000000000000000, -1.000000000000000000 ) ) ;
#44516=FACE_OUTER_BOUND ( 'NONE', #28986, .T. ) ;
#44518=ORIENTED_EDGE ( 'NONE', *, *, #33810, .T. ) ;
#44522=CARTESIAN_POINT ( 'NONE',  ( 0.000000000000000000, 0.000000000000000000, 0.000000000000000000 ) ) ;
#44523=ORIENTED_EDGE ( 'NONE', *, *, #10661, .F. ) ;
#44525=VECTOR ( 'NONE', #2467, 1000.000000000000000 ) ;
#44526=EDGE_CURVE ( 'NONE', #29421, #21411, #46448, .T. ) ;
#44531=DIRECTION ( 'NONE',  ( 0.000000000000000000, 0.000000000000000000, 1.000000000000000000 ) ) ;
#44533=CARTESIAN_POINT ( 'NONE',  ( 0.000000000000000000, -34.94270380257586339, -74.18225833017926618 ) ) ;
#44544=EDGE_CURVE ( 'NONE', #39455, #5074, #39390, .T. ) ;
#44545=DIRECTION ( 'NONE',  ( -1.000000000000000000, 0.000000000000000000, 0.000000000000000000 ) ) ;
#44549=ORIENTED_EDGE ( 'NONE', *, *, #37986, .F. ) ;
#44551=AXIS2_PLACEMENT_3D ( 'NONE', #6460, #47565, #28966 ) ;
#44555=CIRCLE ( 'NONE', #3110, 31.99999999999998934 ) ;
#44560=AXIS2_PLACEMENT_3D ( 'NONE', #1120, #20206, #16067 ) ;
#44561=VECTOR ( 'NONE', #22381, 1000.000000000000000 ) ;
#44567=VERTEX_POINT ( 'NONE', #32606 ) ;
#44574=CARTESIAN_POINT ( 'NONE',  ( 10.00000000000000000, 23.16143007188532366, -73.95703589263949596 ) ) ;
#44577=CARTESIAN_POINT ( 'NONE',  ( 0.000000000000000000, -24.73286445877653961, -73.44644590900085745 ) ) ;
#44582=ORIENTED_EDGE ( 'NONE', *, *, #32808, .F. ) ;
#44583=EDGE_CURVE ( 'NONE', #37330, #36456, #7462, .T. ) ;
#44584=DIRECTION ( 'NONE',  ( 0.000000000000000000, 0.07845909572783793529, 0.9969173337331285190 ) ) ;
#44585=DIRECTION ( 'NONE',  ( 0.000000000000000000, -0.6494480483301739993, -0.7604059656000390355 ) ) ;
#44586=CARTESIAN_POINT ( 'NONE',  ( 10.00000000000000000, -75.11725578898466438, -2.956366410621452001 ) ) ;
#44589=ADVANCED_FACE ( 'NONE', ( #6669 ), #25013, .T. ) ;
#44596=DIRECTION ( 'NONE',  ( 0.000000000000000000, -0.9969173337331270757, -0.07845909572785580988 ) ) ;
#44604=DIRECTION ( 'NONE',  ( -1.000000000000000000, 0.000000000000000000, 0.000000000000000000 ) ) ;
#44607=EDGE_CURVE ( 'NONE', #35473, #25837, #5785, .T. ) ;
#44613=EDGE_CURVE ( 'NONE', #3193, #29274, #34801, .T. ) ;
#44622=ADVANCED_FACE ( 'NONE', ( #37244 ), #14498, .T. ) ;
#44625=CARTESIAN_POINT ( 'NONE',  ( 10.00000000000000000, -33.71516098798792171, 74.74816331893418919 ) ) ;
#44629=ORIENTED_EDGE ( 'NONE', *, *, #12544, .F. ) ;
#44630=FACE_OUTER_BOUND ( 'NONE', #18548, .T. ) ;
#44631=EDGE_LOOP ( 'NONE', ( #8714, #10087, #12012, #7300 ) ) ;
#44633=CARTESIAN_POINT ( 'NONE',  ( 10.00000000000000000, 0.000000000000000000, 0.000000000000000000 ) ) ;
#44635=VECTOR ( 'NONE', #19834, 1000.000000000000000 ) ;
#44637=DIRECTION ( 'NONE',  ( 0.000000000000000000, 0.000000000000000000, 1.000000000000000000 ) ) ;
#44638=ORIENTED_EDGE ( 'NONE', *, *, #888, .F. ) ;
#44650=EDGE_CURVE ( 'NONE', #15618, #42302, #40196, .T. ) ;
#44655=ORIENTED_EDGE ( 'NONE', *, *, #44613, .T. ) ;
#44661=DIRECTION ( 'NONE',  ( 0.000000000000000000, 0.000000000000000000, 1.000000000000000000 ) ) ;
#44667=AXIS2_PLACEMENT_3D ( 'NONE', #41286, #22668, #1116 ) ;
#44671=ORIENTED_EDGE ( 'NONE', *, *, #29111, .F. ) ;
#44673=ORIENTED_EDGE ( 'NONE', *, *, #9317, .F. ) ;
#44679=LINE ( 'NONE', #47859, #39446 ) ;
#44684=CARTESIAN_POINT ( 'NONE',  ( -10.00000000000000000, 0.000000000000000000, 0.000000000000000000 ) ) ;
#44687=EDGE_CURVE ( 'NONE', #45907, #13460, #9791, .T. ) ;
#44689=EDGE_LOOP ( 'NONE', ( #8261, #42345, #963, #18886 ) ) ;
#44692=EDGE_LOOP ( 'NONE', ( #7299, #35726, #5511, #12651 ) ) ;
#44695=EDGE_CURVE ( 'NONE', #30299, #31998, #19840, .T. ) ;
#44699=CYLINDRICAL_SURFACE ( 'NONE', #3357, 77.49899999999999523 ) ;
#44707=DIRECTION ( 'NONE',  ( -1.000000000000000000, -0.000000000000000000, -0.000000000000000000 ) ) ;
#44708=ORIENTED_EDGE ( 'NONE', *, *, #46757, .T. ) ;
#44710=EDGE_LOOP ( 'NONE', ( #16277, #43963, #43600, #36425 ) ) ;
#44713=AXIS2_PLACEMENT_3D ( 'NONE', #26886, #37170, #41821 ) ;
#44719=LINE ( 'NONE', #29791, #7601 ) ;
#44722=VECTOR ( 'NONE', #19770, 1000.000000000000000 ) ;
#44732=CARTESIAN_POINT ( 'NONE',  ( 10.00000000000000000, 77.49459641780886443, 0.8261519478433866359 ) ) ;
#44735=FACE_OUTER_BOUND ( 'NONE', #48242, .T. ) ;
#44736=EDGE_CURVE ( 'NONE', #20071, #7163, #15462, .T. ) ;
#44737=EDGE_LOOP ( 'NONE', ( #24040, #33770, #120, #4118 ) ) ;
#44754=EDGE_CURVE ( 'NONE', #44507, #28263, #4289, .T. ) ;
#44756=ORIENTED_EDGE ( 'NONE', *, *, #45114, .F. ) ;
#44761=VERTEX_POINT ( 'NONE', #33798 ) ;
#44763=EDGE_LOOP ( 'NONE', ( #8260, #36612, #22110, #34629 ) ) ;
#44765=CARTESIAN_POINT ( 'NONE',  ( 0.000000000000000000, 0.000000000000000000, 0.000000000000000000 ) ) ;
#44767=CARTESIAN_POINT ( 'NONE',  ( 10.00000000000000000, -65.59268652807237743, 36.72794159290217664 ) ) ;
#44769=ORIENTED_EDGE ( 'NONE', *, *, #45463, .F. ) ;
#44771=DIRECTION ( 'NONE',  ( 1.000000000000000000, -0.000000000000000000, 0.000000000000000000 ) ) ;
#44778=AXIS2_PLACEMENT_3D ( 'NONE', #5987, #1577, #13315 ) ;
#44787=AXIS2_PLACEMENT_3D ( 'NONE', #23064, #30416, #33356 ) ;
#44788=DIRECTION ( 'NONE',  ( -1.000000000000000000, 0.000000000000000000, 0.000000000000000000 ) ) ;
#44790=AXIS2_PLACEMENT_3D ( 'NONE', #16914, #6617, #2002 ) ;
#44792=CARTESIAN_POINT ( 'NONE',  ( 10.00000000000000000, -74.18225833017864090, -34.94270380257719211 ) ) ;
#44794=VECTOR ( 'NONE', #32020, 1000.000000000000000 ) ;
#44797=EDGE_CURVE ( 'NONE', #27040, #46360, #2683, .T. ) ;
#44800=DIRECTION ( 'NONE',  ( -1.000000000000000000, -0.000000000000000000, -0.000000000000000000 ) ) ;
#44801=EDGE_CURVE ( 'NONE', #32047, #15128, #44908, .T. ) ;
#44804=AXIS2_PLACEMENT_3D ( 'NONE', #44141, #3742, #18666 ) ;
#44805=AXIS2_PLACEMENT_3D ( 'NONE', #32145, #47064, #6197 ) ;
#44806=ORIENTED_EDGE ( 'NONE', *, *, #39852, .T. ) ;
#44808=DIRECTION ( 'NONE',  ( 0.000000000000000000, 0.000000000000000000, 1.000000000000000000 ) ) ;
#44809=VECTOR ( 'NONE', #11343, 1000.000000000000000 ) ;
#44816=CARTESIAN_POINT ( 'NONE',  ( 10.00000000000000000, 0.000000000000000000, 0.000000000000000000 ) ) ;
#44822=EDGE_LOOP ( 'NONE', ( #11686, #25022, #26215, #47636 ) ) ;
#44824=ORIENTED_EDGE ( 'NONE', *, *, #38235, .F. ) ;
#44828=DIRECTION ( 'NONE',  ( 0.000000000000000000, -0.9510565162951499785, -0.3090169943749582204 ) ) ;
#44829=LINE ( 'NONE', #26238, #28184 ) ;
#44830=CARTESIAN_POINT ( 'NONE',  ( 10.00000000000000000, -75.54627589209931671, -17.28742895386164591 ) ) ;
#44841=CIRCLE ( 'NONE', #31581, 82.00000000000000000 ) ;
#44843=CARTESIAN_POINT ( 'NONE',  ( 10.00000000000000000, 26.02418014898407961, -70.52718814184231633 ) ) ;
#44854=DIRECTION ( 'NONE',  ( 0.000000000000000000, 0.000000000000000000, 1.000000000000000000 ) ) ;
#44858=AXIS2_PLACEMENT_3D ( 'NONE', #3997, #8143, #33839 ) ;
#44859=ORIENTED_EDGE ( 'NONE', *, *, #36962, .F. ) ;
#44860=DIRECTION ( 'NONE',  ( 0.000000000000000000, -0.7071067811865389130, -0.7071067811865561215 ) ) ;
#44862=ORIENTED_EDGE ( 'NONE', *, *, #31642, .T. ) ;
#44873=ORIENTED_EDGE ( 'NONE', *, *, #16095, .T. ) ;
#44878=CARTESIAN_POINT ( 'NONE',  ( 10.00000000000000000, 65.59268652807210742, 36.72794159290264560 ) ) ;
#44881=ORIENTED_EDGE ( 'NONE', *, *, #24710, .F. ) ;
#44886=CIRCLE ( 'NONE', #40222, 31.99999999999999645 ) ;
#44890=DIRECTION ( 'NONE',  ( 0.000000000000000000, -0.8090169943749402348, -0.5877852522924830181 ) ) ;
#44893=DIRECTION ( 'NONE',  ( -1.000000000000000000, 0.000000000000000000, -0.000000000000000000 ) ) ;
#44897=EDGE_CURVE ( 'NONE', #31833, #14564, #27724, .T. ) ;
#44902=CARTESIAN_POINT ( 'NONE',  ( 0.000000000000000000, 81.34940948281351325, -10.30890764327296161 ) ) ;
#44903=AXIS2_PLACEMENT_3D ( 'NONE', #35, #282, #44596 ) ;
#44904=CARTESIAN_POINT ( 'NONE',  ( 0.000000000000000000, -46.11716303203136391, -67.80270845531939017 ) ) ;
#44907=VERTEX_POINT ( 'NONE', #24013 ) ;
#44908=CIRCLE ( 'NONE', #9710, 31.99999999999999289 ) ;
#44918=VECTOR ( 'NONE', #18725, 1000.000000000000000 ) ;
#44921=ADVANCED_FACE ( 'NONE', ( #1256 ), #4916, .T. ) ;
#44924=EDGE_CURVE ( 'NONE', #17540, #10420, #46492, .T. ) ;
#44926=CARTESIAN_POINT ( 'NONE',  ( 10.00000000000000000, -76.41127070299280888, 12.93880638057289012 ) ) ;
#44943=ORIENTED_EDGE ( 'NONE', *, *, #606, .T. ) ;
#44957=CARTESIAN_POINT ( 'NONE',  ( 10.00000000000000000, 68.67312586195046720, -35.91791733033402068 ) ) ;
#44958=VERTEX_POINT ( 'NONE', #47243 ) ;
#44959=LINE ( 'NONE', #153, #45464 ) ;
#44962=VERTEX_POINT ( 'NONE', #14437 ) ;
#44963=DIRECTION ( 'NONE',  ( -1.000000000000000000, 0.000000000000000000, -0.000000000000000000 ) ) ;
#44966=DIRECTION ( 'NONE',  ( -1.000000000000000000, 0.000000000000000000, 0.000000000000000000 ) ) ;
#44970=VECTOR ( 'NONE', #14722, 1000.000000000000000 ) ;
#44972=CYLINDRICAL_SURFACE ( 'NONE', #34959, 77.49899999999999523 ) ;
#44976=EDGE_LOOP ( 'NONE', ( #29075, #35522, #27349, #27147 ) ) ;
#44977=AXIS2_PLACEMENT_3D ( 'NONE', #2936, #36701, #6859 ) ;
#44979=DIRECTION ( 'NONE',  ( 0.000000000000000000, 0.000000000000000000, 1.000000000000000000 ) ) ;
#44981=VECTOR ( 'NONE', #4027, 1000.000000000000000 ) ;
#44987=DIRECTION ( 'NONE',  ( 1.000000000000000000, 0.000000000000000000, 0.000000000000000000 ) ) ;
#44992=DIRECTION ( 'NONE',  ( 0.000000000000000000, 0.000000000000000000, 1.000000000000000000 ) ) ;
#45005=ORIENTED_EDGE ( 'NONE', *, *, #38351, .F. ) ;
#45012=ORIENTED_EDGE ( 'NONE', *, *, #22753, .T. ) ;
#45018=DIRECTION ( 'NONE',  ( 1.000000000000000000, -0.000000000000000000, -0.000000000000000000 ) ) ;
#45019=ORIENTED_EDGE ( 'NONE', *, *, #15979, .T. ) ;
#45024=DIRECTION ( 'NONE',  ( 0.000000000000000000, 0.000000000000000000, -1.000000000000000000 ) ) ;
#45025=AXIS2_PLACEMENT_3D ( 'NONE', #9673, #27565, #42493 ) ;
#45029=DIRECTION ( 'NONE',  ( 1.000000000000000000, 0.000000000000000000, -0.000000000000000000 ) ) ;
#45034=CARTESIAN_POINT ( 'NONE',  ( 10.00000000000000000, 59.03961581697399907, 46.53671651293969802 ) ) ;
#45038=VERTEX_POINT ( 'NONE', #39902 ) ;
#45042=DIRECTION ( 'NONE',  ( -1.000000000000000000, 0.000000000000000000, 0.000000000000000000 ) ) ;
#45052=VERTEX_POINT ( 'NONE', #35978 ) ;
#45059=FACE_OUTER_BOUND ( 'NONE', #8402, .T. ) ;
#45062=ORIENTED_EDGE ( 'NONE', *, *, #8129, .F. ) ;
#45066=VERTEX_POINT ( 'NONE', #7078 ) ;
#45073=CIRCLE ( 'NONE', #12243, 82.00000000000000000 ) ;
#45074=DIRECTION ( 'NONE',  ( -1.000000000000000000, 0.000000000000000000, 0.000000000000000000 ) ) ;
#45080=DIRECTION ( 'NONE',  ( 0.000000000000000000, -0.7604059656000227152, -0.6494480483301933171 ) ) ;
#45088=EDGE_CURVE ( 'NONE', #39890, #8273, #13718, .T. ) ;
#45091=LINE ( 'NONE', #34059, #12311 ) ;
#45098=EDGE_CURVE ( 'NONE', #24069, #32517, #18305, .T. ) ;
#45099=EDGE_LOOP ( 'NONE', ( #10063, #5148, #2833, #14960 ) ) ;
#45101=LINE ( 'NONE', #41425, #11232 ) ;
#45103=FACE_OUTER_BOUND ( 'NONE', #24393, .T. ) ;
#45106=DIRECTION ( 'NONE',  ( -1.000000000000000000, 0.000000000000000000, 0.000000000000000000 ) ) ;
#45114=EDGE_CURVE ( 'NONE', #9766, #17390, #37074, .T. ) ;
#45115=AXIS2_PLACEMENT_3D ( 'NONE', #600, #34126, #7216 ) ;
#45121=AXIS2_PLACEMENT_3D ( 'NONE', #2564, #48088, #36105 ) ;
#45125=ORIENTED_EDGE ( 'NONE', *, *, #18070, .T. ) ;
#45131=VERTEX_POINT ( 'NONE', #699 ) ;
#45132=ORIENTED_EDGE ( 'NONE', *, *, #28411, .T. ) ;
#45133=CARTESIAN_POINT ( 'NONE',  ( -10.00000000000000000, 0.000000000000000000, 0.000000000000000000 ) ) ;
#45137=DIRECTION ( 'NONE',  ( 0.000000000000000000, 0.000000000000000000, 1.000000000000000000 ) ) ;
#45144=EDGE_CURVE ( 'NONE', #46010, #39534, #48044, .T. ) ;
#45158=DIRECTION ( 'NONE',  ( -1.000000000000000000, 0.000000000000000000, 0.000000000000000000 ) ) ;
#45160=DIRECTION ( 'NONE',  ( -1.000000000000000000, 0.000000000000000000, 0.000000000000000000 ) ) ;
#45170=CARTESIAN_POINT ( 'NONE',  ( 10.00000000000000000, -36.72794159290288718, 65.59268652807197952 ) ) ;
#45172=EDGE_CURVE ( 'NONE', #22252, #44086, #12119, .T. ) ;
#45173=DIRECTION ( 'NONE',  ( 0.000000000000000000, 0.000000000000000000, 1.000000000000000000 ) ) ;
#45175=DIRECTION ( 'NONE',  ( -1.000000000000000000, 0.000000000000000000, -0.000000000000000000 ) ) ;
#45179=ORIENTED_EDGE ( 'NONE', *, *, #33590, .T. ) ;
#45181=DIRECTION ( 'NONE',  ( -1.000000000000000000, -0.000000000000000000, -0.000000000000000000 ) ) ;
#45183=VECTOR ( 'NONE', #26348, 1000.000000000000000 ) ;
#45199=VERTEX_POINT ( 'NONE', #934 ) ;
#45204=DIRECTION ( 'NONE',  ( 0.000000000000000000, 0.9510565162951523099, 0.3090169943749515591 ) ) ;
#45205=CIRCLE ( 'NONE', #35830, 32.00000000000000000 ) ;
#45207=CARTESIAN_POINT ( 'NONE',  ( 10.00000000000000000, -58.39081064771713869, -50.95692526931392052 ) ) ;
#45208=FACE_OUTER_BOUND ( 'NONE', #47045, .T. ) ;
#45211=AXIS2_PLACEMENT_3D ( 'NONE', #23675, #23930, #42778 ) ;
#45217=EDGE_CURVE ( 'NONE', #46360, #43938, #15257, .T. ) ;
#45218=CYLINDRICAL_SURFACE ( 'NONE', #33401, 77.49899999999999523 ) ;
#45229=ADVANCED_FACE ( 'NONE', ( #31072 ), #12456, .T. ) ;
#45231=ORIENTED_EDGE ( 'NONE', *, *, #3637, .T. ) ;
#45233=VECTOR ( 'NONE', #46381, 1000.000000000000000 ) ;
#45240=VERTEX_POINT ( 'NONE', #1442 ) ;
#45251=ORIENTED_EDGE ( 'NONE', *, *, #37310, .T. ) ;
#45261=CARTESIAN_POINT ( 'NONE',  ( 10.00000000000000000, -73.73191006444561424, -14.66109333815538918 ) ) ;
#45262=EDGE_CURVE ( 'NONE', #17289, #1183, #9491, .T. ) ;
#45263=CARTESIAN_POINT ( 'NONE',  ( 0.000000000000000000, 0.000000000000000000, 0.000000000000000000 ) ) ;
#45264=CARTESIAN_POINT ( 'NONE',  ( 0.000000000000000000, 68.67312586194995561, 35.91791733033500122 ) ) ;
#45272=AXIS2_PLACEMENT_3D ( 'NONE', #33608, #3515, #7440 ) ;
#45274=ORIENTED_EDGE ( 'NONE', *, *, #13217, .F. ) ;
#45276=DIRECTION ( 'NONE',  ( 0.000000000000000000, 0.000000000000000000, 1.000000000000000000 ) ) ;
#45282=VERTEX_POINT ( 'NONE', #19774 ) ;
#45283=ORIENTED_EDGE ( 'NONE', *, *, #22539, .F. ) ;
#45284=VERTEX_POINT ( 'NONE', #2162 ) ;
#45286=DIRECTION ( 'NONE',  ( 0.000000000000000000, 0.000000000000000000, 1.000000000000000000 ) ) ;
#45288=ORIENTED_EDGE ( 'NONE', *, *, #47799, .F. ) ;
#45289=ORIENTED_EDGE ( 'NONE', *, *, #47705, .T. ) ;
#45290=CARTESIAN_POINT ( 'NONE',  ( 0.000000000000000000, 79.10210256391368944, 21.60688246758614284 ) ) ;
#45291=ORIENTED_EDGE ( 'NONE', *, *, #26258, .T. ) ;
#45294=CARTESIAN_POINT ( 'NONE',  ( 10.00000000000000000, -8.966570791700142706, -81.50828551894234408 ) ) ;
#45297=DIRECTION ( 'NONE',  ( -1.000000000000000000, 0.000000000000000000, -0.000000000000000000 ) ) ;
#45299=ORIENTED_EDGE ( 'NONE', *, *, #9160, .T. ) ;
#45306=DIRECTION ( 'NONE',  ( -1.000000000000000000, 0.000000000000000000, 0.000000000000000000 ) ) ;
#45308=DIRECTION ( 'NONE',  ( -1.000000000000000000, -0.000000000000000000, -0.000000000000000000 ) ) ;
#45309=ADVANCED_FACE ( 'NONE', ( #12948 ), #8764, .T. ) ;
#45312=EDGE_CURVE ( 'NONE', #36574, #24182, #38657, .T. ) ;
#45321=CARTESIAN_POINT ( 'NONE',  ( 10.00000000000000000, 0.000000000000000000, 0.000000000000000000 ) ) ;
#45323=FACE_OUTER_BOUND ( 'NONE', #13420, .T. ) ;
#45329=PRODUCT_CONTEXT ( 'NONE', #28226, 'mechanical' ) ;
#45330=CARTESIAN_POINT ( 'NONE',  ( 10.00000000000000000, 59.03961581697465277, -46.53671651293886669 ) ) ;
#45334=VERTEX_POINT ( 'NONE', #16855 ) ;
#45336=EDGE_CURVE ( 'NONE', #10873, #47251, #31693, .T. ) ;
#45339=CARTESIAN_POINT ( 'NONE',  ( 0.000000000000000000, 34.94270380257639630, 74.18225833017899618 ) ) ;
#45347=CARTESIAN_POINT ( 'NONE',  ( 0.000000000000000000, -8.966570791701281351, 81.50828551894224461 ) ) ;
#45353=ORIENTED_EDGE ( 'NONE', *, *, #10737, .T. ) ;
#45362=DIRECTION ( 'NONE',  ( 1.000000000000000000, -0.000000000000000000, 0.000000000000000000 ) ) ;
#45364=DIRECTION ( 'NONE',  ( -1.000000000000000000, 0.000000000000000000, 0.000000000000000000 ) ) ;
#45365=AXIS2_PLACEMENT_3D ( 'NONE', #13844, #43687, #2805 ) ;
#45369=CIRCLE ( 'NONE', #3146, 82.00000000000000000 ) ;
#45371=DIRECTION ( 'NONE',  ( -1.000000000000000000, 0.000000000000000000, 0.000000000000000000 ) ) ;
#45373=LINE ( 'NONE', #34117, #22301 ) ;
#45379=EDGE_CURVE ( 'NONE', #27354, #19209, #9756, .T. ) ;
#45385=ORIENTED_EDGE ( 'NONE', *, *, #12305, .F. ) ;
#45387=VECTOR ( 'NONE', #32477, 1000.000000000000000 ) ;
#45396=ADVANCED_FACE ( 'NONE', ( #46949 ), #14803, .T. ) ;
#45399=CARTESIAN_POINT ( 'NONE',  ( 0.000000000000000000, 0.000000000000000000, 0.000000000000000000 ) ) ;
#45412=ORIENTED_EDGE ( 'NONE', *, *, #44650, .F. ) ;
#45415=ORIENTED_EDGE ( 'NONE', *, *, #46609, .F. ) ;
#45425=DIRECTION ( 'NONE',  ( 1.000000000000000000, -0.000000000000000000, -0.000000000000000000 ) ) ;
#45433=CIRCLE ( 'NONE', #24327, 32.00000000000000000 ) ;
#45437=CARTESIAN_POINT ( 'NONE',  ( 0.000000000000000000, -76.66974797899844418, 11.30684508768314522 ) ) ;
#45445=LINE ( 'NONE', #887, #1404 ) ;
#45446=AXIS2_PLACEMENT_3D ( 'NONE', #14956, #22540, #44808 ) ;
#45451=ORIENTED_EDGE ( 'NONE', *, *, #44897, .F. ) ;
#45455=CIRCLE ( 'NONE', #7168, 32.00000000000000000 ) ;
#45462=VECTOR ( 'NONE', #31238, 1000.000000000000000 ) ;
#45463=EDGE_CURVE ( 'NONE', #36456, #21451, #22620, .T. ) ;
#45464=VECTOR ( 'NONE', #7750, 1000.000000000000000 ) ;
#45467=CYLINDRICAL_SURFACE ( 'NONE', #32878, 31.99999999999999289 ) ;
#45469=CARTESIAN_POINT ( 'NONE',  ( 0.000000000000000000, -10.30890764327441822, 81.34940948281332851 ) ) ;
#45473=FACE_OUTER_BOUND ( 'NONE', #37399, .T. ) ;
#45477=ORIENTED_EDGE ( 'NONE', *, *, #40567, .T. ) ;
#45484=DIRECTION ( 'NONE',  ( 0.000000000000000000, 0.000000000000000000, 1.000000000000000000 ) ) ;
#45486=DIRECTION ( 'NONE',  ( 0.000000000000000000, 1.000000000000000000, 3.491481338843133355E-15 ) ) ;
#45487=DIRECTION ( 'NONE',  ( -1.000000000000000000, 0.000000000000000000, -0.000000000000000000 ) ) ;
#45488=DIRECTION ( 'NONE',  ( 0.000000000000000000, 0.000000000000000000, 1.000000000000000000 ) ) ;
#45489=CARTESIAN_POINT ( 'NONE',  ( 0.000000000000000000, -16.65972982744877484, -80.28980883073775487 ) ) ;
#45490=DIRECTION ( 'NONE',  ( -1.000000000000000000, -0.000000000000000000, 0.000000000000000000 ) ) ;
#45491=CARTESIAN_POINT ( 'NONE',  ( 10.00000000000000000, 0.000000000000000000, 0.000000000000000000 ) ) ;
#45492=FACE_OUTER_BOUND ( 'NONE', #31341, .T. ) ;
#45496=AXIS2_PLACEMENT_3D ( 'NONE', #24227, #35002, #2199 ) ;
#45501=ORIENTED_EDGE ( 'NONE', *, *, #4171, .T. ) ;
#45506=DIRECTION ( 'NONE',  ( 0.000000000000000000, 0.7604059656000277112, 0.6494480483301875440 ) ) ;
#45510=EDGE_CURVE ( 'NONE', #24990, #11779, #9030, .T. ) ;
#45511=DIRECTION ( 'NONE',  ( 0.000000000000000000, 0.4539904997395476927, -0.8910065241883674547 ) ) ;
#45521=VERTEX_POINT ( 'NONE', #22859 ) ;
#45524=ORIENTED_EDGE ( 'NONE', *, *, #42839, .T. ) ;
#45533=ORIENTED_EDGE ( 'NONE', *, *, #1678, .T. ) ;
#45534=CARTESIAN_POINT ( 'NONE',  ( 10.00000000000000000, 36.73666225445988687, -65.58780272294035285 ) ) ;
#45538=DIRECTION ( 'NONE',  ( -1.000000000000000000, 0.000000000000000000, 0.000000000000000000 ) ) ;
#45545=DIRECTION ( 'NONE',  ( -1.000000000000000000, -0.000000000000000000, -0.000000000000000000 ) ) ;
#45551=DIRECTION ( 'NONE',  ( -1.000000000000000000, -0.000000000000000000, 0.000000000000000000 ) ) ;
#45554=DIRECTION ( 'NONE',  ( -1.000000000000000000, -0.000000000000000000, 0.000000000000000000 ) ) ;
#45555=CARTESIAN_POINT ( 'NONE',  ( 0.000000000000000000, 0.000000000000000000, 0.000000000000000000 ) ) ;
#45558=DIRECTION ( 'NONE',  ( 0.000000000000000000, 0.000000000000000000, 1.000000000000000000 ) ) ;
#45567=CIRCLE ( 'NONE', #11319, 31.99999999999999645 ) ;
#45568=ORIENTED_EDGE ( 'NONE', *, *, #6143, .T. ) ;
#45570=CARTESIAN_POINT ( 'NONE',  ( -10.00000000000000000, 0.000000000000000000, 0.000000000000000000 ) ) ;
#45571=AXIS2_PLACEMENT_3D ( 'NONE', #31313, #8527, #46479 ) ;
#45572=ORIENTED_EDGE ( 'NONE', *, *, #18560, .T. ) ;
#45581=EDGE_CURVE ( 'NONE', #361, #697, #45373, .T. ) ;
#45585=EDGE_LOOP ( 'NONE', ( #27604, #30936, #328, #20813 ) ) ;
#45589=DIRECTION ( 'NONE',  ( 0.000000000000000000, -0.9876883405951359940, -0.1564344650402420267 ) ) ;
#45590=DIRECTION ( 'NONE',  ( 0.000000000000000000, -0.8090169943749403458, -0.5877852522924830181 ) ) ;
#45595=LINE ( 'NONE', #4014, #6045 ) ;
#45597=ORIENTED_EDGE ( 'NONE', *, *, #4210, .T. ) ;
#45599=DIRECTION ( 'NONE',  ( 0.000000000000000000, 0.000000000000000000, 1.000000000000000000 ) ) ;
#45601=AXIS2_PLACEMENT_3D ( 'NONE', #38850, #35151, #34188 ) ;
#45609=AXIS2_PLACEMENT_3D ( 'NONE', #21953, #18534, #26120 ) ;
#45612=CYLINDRICAL_SURFACE ( 'NONE', #6412, 82.00000000000000000 ) ;
#45623=VERTEX_POINT ( 'NONE', #19907 ) ;
#45625=EDGE_CURVE ( 'NONE', #32554, #6182, #9786, .T. ) ;
#45626=DIRECTION ( 'NONE',  ( 0.000000000000000000, 0.8090169943749445647, 0.5877852522924770229 ) ) ;
#45632=DIRECTION ( 'NONE',  ( 0.000000000000000000, 1.000000000000000000, 3.491481338843133355E-15 ) ) ;
#45634=AXIS2_PLACEMENT_3D ( 'NONE', #1576, #31445, #2516 ) ;
#45637=CIRCLE ( 'NONE', #24545, 31.99999999999998579 ) ;
#45653=ORIENTED_EDGE ( 'NONE', *, *, #29147, .F. ) ;
#45658=AXIS2_PLACEMENT_3D ( 'NONE', #16938, #46568, #46317 ) ;
#45659=DIRECTION ( 'NONE',  ( -1.000000000000000000, 0.000000000000000000, 0.000000000000000000 ) ) ;
#45662=ORIENTED_EDGE ( 'NONE', *, *, #12305, .T. ) ;
#45663=CYLINDRICAL_SURFACE ( 'NONE', #13068, 31.99999999999999289 ) ;
#45670=LINE ( 'NONE', #865, #33690 ) ;
#45672=FACE_OUTER_BOUND ( 'NONE', #1464, .T. ) ;
#45674=CARTESIAN_POINT ( 'NONE',  ( 0.000000000000000000, -2.946379043146863719, 75.11764819372146462 ) ) ;
#45680=DIRECTION ( 'NONE',  ( -1.000000000000000000, -0.000000000000000000, -0.000000000000000000 ) ) ;
#45690=ORIENTED_EDGE ( 'NONE', *, *, #5365, .F. ) ;
#45692=CIRCLE ( 'NONE', #15992, 82.00000000000000000 ) ;
#45711=EDGE_CURVE ( 'NONE', #8653, #36574, #5125, .T. ) ;
#45714=AXIS2_PLACEMENT_3D ( 'NONE', #5117, #42804, #39364 ) ;
#45718=VERTEX_POINT ( 'NONE', #9866 ) ;
#45721=EDGE_CURVE ( 'NONE', #20063, #5905, #17194, .T. ) ;
#45723=CARTESIAN_POINT ( 'NONE',  ( 10.00000000000000000, 0.000000000000000000, 0.000000000000000000 ) ) ;
#45729=VERTEX_POINT ( 'NONE', #35576 ) ;
#45731=CARTESIAN_POINT ( 'NONE',  ( 10.00000000000000000, -41.76937507738831812, 62.50329211542423025 ) ) ;
#45742=EDGE_LOOP ( 'NONE', ( #40257, #38936, #20910, #25 ) ) ;
#45744=DIRECTION ( 'NONE',  ( -1.000000000000000000, -0.000000000000000000, -0.000000000000000000 ) ) ;
#45745=ORIENTED_EDGE ( 'NONE', *, *, #40350, .T. ) ;
#45748=CARTESIAN_POINT ( 'NONE',  ( 0.000000000000000000, -20.41045688087876897, 72.35160999960810102 ) ) ;
#45752=DIRECTION ( 'NONE',  ( -1.000000000000000000, 0.000000000000000000, 0.000000000000000000 ) ) ;
#45755=CARTESIAN_POINT ( 'NONE',  ( 0.000000000000000000, -68.27212725128254078, -31.46837873495049465 ) ) ;
#45762=ORIENTED_EDGE ( 'NONE', *, *, #9933, .T. ) ;
#45773=ORIENTED_EDGE ( 'NONE', *, *, #29559, .T. ) ;
#45775=EDGE_CURVE ( 'NONE', #33952, #38558, #8214, .T. ) ;
#45776=EDGE_CURVE ( 'NONE', #6985, #36193, #41844, .T. ) ;
#45780=ORIENTED_EDGE ( 'NONE', *, *, #47848, .T. ) ;
#45794=CARTESIAN_POINT ( 'NONE',  ( 5.000000000000002665, -78.73519480814971416, 22.90783923731600069 ) ) ;
#45796=EDGE_LOOP ( 'NONE', ( #12428, #4761, #32078, #27279 ) ) ;
#45806=CARTESIAN_POINT ( 'NONE',  ( 10.00000000000000000, -6.903761155838323837, 77.19088730480521576 ) ) ;
#45807=DIRECTION ( 'NONE',  ( -1.000000000000000000, 0.000000000000000000, 0.000000000000000000 ) ) ;
#45810=CIRCLE ( 'NONE', #20782, 82.00000000000000000 ) ;
#45813=CIRCLE ( 'NONE', #16112, 77.49899999999999523 ) ;
#45814=CARTESIAN_POINT ( 'NONE',  ( 10.00000000000000000, 34.44570377933695227, -69.42325613327405165 ) ) ;
#45823=CIRCLE ( 'NONE', #33334, 31.99999999999999645 ) ;
#45824=DIRECTION ( 'NONE',  ( 0.000000000000000000, -0.7071067811865536790, 0.7071067811865412445 ) ) ;
#45831=ORIENTED_EDGE ( 'NONE', *, *, #1678, .F. ) ;
#45837=DIRECTION ( 'NONE',  ( 0.000000000000000000, -0.6494480483301739993, -0.7604059656000392575 ) ) ;
#45838=SHAPE_DEFINITION_REPRESENTATION ( #20629, #31260 ) ;
#45846=ORIENTED_EDGE ( 'NONE', *, *, #3350, .F. ) ;
#45849=ORIENTED_EDGE ( 'NONE', *, *, #7463, .F. ) ;
#45852=CARTESIAN_POINT ( 'NONE',  ( 10.00000000000000000, 0.000000000000000000, 0.000000000000000000 ) ) ;
#45853=ORIENTED_EDGE ( 'NONE', *, *, #23798, .T. ) ;
#45854=AXIS2_PLACEMENT_3D ( 'NONE', #23768, #1004, #27216 ) ;
#45861=ORIENTED_EDGE ( 'NONE', *, *, #33262, .F. ) ;
#45875=ADVANCED_FACE ( 'NONE', ( #14509 ), #6682, .T. ) ;
#45883=CARTESIAN_POINT ( 'NONE',  ( 10.00000000000000000, -73.95703589263958122, -23.16143007188506431 ) ) ;
#45884=DIRECTION ( 'NONE',  ( -1.000000000000000000, 0.000000000000000000, 0.000000000000000000 ) ) ;
#45895=DIRECTION ( 'NONE',  ( 1.000000000000000000, 0.000000000000000000, 0.000000000000000000 ) ) ;
#45900=VERTEX_POINT ( 'NONE', #25741 ) ;
#45902=CARTESIAN_POINT ( 'NONE',  ( -10.00000000000000000, 0.000000000000000000, 0.000000000000000000 ) ) ;
#45903=DIRECTION ( 'NONE',  ( -1.000000000000000000, 0.000000000000000000, -0.000000000000000000 ) ) ;
#45907=VERTEX_POINT ( 'NONE', #11325 ) ;
#45908=VERTEX_POINT ( 'NONE', #10335 ) ;
#45909=ORIENTED_EDGE ( 'NONE', *, *, #9116, .T. ) ;
#45910=FACE_OUTER_BOUND ( 'NONE', #23279, .T. ) ;
#45911=DIRECTION ( 'NONE',  ( 0.000000000000000000, 0.9876883405951383255, -0.1564344650402276216 ) ) ;
#45915=ORIENTED_EDGE ( 'NONE', *, *, #39126, .T. ) ;
#45916=CARTESIAN_POINT ( 'NONE',  ( 0.000000000000000000, -60.67117009219176538, 55.16347631943019536 ) ) ;
#45924=FACE_OUTER_BOUND ( 'NONE', #35110, .T. ) ;
#45937=EDGE_CURVE ( 'NONE', #8725, #23235, #19215, .T. ) ;
#45938=EDGE_CURVE ( 'NONE', #25055, #25836, #8259, .T. ) ;
#45941=ADVANCED_FACE ( 'NONE', ( #18413 ), #10831, .T. ) ;
#45942=VECTOR ( 'NONE', #23817, 1000.000000000000000 ) ;
#45948=EDGE_CURVE ( 'NONE', #37098, #9486, #37999, .T. ) ;
#45949=ORIENTED_EDGE ( 'NONE', *, *, #43655, .F. ) ;
#45950=CARTESIAN_POINT ( 'NONE',  ( 0.000000000000000000, 0.000000000000000000, 77.49899999999999523 ) ) ;
#45953=VECTOR ( 'NONE', #37869, 1000.000000000000000 ) ;
#45960=DIRECTION ( 'NONE',  ( 0.000000000000000000, 0.000000000000000000, 1.000000000000000000 ) ) ;
#45963=CARTESIAN_POINT ( 'NONE',  ( 0.000000000000000000, -18.89407956138203204, -75.16055320797050854 ) ) ;
#45965=VERTEX_POINT ( 'NONE', #280 ) ;
#45970=CARTESIAN_POINT ( 'NONE',  ( 10.00000000000000000, -2.956366410621191765, 75.11725578898467859 ) ) ;
#45980=DIRECTION ( 'NONE',  ( -1.000000000000000000, -0.000000000000000000, 0.000000000000000000 ) ) ;
#45983=VERTEX_POINT ( 'NONE', #11794 ) ;
#45989=VERTEX_POINT ( 'NONE', #19841 ) ;
#45999=CIRCLE ( 'NONE', #24873, 82.00000000000000000 ) ;
#46010=VERTEX_POINT ( 'NONE', #15237 ) ;
#46013=DIRECTION ( 'NONE',  ( -1.000000000000000000, -0.000000000000000000, 0.000000000000000000 ) ) ;
#46015=DIRECTION ( 'NONE',  ( -1.000000000000000000, 0.000000000000000000, -0.000000000000000000 ) ) ;
#46016=ORIENTED_EDGE ( 'NONE', *, *, #14825, .F. ) ;
#46017=ORIENTED_EDGE ( 'NONE', *, *, #41853, .T. ) ;
#46031=DIRECTION ( 'NONE',  ( 0.000000000000000000, 0.000000000000000000, 1.000000000000000000 ) ) ;
#46038=ORIENTED_EDGE ( 'NONE', *, *, #33746, .T. ) ;
#46047=CARTESIAN_POINT ( 'NONE',  ( 10.00000000000000000, 0.000000000000000000, 0.000000000000000000 ) ) ;
#46049=ORIENTED_EDGE ( 'NONE', *, *, #33419, .T. ) ;
#46050=AXIS2_PLACEMENT_3D ( 'NONE', #38369, #26151, #26876 ) ;
#46053=DIRECTION ( 'NONE',  ( -1.000000000000000000, -0.000000000000000000, 0.000000000000000000 ) ) ;
#46057=ADVANCED_FACE ( 'NONE', ( #24492 ), #31865, .T. ) ;
#46066=CARTESIAN_POINT ( 'NONE',  ( 0.000000000000000000, -75.16055320797043748, 18.89407956138229494 ) ) ;
#46076=ORIENTED_EDGE ( 'NONE', *, *, #43769, .F. ) ;
#46082=VERTEX_POINT ( 'NONE', #5656 ) ;
#46083=ORIENTED_EDGE ( 'NONE', *, *, #40581, .F. ) ;
#46088=EDGE_LOOP ( 'NONE', ( #19076, #24849, #11883, #43120 ) ) ;
#46096=ORIENTED_EDGE ( 'NONE', *, *, #37164, .T. ) ;
#46097=ADVANCED_FACE ( 'NONE', ( #35510 ), #24247, .T. ) ;
#46102=EDGE_LOOP ( 'NONE', ( #46049, #7725, #12998, #22200 ) ) ;
#46104=DIRECTION ( 'NONE',  ( 0.000000000000000000, -0.4539904997395541875, 0.8910065241883642351 ) ) ;
#46107=FACE_OUTER_BOUND ( 'NONE', #41870, .T. ) ;
#46113=CARTESIAN_POINT ( 'NONE',  ( 10.00000000000000000, 31.46837873495072913, -68.27212725128242710 ) ) ;
#46119=ORIENTED_EDGE ( 'NONE', *, *, #44736, .F. ) ;
#46120=EDGE_CURVE ( 'NONE', #23364, #41584, #12980, .T. ) ;
#46122=ORIENTED_EDGE ( 'NONE', *, *, #5478, .F. ) ;
#46125=CARTESIAN_POINT ( 'NONE',  ( 5.000000000000000000, 55.16347631943042984, 60.67117009219156643 ) ) ;
#46126=VERTEX_POINT ( 'NONE', #20570 ) ;
#46129=ORIENTED_EDGE ( 'NONE', *, *, #26800, .T. ) ;
#46131=ORIENTED_EDGE ( 'NONE', *, *, #37032, .T. ) ;
#46134=AXIS2_PLACEMENT_3D ( 'NONE', #9397, #46626, #1095 ) ;
#46138=AXIS2_PLACEMENT_3D ( 'NONE', #21309, #44321, #36247 ) ;
#46142=ORIENTED_EDGE ( 'NONE', *, *, #45336, .F. ) ;
#46144=ADVANCED_FACE ( 'NONE', ( #42375 ), #8829, .T. ) ;
#46145=COLOUR_RGB ( '', 0.66274510, 0.83137255, 0.94901961) ;
#46146=CARTESIAN_POINT ( 'NONE',  ( 0.000000000000000000, 0.000000000000000000, 0.000000000000000000 ) ) ;
#46147=CARTESIAN_POINT ( 'NONE',  ( -10.00000000000000000, 0.000000000000000000, 0.000000000000000000 ) ) ;
#46158=LINE ( 'NONE', #16534, #22858 ) ;
#46159=LINE ( 'NONE', #23880, #2647 ) ;
#46160=CARTESIAN_POINT ( 'NONE',  ( 10.00000000000000000, 0.000000000000000000, 0.000000000000000000 ) ) ;
#46162=CARTESIAN_POINT ( 'NONE',  ( 10.00000000000000000, 0.000000000000000000, 0.000000000000000000 ) ) ;
#46165=DIRECTION ( 'NONE',  ( 0.000000000000000000, 0.000000000000000000, -1.000000000000000000 ) ) ;
#46182=ORIENTED_EDGE ( 'NONE', *, *, #7656, .T. ) ;
#46183=ORIENTED_EDGE ( 'NONE', *, *, #26691, .F. ) ;
#46186=DIRECTION ( 'NONE',  ( 0.000000000000000000, 0.5224985647159441360, 0.8526401643540951758 ) ) ;
#46197=ORIENTED_EDGE ( 'NONE', *, *, #43061, .T. ) ;
#46212=EDGE_CURVE ( 'NONE', #44331, #1101, #14444, .T. ) ;
#46217=AXIS2_PLACEMENT_3D ( 'NONE', #26169, #33499, #14429 ) ;
#46220=CARTESIAN_POINT ( 'NONE',  ( 0.000000000000000000, 0.000000000000000000, 0.000000000000000000 ) ) ;
#46223=AXIS2_PLACEMENT_3D ( 'NONE', #32254, #28585, #43516 ) ;
#46228=DIRECTION ( 'NONE',  ( -1.000000000000000000, 0.000000000000000000, 0.000000000000000000 ) ) ;
#46231=DIRECTION ( 'NONE',  ( 0.000000000000000000, 0.2334453638558990629, 0.9723699203976782224 ) ) ;
#46234=VERTEX_POINT ( 'NONE', #48209 ) ;
#46236=ORIENTED_EDGE ( 'NONE', *, *, #33225, .T. ) ;
#46238=CIRCLE ( 'NONE', #4830, 77.49900000000000944 ) ;
#46239=EDGE_CURVE ( 'NONE', #27291, #6602, #6379, .T. ) ;
#46240=VECTOR ( 'NONE', #30993, 1000.000000000000000 ) ;
#46248=EDGE_CURVE ( 'NONE', #8812, #19820, #34098, .T. ) ;
#46249=ORIENTED_EDGE ( 'NONE', *, *, #46970, .F. ) ;
#46258=ADVANCED_FACE ( 'NONE', ( #44298 ), #21773, .T. ) ;
#46259=EDGE_CURVE ( 'NONE', #35449, #17495, #44269, .T. ) ;
#46261=EDGE_LOOP ( 'NONE', ( #8029, #4901, #38821, #22495 ) ) ;
#46267=DIRECTION ( 'NONE',  ( 0.000000000000000000, 0.000000000000000000, -1.000000000000000000 ) ) ;
#46268=ORIENTED_EDGE ( 'NONE', *, *, #47365, .F. ) ;
#46272=CARTESIAN_POINT ( 'NONE',  ( 10.00000000000000000, 0.000000000000000000, 0.000000000000000000 ) ) ;
#46276=DIRECTION ( 'NONE',  ( 1.000000000000000000, 0.000000000000000000, 0.000000000000000000 ) ) ;
#46282=DIRECTION ( 'NONE',  ( -1.000000000000000000, -0.000000000000000000, 0.000000000000000000 ) ) ;
#46298=VERTEX_POINT ( 'NONE', #17857 ) ;
#46308=AXIS2_PLACEMENT_3D ( 'NONE', #13307, #40463, #28721 ) ;
#46310=AXIS2_PLACEMENT_3D ( 'NONE', #40377, #17349, #6836 ) ;
#46311=CARTESIAN_POINT ( 'NONE',  ( 0.000000000000000000, -21.60688246758530440, -79.10210256391390260 ) ) ;
#46312=ORIENTED_EDGE ( 'NONE', *, *, #8611, .T. ) ;
#46313=FILL_AREA_STYLE_COLOUR ( '', #46145 ) ;
#46315=EDGE_CURVE ( 'NONE', #47056, #24088, #32564, .T. ) ;
#46317=DIRECTION ( 'NONE',  ( 0.000000000000000000, 0.1564344650402311743, -0.9876883405951377704 ) ) ;
#46335=DIRECTION ( 'NONE',  ( 0.000000000000000000, 0.8910065241883655673, 0.4539904997395510233 ) ) ;
#46337=VERTEX_POINT ( 'NONE', #45264 ) ;
#46340=DIRECTION ( 'NONE',  ( -1.000000000000000000, 0.000000000000000000, -0.000000000000000000 ) ) ;
#46354=ORIENTED_EDGE ( 'NONE', *, *, #45775, .F. ) ;
#46355=CARTESIAN_POINT ( 'NONE',  ( 0.000000000000000000, -51.29473840253177741, -63.97538442413482329 ) ) ;
#46357=ORIENTED_EDGE ( 'NONE', *, *, #44695, .F. ) ;
#46359=EDGE_CURVE ( 'NONE', #23354, #46842, #33512, .T. ) ;
#46360=VERTEX_POINT ( 'NONE', #27159 ) ;
#46366=EDGE_CURVE ( 'NONE', #12926, #371, #34469, .T. ) ;
#46369=ORIENTED_EDGE ( 'NONE', *, *, #13271, .F. ) ;
#46370=ADVANCED_FACE ( 'NONE', ( #8050 ), #23460, .T. ) ;
#46372=AXIS2_PLACEMENT_3D ( 'NONE', #48135, #40793, #7742 ) ;
#46381=DIRECTION ( 'NONE',  ( 1.000000000000000000, -0.000000000000000000, 0.000000000000000000 ) ) ;
#46383=FACE_OUTER_BOUND ( 'NONE', #34598, .T. ) ;
#46393=DIRECTION ( 'NONE',  ( -1.000000000000000000, 0.000000000000000000, 0.000000000000000000 ) ) ;
#46404=CARTESIAN_POINT ( 'NONE',  ( 0.000000000000000000, 30.41916302227216562, -71.27951684757994144 ) ) ;
#46405=EDGE_CURVE ( 'NONE', #11579, #33952, #4407, .T. ) ;
#46413=CARTESIAN_POINT ( 'NONE',  ( 10.00000000000000000, -62.50329211542407393, -41.76937507738853839 ) ) ;
#46416=CARTESIAN_POINT ( 'NONE',  ( 10.00000000000000178, 0.000000000000000000, 0.000000000000000000 ) ) ;
#46422=CIRCLE ( 'NONE', #25288, 31.99999999999999645 ) ;
#46430=AXIS2_PLACEMENT_3D ( 'NONE', #14021, #40940, #21616 ) ;
#46433=CIRCLE ( 'NONE', #22977, 82.00000000000000000 ) ;
#46443=CIRCLE ( 'NONE', #23763, 32.00000000000000000 ) ;
#46444=DIRECTION ( 'NONE',  ( 0.000000000000000000, -0.1564344650402170744, -0.9876883405951398798 ) ) ;
#46448=CIRCLE ( 'NONE', #1082, 31.99999999999999289 ) ;
#46449=CYLINDRICAL_SURFACE ( 'NONE', #36064, 82.00000000000000000 ) ;
#46450=VERTEX_POINT ( 'NONE', #11981 ) ;
#46452=ORIENTED_EDGE ( 'NONE', *, *, #6328, .F. ) ;
#46455=CIRCLE ( 'NONE', #42543, 31.99999999999998579 ) ;
#46467=EDGE_CURVE ( 'NONE', #18434, #773, #20025, .T. ) ;
#46479=DIRECTION ( 'NONE',  ( 0.000000000000000000, -0.4539904997395350361, -0.8910065241883738940 ) ) ;
#46482=DIRECTION ( 'NONE',  ( -1.000000000000000000, 0.000000000000000000, 0.000000000000000000 ) ) ;
#46484=LINE ( 'NONE', #28113, #9693 ) ;
#46485=DIRECTION ( 'NONE',  ( 1.000000000000000000, 0.000000000000000000, 0.000000000000000000 ) ) ;
#46492=CIRCLE ( 'NONE', #12879, 31.99999999999999289 ) ;
#46495=AXIS2_PLACEMENT_3D ( 'NONE', #42444, #6214, #24571 ) ;
#46497=CARTESIAN_POINT ( 'NONE',  ( -10.00000000000000000, 0.000000000000000000, 0.000000000000000000 ) ) ;
#46498=DIRECTION ( 'NONE',  ( -1.000000000000000000, 0.000000000000000000, 0.000000000000000000 ) ) ;
#46501=CIRCLE ( 'NONE', #20707, 31.99999999999999289 ) ;
#46503=CARTESIAN_POINT ( 'NONE',  ( 0.000000000000000000, -54.21277698773715059, 55.38113227695762930 ) ) ;
#46505=EDGE_LOOP ( 'NONE', ( #5595, #33001, #46129, #47332 ) ) ;
#46510=DIRECTION ( 'NONE',  ( 0.000000000000000000, -0.9723699203976789995, 0.2334453638558956767 ) ) ;
#46515=CARTESIAN_POINT ( 'NONE',  ( 10.00000000000000000, -31.46837873494930093, -68.27212725128309501 ) ) ;
#46520=VERTEX_POINT ( 'NONE', #20771 ) ;
#46523=DIRECTION ( 'NONE',  ( 0.000000000000000000, 0.000000000000000000, 1.000000000000000000 ) ) ;
#46531=EDGE_CURVE ( 'NONE', #17307, #41084, #40370, .T. ) ;
#46537=CARTESIAN_POINT ( 'NONE',  ( 10.00000000000000000, -55.20638768913797634, 51.02545421589302777 ) ) ;
#46541=CARTESIAN_POINT ( 'NONE',  ( 0.000000000000000000, 16.00000000000000000, 2.500000000000000000 ) ) ;
#46544=CARTESIAN_POINT ( 'NONE',  ( 10.00000000000000000, -67.80270845531855173, -46.11716303203261447 ) ) ;
#46546=EDGE_CURVE ( 'NONE', #7240, #10549, #8321, .T. ) ;
#46548=AXIS2_PLACEMENT_3D ( 'NONE', #48311, #7194, #29475 ) ;
#46560=VERTEX_POINT ( 'NONE', #24685 ) ;
#46568=DIRECTION ( 'NONE',  ( -1.000000000000000000, 0.000000000000000000, -0.000000000000000000 ) ) ;
#46575=VERTEX_POINT ( 'NONE', #19783 ) ;
#46579=DIRECTION ( 'NONE',  ( -1.000000000000000000, -0.000000000000000000, -0.000000000000000000 ) ) ;
#46584=CARTESIAN_POINT ( 'NONE',  ( 0.000000000000000000, -2.956366410620109519, -75.11725578898472122 ) ) ;
#46586=ORIENTED_EDGE ( 'NONE', *, *, #46910, .T. ) ;
#46589=EDGE_CURVE ( 'NONE', #34506, #20063, #41185, .T. ) ;
#46590=LINE ( 'NONE', #13056, #20614 ) ;
#46592=CARTESIAN_POINT ( 'NONE',  ( 0.000000000000000000, 62.20884554314020676, 46.21855187248652896 ) ) ;
#46593=DIRECTION ( 'NONE',  ( 1.000000000000000000, 0.000000000000000000, 0.000000000000000000 ) ) ;
#46599=LINE ( 'NONE', #34580, #20364 ) ;
#46603=DIRECTION ( 'NONE',  ( -1.000000000000000000, 0.000000000000000000, -0.000000000000000000 ) ) ;
#46606=CARTESIAN_POINT ( 'NONE',  ( 5.000000000000000000, 79.10210256391368944, 21.60688246758614284 ) ) ;
#46608=AXIS2_PLACEMENT_3D ( 'NONE', #9201, #35379, #8958 ) ;
#46609=EDGE_CURVE ( 'NONE', #14073, #13144, #23711, .T. ) ;
#46612=CARTESIAN_POINT ( 'NONE',  ( 10.00000000000000000, 73.95703589263975175, 23.16143007188454206 ) ) ;
#46616=DIRECTION ( 'NONE',  ( 1.000000000000000000, 0.000000000000000000, 0.000000000000000000 ) ) ;
#46620=AXIS2_PLACEMENT_3D ( 'NONE', #763, #30405, #15703 ) ;
#46622=AXIS2_PLACEMENT_3D ( 'NONE', #7375, #33786, #3946 ) ;
#46626=DIRECTION ( 'NONE',  ( -1.000000000000000000, -0.000000000000000000, -0.000000000000000000 ) ) ;
#46635=FACE_OUTER_BOUND ( 'NONE', #16945, .T. ) ;
#46638=VERTEX_POINT ( 'NONE', #40348 ) ;
#46640=DIRECTION ( 'NONE',  ( -1.000000000000000000, -0.000000000000000000, -0.000000000000000000 ) ) ;
#46646=CARTESIAN_POINT ( 'NONE',  ( 10.00000000000000178, 12.24744871391589029, 2.499999999999999556 ) ) ;
#46652=ORIENTED_EDGE ( 'NONE', *, *, #31188, .T. ) ;
#46653=DIRECTION ( 'NONE',  ( 0.000000000000000000, -0.6494480483301739993, -0.7604059656000392575 ) ) ;
#46661=FACE_OUTER_BOUND ( 'NONE', #34933, .T. ) ;
#46666=DIRECTION ( 'NONE',  ( -1.000000000000000000, -0.000000000000000000, 0.000000000000000000 ) ) ;
#46684=VECTOR ( 'NONE', #15643, 1000.000000000000000 ) ;
#46685=CARTESIAN_POINT ( 'NONE',  ( 10.00000000000000000, -30.41916302227060598, -71.27951684758059514 ) ) ;
#46686=ORIENTED_EDGE ( 'NONE', *, *, #3455, .F. ) ;
#46694=DIRECTION ( 'NONE',  ( 0.000000000000000000, 0.07845909572784512398, -0.9969173337331279638 ) ) ;
#46697=DIRECTION ( 'NONE',  ( 0.000000000000000000, 0.7071067811865489050, -0.7071067811865462405 ) ) ;
#46698=ORIENTED_EDGE ( 'NONE', *, *, #27913, .F. ) ;
#46700=DIRECTION ( 'NONE',  ( -1.000000000000000000, 0.000000000000000000, 0.000000000000000000 ) ) ;
#46701=ORIENTED_EDGE ( 'NONE', *, *, #34036, .F. ) ;
#46702=DIRECTION ( 'NONE',  ( -1.000000000000000000, 0.000000000000000000, 0.000000000000000000 ) ) ;
#46714=VECTOR ( 'NONE', #19402, 1000.000000000000000 ) ;
#46715=EDGE_LOOP ( 'NONE', ( #46652, #5305, #38631, #11757 ) ) ;
#46737=ORIENTED_EDGE ( 'NONE', *, *, #37141, .F. ) ;
#46738=AXIS2_PLACEMENT_3D ( 'NONE', #40748, #33637, #22626 ) ;
#46743=EDGE_CURVE ( 'NONE', #38555, #15249, #47421, .T. ) ;
#46744=AXIS2_PLACEMENT_3D ( 'NONE', #264, #29890, #22789 ) ;
#46746=DIRECTION ( 'NONE',  ( -1.000000000000000000, 0.000000000000000000, 0.000000000000000000 ) ) ;
#46749=ORIENTED_EDGE ( 'NONE', *, *, #40834, .T. ) ;
#46756=ORIENTED_EDGE ( 'NONE', *, *, #47613, .F. ) ;
#46757=EDGE_CURVE ( 'NONE', #16336, #39882, #14145, .T. ) ;
#46758=CARTESIAN_POINT ( 'NONE',  ( 10.00000000000000000, 41.19522573413826194, -65.64334221924865176 ) ) ;
#46765=VERTEX_POINT ( 'NONE', #34409 ) ;
#46769=DIRECTION ( 'NONE',  ( 0.000000000000000000, 0.000000000000000000, 1.000000000000000000 ) ) ;
#46770=CARTESIAN_POINT ( 'NONE',  ( 0.000000000000000000, -51.02545421589363883, 55.20638768913742922 ) ) ;
#46772=ORIENTED_EDGE ( 'NONE', *, *, #15487, .T. ) ;
#46779=DIRECTION ( 'NONE',  ( -1.000000000000000000, 0.000000000000000000, 0.000000000000000000 ) ) ;
#46782=DIRECTION ( 'NONE',  ( 0.000000000000000000, 0.000000000000000000, 1.000000000000000000 ) ) ;
#46783=DIRECTION ( 'NONE',  ( -1.000000000000000000, 0.000000000000000000, 0.000000000000000000 ) ) ;
#46791=ORIENTED_EDGE ( 'NONE', *, *, #34726, .T. ) ;
#46799=CARTESIAN_POINT ( 'NONE',  ( -10.00000000000000000, 0.000000000000000000, 0.000000000000000000 ) ) ;
#46803=CARTESIAN_POINT ( 'NONE',  ( 0.000000000000000000, -58.39081064771787766, 50.95692526931307498 ) ) ;
#46807=FACE_OUTER_BOUND ( 'NONE', #14670, .T. ) ;
#46808=VERTEX_POINT ( 'NONE', #41788 ) ;
#46809=VERTEX_POINT ( 'NONE', #4097 ) ;
#46817=LINE ( 'NONE', #36020, #27350 ) ;
#46826=ADVANCED_FACE ( 'NONE', ( #41306 ), #41542, .T. ) ;
#46830=DIRECTION ( 'NONE',  ( 0.000000000000000000, 0.000000000000000000, 1.000000000000000000 ) ) ;
#46840=DIRECTION ( 'NONE',  ( -1.000000000000000000, 0.000000000000000000, 0.000000000000000000 ) ) ;
#46842=VERTEX_POINT ( 'NONE', #22927 ) ;
#46848=AXIS2_PLACEMENT_3D ( 'NONE', #19278, #23198, #11700 ) ;
#46858=EDGE_CURVE ( 'NONE', #16326, #41579, #37868, .T. ) ;
#46874=AXIS2_PLACEMENT_3D ( 'NONE', #22799, #41645, #15696 ) ;
#46876=ORIENTED_EDGE ( 'NONE', *, *, #2877, .F. ) ;
#46878=CARTESIAN_POINT ( 'NONE',  ( 10.00000000000000000, 60.67117009219215618, -55.16347631942976193 ) ) ;
#46884=DIRECTION ( 'NONE',  ( 0.000000000000000000, 0.000000000000000000, 1.000000000000000000 ) ) ;
#46890=DIRECTION ( 'NONE',  ( 0.000000000000000000, 0.7604059656000323741, -0.6494480483301819929 ) ) ;
#46891=CYLINDRICAL_SURFACE ( 'NONE', #18401, 31.99999999999999289 ) ;
#46894=DIRECTION ( 'NONE',  ( 0.000000000000000000, 0.000000000000000000, 1.000000000000000000 ) ) ;
#46898=DIRECTION ( 'NONE',  ( 0.000000000000000000, 0.000000000000000000, -1.000000000000000000 ) ) ;
#46900=ORIENTED_EDGE ( 'NONE', *, *, #40596, .F. ) ;
#46910=EDGE_CURVE ( 'NONE', #21719, #15799, #30242, .T. ) ;
#46917=DIRECTION ( 'NONE',  ( -1.000000000000000000, 0.000000000000000000, 0.000000000000000000 ) ) ;
#46918=DIRECTION ( 'NONE',  ( -1.000000000000000000, 0.000000000000000000, 0.000000000000000000 ) ) ;
#46949=FACE_OUTER_BOUND ( 'NONE', #14695, .T. ) ;
#46959=CARTESIAN_POINT ( 'NONE',  ( 0.000000000000000000, 51.02545421589324803, 55.20638768913779870 ) ) ;
#46962=ORIENTED_EDGE ( 'NONE', *, *, #39230, .T. ) ;
#46970=EDGE_CURVE ( 'NONE', #41232, #36602, #47447, .T. ) ;
#46973=EDGE_CURVE ( 'NONE', #10347, #38387, #6062, .T. ) ;
#46975=AXIS2_PLACEMENT_3D ( 'NONE', #1554, #46593, #16725 ) ;
#46982=CIRCLE ( 'NONE', #8669, 77.49899999999999523 ) ;
#46983=DIRECTION ( 'NONE',  ( 0.000000000000000000, 0.9510565162951523099, 0.3090169943749513926 ) ) ;
#46995=EDGE_CURVE ( 'NONE', #11808, #27040, #13082, .T. ) ;
#47003=DIRECTION ( 'NONE',  ( -1.000000000000000000, 0.000000000000000000, 0.000000000000000000 ) ) ;
#47014=CARTESIAN_POINT ( 'NONE',  ( 10.00000000000000000, 0.000000000000000000, 0.000000000000000000 ) ) ;
#47017=DIRECTION ( 'NONE',  ( 0.000000000000000000, 0.000000000000000000, 1.000000000000000000 ) ) ;
#47020=DIRECTION ( 'NONE',  ( 0.000000000000000000, 0.000000000000000000, 1.000000000000000000 ) ) ;
#47021=CIRCLE ( 'NONE', #117, 82.00000000000000000 ) ;
#47022=EDGE_CURVE ( 'NONE', #23694, #13395, #9932, .T. ) ;
#47031=DIRECTION ( 'NONE',  ( 0.000000000000000000, 0.000000000000000000, 1.000000000000000000 ) ) ;
#47033=DIRECTION ( 'NONE',  ( 0.000000000000000000, 0.000000000000000000, -1.000000000000000000 ) ) ;
#47035=LINE ( 'NONE', #5208, #21910 ) ;
#47036=ORIENTED_EDGE ( 'NONE', *, *, #11509, .T. ) ;
#47037=AXIS2_PLACEMENT_3D ( 'NONE', #39180, #36410, #43992 ) ;
#47045=EDGE_LOOP ( 'NONE', ( #48309, #32702, #29519, #22958 ) ) ;
#47048=AXIS2_PLACEMENT_3D ( 'NONE', #16306, #26598, #22913 ) ;
#47051=CARTESIAN_POINT ( 'NONE',  ( 10.00000000000000000, 78.73519480814954363, 22.90783923731657978 ) ) ;
#47053=CARTESIAN_POINT ( 'NONE',  ( 0.000000000000000000, 65.58780272294076497, 36.73666225445916211 ) ) ;
#47056=VERTEX_POINT ( 'NONE', #36591 ) ;
#47059=FACE_OUTER_BOUND ( 'NONE', #38378, .T. ) ;
#47062=VERTEX_POINT ( 'NONE', #32456 ) ;
#47064=DIRECTION ( 'NONE',  ( -1.000000000000000000, 0.000000000000000000, -0.000000000000000000 ) ) ;
#47070=DIRECTION ( 'NONE',  ( 0.000000000000000000, 0.000000000000000000, -1.000000000000000000 ) ) ;
#47073=DIRECTION ( 'NONE',  ( 1.000000000000000000, 0.000000000000000000, -0.000000000000000000 ) ) ;
#47074=ORIENTED_EDGE ( 'NONE', *, *, #101, .F. ) ;
#47075=CIRCLE ( 'NONE', #9531, 82.00000000000000000 ) ;
#47077=DIRECTION ( 'NONE',  ( 0.000000000000000000, 0.9876883405951383255, -0.1564344650402277048 ) ) ;
#47083=LINE ( 'NONE', #2518, #5729 ) ;
#47085=ORIENTED_EDGE ( 'NONE', *, *, #3543, .T. ) ;
#47088=AXIS2_PLACEMENT_3D ( 'NONE', #35649, #20715, #2121 ) ;
#47090=ORIENTED_EDGE ( 'NONE', *, *, #7066, .F. ) ;
#47107=ORIENTED_EDGE ( 'NONE', *, *, #46366, .T. ) ;
#47114=CARTESIAN_POINT ( 'NONE',  ( 10.00000000000000000, 0.000000000000000000, 0.000000000000000000 ) ) ;
#47115=DIRECTION ( 'NONE',  ( 0.000000000000000000, 0.000000000000000000, -1.000000000000000000 ) ) ;
#47118=DIRECTION ( 'NONE',  ( -1.000000000000000000, -0.000000000000000000, -0.000000000000000000 ) ) ;
#47119=EDGE_CURVE ( 'NONE', #36392, #36384, #29494, .T. ) ;
#47121=VECTOR ( 'NONE', #23390, 1000.000000000000000 ) ;
#47125=DIRECTION ( 'NONE',  ( -1.000000000000000000, 0.000000000000000000, 0.000000000000000000 ) ) ;
#47134=CIRCLE ( 'NONE', #15108, 31.99999999999999645 ) ;
#47135=ADVANCED_FACE ( 'NONE', ( #28541 ), #43476, .T. ) ;
#47136=CYLINDRICAL_SURFACE ( 'NONE', #13476, 31.99999999999999289 ) ;
#47140=AXIS2_PLACEMENT_3D ( 'NONE', #13244, #35754, #32092 ) ;
#47144=AXIS2_PLACEMENT_3D ( 'NONE', #11193, #3604, #29064 ) ;
#47149=ORIENTED_EDGE ( 'NONE', *, *, #5196, .F. ) ;
#47150=AXIS2_PLACEMENT_3D ( 'NONE', #41466, #12105, #7921 ) ;
#47158=VERTEX_POINT ( 'NONE', #29002 ) ;
#47159=CIRCLE ( 'NONE', #17454, 32.00000000000000000 ) ;
#47162=ORIENTED_EDGE ( 'NONE', *, *, #14697, .T. ) ;
#47169=CARTESIAN_POINT ( 'NONE',  ( 5.000000000000002665, -80.55351364060578589, -15.33399622253568673 ) ) ;
#47182=CIRCLE ( 'NONE', #41697, 77.49899999999998101 ) ;
#47192=AXIS2_PLACEMENT_3D ( 'NONE', #32907, #14577, #18475 ) ;
#47199=DIRECTION ( 'NONE',  ( -1.000000000000000000, 0.000000000000000000, 0.000000000000000000 ) ) ;
#47201=CIRCLE ( 'NONE', #1898, 77.49899999999999523 ) ;
#47203=ADVANCED_FACE ( 'NONE', ( #10895 ), #14579, .T. ) ;
#47205=EDGE_LOOP ( 'NONE', ( #20718, #42546, #35012, #36721 ) ) ;
#47206=CARTESIAN_POINT ( 'NONE',  ( 10.00000000000000000, 0.000000000000000000, 0.000000000000000000 ) ) ;
#47210=EDGE_CURVE ( 'NONE', #16837, #42551, #29496, .T. ) ;
#47211=AXIS2_PLACEMENT_3D ( 'NONE', #24789, #21094, #27990 ) ;
#47218=ORIENTED_EDGE ( 'NONE', *, *, #41018, .F. ) ;
#47222=VECTOR ( 'NONE', #43879, 1000.000000000000000 ) ;
#47225=ORIENTED_EDGE ( 'NONE', *, *, #45312, .T. ) ;
#47226=AXIS2_PLACEMENT_3D ( 'NONE', #4866, #936, #15884 ) ;
#47231=VECTOR ( 'NONE', #151, 1000.000000000000000 ) ;
#47232=ORIENTED_EDGE ( 'NONE', *, *, #11556, .T. ) ;
#47235=DIRECTION ( 'NONE',  ( 0.000000000000000000, 0.000000000000000000, 1.000000000000000000 ) ) ;
#47241=ORIENTED_EDGE ( 'NONE', *, *, #29576, .F. ) ;
#47243=CARTESIAN_POINT ( 'NONE',  ( 0.000000000000000000, 50.95692526931414790, -58.39081064771693974 ) ) ;
#47246=CIRCLE ( 'NONE', #22227, 77.49899999999999523 ) ;
#47248=CARTESIAN_POINT ( 'NONE',  ( 10.00000000000000000, -14.66109333815513160, 73.73191006444567108 ) ) ;
#47249=EDGE_CURVE ( 'NONE', #41560, #747, #16984, .T. ) ;
#47251=VERTEX_POINT ( 'NONE', #22867 ) ;
#47254=DIRECTION ( 'NONE',  ( -1.000000000000000000, 0.000000000000000000, 0.000000000000000000 ) ) ;
#47257=DIRECTION ( 'NONE',  ( 0.000000000000000000, 0.000000000000000000, 1.000000000000000000 ) ) ;
#47259=CARTESIAN_POINT ( 'NONE',  ( 5.000000000000002665, 10.30890764327382847, 81.34940948281339956 ) ) ;
#47267=AXIS2_PLACEMENT_3D ( 'NONE', #45555, #34537, #30898 ) ;
#47271=AXIS2_PLACEMENT_3D ( 'NONE', #35595, #32167, #24094 ) ;
#47275=ORIENTED_EDGE ( 'NONE', *, *, #41435, .T. ) ;
#47279=ORIENTED_EDGE ( 'NONE', *, *, #11543, .F. ) ;
#47283=LINE ( 'NONE', #40647, #14396 ) ;
#47293=VERTEX_POINT ( 'NONE', #7932 ) ;
#47297=ORIENTED_EDGE ( 'NONE', *, *, #44156, .T. ) ;
#47299=ORIENTED_EDGE ( 'NONE', *, *, #7520, .F. ) ;
#47301=ADVANCED_FACE ( 'NONE', ( #37804 ), #26061, .T. ) ;
#47302=CARTESIAN_POINT ( 'NONE',  ( 10.00000000000000000, 74.65374052328660071, -8.840884882374309583 ) ) ;
#47306=VECTOR ( 'NONE', #19708, 1000.000000000000000 ) ;
#47311=EDGE_CURVE ( 'NONE', #41579, #23140, #6855, .T. ) ;
#47317=CARTESIAN_POINT ( 'NONE',  ( 10.00000000000000000, 0.000000000000000000, 0.000000000000000000 ) ) ;
#47325=CARTESIAN_POINT ( 'NONE',  ( 5.000000000000002665, -71.87247863392386193, -39.47590169984923136 ) ) ;
#47331=CARTESIAN_POINT ( 'NONE',  ( 10.00000000000000000, -76.69515212745996280, -29.01471420065644580 ) ) ;
#47332=ORIENTED_EDGE ( 'NONE', *, *, #36306, .T. ) ;
#47334=ADVANCED_FACE ( 'NONE', ( #7470 ), #26312, .T. ) ;
#47341=ADVANCED_FACE ( 'NONE', ( #12120 ), #43106, .T. ) ;
#47358=CARTESIAN_POINT ( 'NONE',  ( 0.000000000000000000, -36.73666225445845157, -65.58780272294114866 ) ) ;
#47365=EDGE_CURVE ( 'NONE', #16326, #47293, #26391, .T. ) ;
#47367=CARTESIAN_POINT ( 'NONE',  ( 0.000000000000000000, 16.00000000000000000, -2.500000000000000000 ) ) ;
#47375=LINE ( 'NONE', #32203, #47835 ) ;
#47382=CARTESIAN_POINT ( 'NONE',  ( 10.00000000000000000, -75.11764819372145041, -2.946379043147127064 ) ) ;
#47383=CARTESIAN_POINT ( 'NONE',  ( 10.00000000000000000, 65.59268652807210742, 36.72794159290264560 ) ) ;
#47388=EDGE_LOOP ( 'NONE', ( #21093, #29514, #14789, #30326 ) ) ;
#47389=CARTESIAN_POINT ( 'NONE',  ( 5.000000000000000000, 2.543863470248396208, 81.96053171279903893 ) ) ;
#47394=AXIS2_PLACEMENT_3D ( 'NONE', #15416, #4872, #30345 ) ;
#47398=ORIENTED_EDGE ( 'NONE', *, *, #46995, .F. ) ;
#47399=AXIS2_PLACEMENT_3D ( 'NONE', #45970, #46700, #35901 ) ;
#47405=DIRECTION ( 'NONE',  ( -1.000000000000000000, 0.000000000000000000, 0.000000000000000000 ) ) ;
#47407=CARTESIAN_POINT ( 'NONE',  ( 10.00000000000000000, -41.76106447765533147, 62.50884508063410294 ) ) ;
#47408=ORIENTED_EDGE ( 'NONE', *, *, #39456, .F. ) ;
#47416=EDGE_CURVE ( 'NONE', #29028, #13811, #39681, .T. ) ;
#47421=CIRCLE ( 'NONE', #17711, 77.49899999999999523 ) ;
#47424=CYLINDRICAL_SURFACE ( 'NONE', #20983, 82.00000000000000000 ) ;
#47434=DIRECTION ( 'NONE',  ( -1.000000000000000000, -0.000000000000000000, -0.000000000000000000 ) ) ;
#47435=AXIS2_PLACEMENT_3D ( 'NONE', #32949, #18014, #26096 ) ;
#47436=DIRECTION ( 'NONE',  ( -1.000000000000000000, 0.000000000000000000, 0.000000000000000000 ) ) ;
#47437=CARTESIAN_POINT ( 'NONE',  ( 0.000000000000000000, 81.34940948281337114, 10.30890764327411979 ) ) ;
#47439=LINE ( 'NONE', #13427, #15139 ) ;
#47446=ORIENTED_EDGE ( 'NONE', *, *, #3543, .F. ) ;
#47447=CIRCLE ( 'NONE', #13855, 77.49899999999999523 ) ;
#47450=ADVANCED_FACE ( 'NONE', ( #20835 ), #43586, .T. ) ;
#47453=ORIENTED_EDGE ( 'NONE', *, *, #15432, .F. ) ;
#47455=AXIS2_PLACEMENT_3D ( 'NONE', #29947, #32890, #3268 ) ;
#47457=VERTEX_POINT ( 'NONE', #27044 ) ;
#47463=DIRECTION ( 'NONE',  ( 1.000000000000000000, 0.000000000000000000, -0.000000000000000000 ) ) ;
#47466=CARTESIAN_POINT ( 'NONE',  ( 0.000000000000000000, 6.903761155837774943, 77.19088730480525840 ) ) ;
#47469=DIRECTION ( 'NONE',  ( 0.000000000000000000, -0.9510565162951565288, 0.3090169943749382919 ) ) ;
#47470=FACE_OUTER_BOUND ( 'NONE', #6116, .T. ) ;
#47472=ORIENTED_EDGE ( 'NONE', *, *, #45948, .T. ) ;
#47480=CYLINDRICAL_SURFACE ( 'NONE', #26080, 82.00000000000000000 ) ;
#47481=CARTESIAN_POINT ( 'NONE',  ( 5.000000000000002665, 8.966570791700698706, 81.50828551894228724 ) ) ;
#47483=AXIS2_PLACEMENT_3D ( 'NONE', #18599, #47491, #25933 ) ;
#47484=CYLINDRICAL_SURFACE ( 'NONE', #9879, 82.00000000000000000 ) ;
#47485=CARTESIAN_POINT ( 'NONE',  ( 5.000000000000002665, -34.94270380257693631, 74.18225833017875459 ) ) ;
#47489=LINE ( 'NONE', #47259, #5342 ) ;
#47491=DIRECTION ( 'NONE',  ( -1.000000000000000000, 0.000000000000000000, -0.000000000000000000 ) ) ;
#47492=ORIENTED_EDGE ( 'NONE', *, *, #471, .T. ) ;
#47495=FACE_OUTER_BOUND ( 'NONE', #32739, .T. ) ;
#47507=VECTOR ( 'NONE', #47879, 1000.000000000000000 ) ;
#47512=DIRECTION ( 'NONE',  ( 0.000000000000000000, 0.000000000000000000, 1.000000000000000000 ) ) ;
#47517=ADVANCED_FACE ( 'NONE', ( #11013 ), #29852, .T. ) ;
#47538=ADVANCED_FACE ( 'NONE', ( #48216 ), #21554, .T. ) ;
#47550=DIRECTION ( 'NONE',  ( 0.000000000000000000, 0.000000000000000000, 1.000000000000000000 ) ) ;
#47551=ORIENTED_EDGE ( 'NONE', *, *, #29512, .T. ) ;
#47557=EDGE_CURVE ( 'NONE', #45718, #30853, #38908, .T. ) ;
#47559=EDGE_CURVE ( 'NONE', #8929, #16330, #22477, .T. ) ;
#47560=AXIS2_PLACEMENT_3D ( 'NONE', #46146, #35611, #42468 ) ;
#47562=FACE_OUTER_BOUND ( 'NONE', #10854, .T. ) ;
#47565=DIRECTION ( 'NONE',  ( 1.000000000000000000, 0.000000000000000000, 0.000000000000000000 ) ) ;
#47570=DIRECTION ( 'NONE',  ( 0.000000000000000000, 0.000000000000000000, 1.000000000000000000 ) ) ;
#47572=ADVANCED_FACE ( 'NONE', ( #33520 ), #48448, .T. ) ;
#47574=CIRCLE ( 'NONE', #29620, 31.99999999999999289 ) ;
#47579=EDGE_CURVE ( 'NONE', #37275, #10994, #2939, .T. ) ;
#47582=DIRECTION ( 'NONE',  ( 0.000000000000000000, -0.9238795325112822976, -0.3826834323651008285 ) ) ;
#47584=LINE ( 'NONE', #14064, #35295 ) ;
#47589=DIRECTION ( 'NONE',  ( 0.000000000000000000, -0.3090169943749548898, 0.9510565162951511997 ) ) ;
#47594=CIRCLE ( 'NONE', #33544, 77.49899999999999523 ) ;
#47604=ORIENTED_EDGE ( 'NONE', *, *, #436, .T. ) ;
#47609=ORIENTED_EDGE ( 'NONE', *, *, #31092, .F. ) ;
#47613=EDGE_CURVE ( 'NONE', #16358, #33111, #36548, .T. ) ;
#47614=CARTESIAN_POINT ( 'NONE',  ( 0.000000000000000000, -69.42325613327415113, -34.44570377933673200 ) ) ;
#47619=DIRECTION ( 'NONE',  ( 0.000000000000000000, 0.000000000000000000, 1.000000000000000000 ) ) ;
#47622=CARTESIAN_POINT ( 'NONE',  ( 0.000000000000000000, 0.000000000000000000, 0.000000000000000000 ) ) ;
#47624=AXIS2_PLACEMENT_3D ( 'NONE', #6760, #14097, #39584 ) ;
#47629=ORIENTED_EDGE ( 'NONE', *, *, #46120, .F. ) ;
#47633=ORIENTED_EDGE ( 'NONE', *, *, #5376, .F. ) ;
#47636=ORIENTED_EDGE ( 'NONE', *, *, #7937, .T. ) ;
#47638=DIRECTION ( 'NONE',  ( -1.000000000000000000, 0.000000000000000000, -0.000000000000000000 ) ) ;
#47646=CARTESIAN_POINT ( 'NONE',  ( 10.00000000000000000, 29.01471420065674423, -76.69515212745983490 ) ) ;
#47648=DIRECTION ( 'NONE',  ( 0.000000000000000000, 0.3826834323650842862, 0.9238795325112890700 ) ) ;
#47656=CARTESIAN_POINT ( 'NONE',  ( 0.000000000000000000, 80.55351364060589958, 15.33399622253511829 ) ) ;
#47657=CIRCLE ( 'NONE', #39082, 77.49899999999999523 ) ;
#47663=VERTEX_POINT ( 'NONE', #34003 ) ;
#47670=VERTEX_POINT ( 'NONE', #12238 ) ;
#47672=DIRECTION ( 'NONE',  ( 0.000000000000000000, 0.3090169943749482839, -0.9510565162951533091 ) ) ;
#47682=LINE ( 'NONE', #14419, #17336 ) ;
#47683=AXIS2_PLACEMENT_3D ( 'NONE', #11377, #19409, #27026 ) ;
#47684=CIRCLE ( 'NONE', #23483, 77.49899999999999523 ) ;
#47692=CYLINDRICAL_SURFACE ( 'NONE', #43108, 31.99999999999999289 ) ;
#47704=DIRECTION ( 'NONE',  ( -1.000000000000000000, 0.000000000000000000, 0.000000000000000000 ) ) ;
#47705=EDGE_CURVE ( 'NONE', #14023, #2189, #17046, .T. ) ;
#47706=CARTESIAN_POINT ( 'NONE',  ( 0.000000000000000000, 16.00000000000000000, 2.500000000000000000 ) ) ;
#47710=DIRECTION ( 'NONE',  ( -1.000000000000000000, 0.000000000000000000, -0.000000000000000000 ) ) ;
#47728=VECTOR ( 'NONE', #2438, 1000.000000000000000 ) ;
#47732=ORIENTED_EDGE ( 'NONE', *, *, #22330, .T. ) ;
#47738=ORIENTED_EDGE ( 'NONE', *, *, #2466, .T. ) ;
#47750=AXIS2_PLACEMENT_3D ( 'NONE', #5278, #1362, #16524 ) ;
#47756=AXIS2_PLACEMENT_3D ( 'NONE', #24946, #28146, #20806 ) ;
#47762=LINE ( 'NONE', #14253, #9338 ) ;
#47772=DIRECTION ( 'NONE',  ( -1.000000000000000000, -0.000000000000000000, 0.000000000000000000 ) ) ;
#47774=EDGE_CURVE ( 'NONE', #7495, #40831, #25638, .T. ) ;
#47778=DIRECTION ( 'NONE',  ( 0.000000000000000000, 0.000000000000000000, 1.000000000000000000 ) ) ;
#47779=DIRECTION ( 'NONE',  ( 0.000000000000000000, 0.000000000000000000, 1.000000000000000000 ) ) ;
#47783=VERTEX_POINT ( 'NONE', #22665 ) ;
#47786=DIRECTION ( 'NONE',  ( 0.000000000000000000, 0.9510565162951521989, 0.3090169943749515591 ) ) ;
#47793=CIRCLE ( 'NONE', #39218, 82.00000000000000000 ) ;
#47794=CARTESIAN_POINT ( 'NONE',  ( 0.000000000000000000, 0.000000000000000000, 0.000000000000000000 ) ) ;
#47797=EDGE_LOOP ( 'NONE', ( #15749, #19435, #40060, #22310 ) ) ;
#47799=EDGE_CURVE ( 'NONE', #29160, #16510, #18741, .T. ) ;
#47806=ORIENTED_EDGE ( 'NONE', *, *, #3866, .T. ) ;
#47808=DIRECTION ( 'NONE',  ( 0.000000000000000000, 0.000000000000000000, 1.000000000000000000 ) ) ;
#47809=DIRECTION ( 'NONE',  ( -1.000000000000000000, 0.000000000000000000, 0.000000000000000000 ) ) ;
#47812=ORIENTED_EDGE ( 'NONE', *, *, #14626, .F. ) ;
#47814=EDGE_LOOP ( 'NONE', ( #3952, #40983, #48268, #943 ) ) ;
#47816=CARTESIAN_POINT ( 'NONE',  ( 0.000000000000000000, 0.000000000000000000, 0.000000000000000000 ) ) ;
#47817=DIRECTION ( 'NONE',  ( -1.000000000000000000, -0.000000000000000000, 0.000000000000000000 ) ) ;
#47819=CARTESIAN_POINT ( 'NONE',  ( 10.00000000000000000, 41.76937507738788469, 62.50329211542452157 ) ) ;
#47829=CYLINDRICAL_SURFACE ( 'NONE', #32612, 32.00000000000000000 ) ;
#47834=EDGE_CURVE ( 'NONE', #11083, #16358, #28007, .T. ) ;
#47835=VECTOR ( 'NONE', #28764, 1000.000000000000000 ) ;
#47838=DIRECTION ( 'NONE',  ( -1.000000000000000000, 0.000000000000000000, 0.000000000000000000 ) ) ;
#47839=ORIENTED_EDGE ( 'NONE', *, *, #35142, .F. ) ;
#47840=EDGE_CURVE ( 'NONE', #6182, #21856, #40550, .T. ) ;
#47841=DIRECTION ( 'NONE',  ( -1.000000000000000000, 0.000000000000000000, -0.000000000000000000 ) ) ;
#47845=ORIENTED_EDGE ( 'NONE', *, *, #33982, .T. ) ;
#47846=EDGE_CURVE ( 'NONE', #25169, #11204, #628, .T. ) ;
#47847=ORIENTED_EDGE ( 'NONE', *, *, #10041, .T. ) ;
#47848=EDGE_CURVE ( 'NONE', #5621, #37239, #17785, .T. ) ;
#47856=DIRECTION ( 'NONE',  ( 0.000000000000000000, 0.000000000000000000, 1.000000000000000000 ) ) ;
#47859=CARTESIAN_POINT ( 'NONE',  ( 5.000000000000002665, -29.01471420065617224, 76.69515212746007649 ) ) ;
#47861=ORIENTED_EDGE ( 'NONE', *, *, #46239, .T. ) ;
#47869=EDGE_CURVE ( 'NONE', #23071, #35415, #41283, .T. ) ;
#47875=DIRECTION ( 'NONE',  ( -1.000000000000000000, 0.000000000000000000, 0.000000000000000000 ) ) ;
#47878=VECTOR ( 'NONE', #42035, 1000.000000000000000 ) ;
#47879=DIRECTION ( 'NONE',  ( 1.000000000000000000, -0.000000000000000000, -0.000000000000000000 ) ) ;
#47880=CARTESIAN_POINT ( 'NONE',  ( 10.00000000000000000, -73.95703589263990807, 23.16143007188399139 ) ) ;
#47881=ORIENTED_EDGE ( 'NONE', *, *, #15046, .T. ) ;
#47887=ORIENTED_EDGE ( 'NONE', *, *, #36519, .T. ) ;
#47891=EDGE_CURVE ( 'NONE', #21969, #46126, #26428, .T. ) ;
#47895=EDGE_CURVE ( 'NONE', #31027, #14287, #23385, .T. ) ;
#47902=EDGE_CURVE ( 'NONE', #37588, #18992, #12380, .T. ) ;
#47903=VECTOR ( 'NONE', #8464, 1000.000000000000000 ) ;
#47907=CARTESIAN_POINT ( 'NONE',  ( 10.00000000000000000, 0.000000000000000000, 0.000000000000000000 ) ) ;
#47909=ORIENTED_EDGE ( 'NONE', *, *, #16082, .T. ) ;
#47910=CIRCLE ( 'NONE', #47150, 31.99999999999999289 ) ;
#47911=ORIENTED_EDGE ( 'NONE', *, *, #19450, .F. ) ;
#47930=AXIS2_PLACEMENT_3D ( 'NONE', #22690, #41079, #18043 ) ;
#47939=CIRCLE ( 'NONE', #29995, 77.49899999999999523 ) ;
#47944=FACE_OUTER_BOUND ( 'NONE', #613, .T. ) ;
#47945=DIRECTION ( 'NONE',  ( 0.000000000000000000, 0.000000000000000000, -1.000000000000000000 ) ) ;
#47948=CIRCLE ( 'NONE', #11207, 32.00000000000000000 ) ;
#47958=CARTESIAN_POINT ( 'NONE',  ( 10.00000000000000000, -72.35160999960831418, 20.41045688087797672 ) ) ;
#47959=EDGE_CURVE ( 'NONE', #37233, #28726, #13143, .T. ) ;
#47968=ORIENTED_EDGE ( 'NONE', *, *, #47119, .T. ) ;
#47975=ORIENTED_EDGE ( 'NONE', *, *, #42945, .T. ) ;
#47976=CIRCLE ( 'NONE', #8920, 31.99999999999999289 ) ;
#47977=AXIS2_PLACEMENT_3D ( 'NONE', #32849, #43, #47778 ) ;
#47979=LINE ( 'NONE', #14707, #12422 ) ;
#47980=CIRCLE ( 'NONE', #20640, 31.99999999999999289 ) ;
#47987=DIRECTION ( 'NONE',  ( -1.000000000000000000, -0.000000000000000000, 0.000000000000000000 ) ) ;
#47990=FACE_OUTER_BOUND ( 'NONE', #11456, .T. ) ;
#47992=ORIENTED_EDGE ( 'NONE', *, *, #36461, .F. ) ;
#47993=DIRECTION ( 'NONE',  ( 0.000000000000000000, 0.000000000000000000, 1.000000000000000000 ) ) ;
#47995=ORIENTED_EDGE ( 'NONE', *, *, #37639, .F. ) ;
#47997=DIRECTION ( 'NONE',  ( 0.000000000000000000, 0.9238795325112851842, 0.3826834323650937786 ) ) ;
#47998=CARTESIAN_POINT ( 'NONE',  ( 10.00000000000000000, -63.18004540533059554, 44.88180994100355292 ) ) ;
#48001=CARTESIAN_POINT ( 'NONE',  ( 10.00000000000000000, 39.78640506895604290, 66.50666863322015843 ) ) ;
#48006=CARTESIAN_POINT ( 'NONE',  ( 10.00000000000000000, 55.19960302592141232, -51.03279382321027668 ) ) ;
#48009=EDGE_LOOP ( 'NONE', ( #21629, #8005, #37208, #45780 ) ) ;
#48044=CIRCLE ( 'NONE', #16019, 31.99999999999999645 ) ;
#48048=VERTEX_POINT ( 'NONE', #31235 ) ;
#48052=AXIS2_PLACEMENT_3D ( 'NONE', #43703, #20954, #39806 ) ;
#48055=AXIS2_PLACEMENT_3D ( 'NONE', #28228, #41535, #16310 ) ;
#48061=VECTOR ( 'NONE', #40669, 1000.000000000000000 ) ;
#48062=ADVANCED_FACE ( 'NONE', ( #44369 ), #14265, .T. ) ;
#48063=VERTEX_POINT ( 'NONE', #6924 ) ;
#48068=LINE ( 'NONE', #39776, #28241 ) ;
#48074=FACE_OUTER_BOUND ( 'NONE', #25687, .T. ) ;
#48078=ORIENTED_EDGE ( 'NONE', *, *, #18560, .F. ) ;
#48081=EDGE_CURVE ( 'NONE', #43442, #33302, #3730, .T. ) ;
#48082=EDGE_CURVE ( 'NONE', #42057, #33952, #666, .T. ) ;
#48088=DIRECTION ( 'NONE',  ( -1.000000000000000000, 0.000000000000000000, -0.000000000000000000 ) ) ;
#48092=CARTESIAN_POINT ( 'NONE',  ( 10.00000000000000000, 0.000000000000000000, 0.000000000000000000 ) ) ;
#48094=EDGE_CURVE ( 'NONE', #6805, #29267, #48348, .T. ) ;
#48095=AXIS2_PLACEMENT_3D ( 'NONE', #45852, #8388, #27005 ) ;
#48105=ORIENTED_EDGE ( 'NONE', *, *, #11111, .F. ) ;
#48107=AXIS2_PLACEMENT_3D ( 'NONE', #35930, #28115, #24918 ) ;
#48108=DIRECTION ( 'NONE',  ( -1.000000000000000000, 0.000000000000000000, 0.000000000000000000 ) ) ;
#48110=ORIENTED_EDGE ( 'NONE', *, *, #40964, .T. ) ;
#48111=AXIS2_PLACEMENT_3D ( 'NONE', #31132, #41187, #30636 ) ;
#48119=ORIENTED_EDGE ( 'NONE', *, *, #18616, .F. ) ;
#48121=EDGE_CURVE ( 'NONE', #48217, #6313, #41313, .T. ) ;
#48126=VECTOR ( 'NONE', #36671, 1000.000000000000000 ) ;
#48131=DIRECTION ( 'NONE',  ( -1.000000000000000000, 0.000000000000000000, -0.000000000000000000 ) ) ;
#48132=DIRECTION ( 'NONE',  ( 1.000000000000000000, -0.000000000000000000, -0.000000000000000000 ) ) ;
#48135=CARTESIAN_POINT ( 'NONE',  ( 10.00000000000000000, -68.26794271651239399, -31.47745569255214093 ) ) ;
#48136=CIRCLE ( 'NONE', #27051, 12.50000000000000000 ) ;
#48138=EDGE_CURVE ( 'NONE', #19466, #25524, #14757, .T. ) ;
#48147=CARTESIAN_POINT ( 'NONE',  ( 10.00000000000000000, 75.11764819372149304, 29.05362095685338986 ) ) ;
#48152=DIRECTION ( 'NONE',  ( 0.000000000000000000, 0.000000000000000000, 1.000000000000000000 ) ) ;
#48155=AXIS2_PLACEMENT_3D ( 'NONE', #11009, #44054, #13953 ) ;
#48158=CARTESIAN_POINT ( 'NONE',  ( 10.00000000000000000, -51.29473840253178452, -63.97538442413483750 ) ) ;
#48164=EDGE_LOOP ( 'NONE', ( #32006, #37706, #38702, #43297 ) ) ;
#48170=VECTOR ( 'NONE', #29968, 1000.000000000000000 ) ;
#48180=EDGE_CURVE ( 'NONE', #22636, #27232, #28035, .T. ) ;
#48182=ORIENTED_EDGE ( 'NONE', *, *, #36034, .F. ) ;
#48186=DIRECTION ( 'NONE',  ( 1.000000000000000000, 0.000000000000000000, 0.000000000000000000 ) ) ;
#48187=CARTESIAN_POINT ( 'NONE',  ( 10.00000000000000000, 71.91182617369189245, 28.89263327155772743 ) ) ;
#48189=EDGE_LOOP ( 'NONE', ( #10235, #6817, #44518, #20524 ) ) ;
#48190=ORIENTED_EDGE ( 'NONE', *, *, #37463, .F. ) ;
#48192=CARTESIAN_POINT ( 'NONE',  ( 10.00000000000000000, 46.54456581323888997, -59.03342792756214408 ) ) ;
#48193=CARTESIAN_POINT ( 'NONE',  ( 10.00000000000000000, 0.000000000000000000, 0.000000000000000000 ) ) ;
#48196=EDGE_CURVE ( 'NONE', #34129, #27354, #8592, .T. ) ;
#48198=DIRECTION ( 'NONE',  ( -1.000000000000000000, 0.000000000000000000, 0.000000000000000000 ) ) ;
#48202=CIRCLE ( 'NONE', #10687, 31.99999999999998934 ) ;
#48207=DIRECTION ( 'NONE',  ( 1.000000000000000000, 0.000000000000000000, 0.000000000000000000 ) ) ;
#48209=CARTESIAN_POINT ( 'NONE',  ( 10.00000000000000000, 63.18004540533029001, 44.88180994100400767 ) ) ;
#48216=FACE_OUTER_BOUND ( 'NONE', #28362, .T. ) ;
#48217=VERTEX_POINT ( 'NONE', #31139 ) ;
#48219=ADVANCED_FACE ( 'NONE', ( #4694 ), #30176, .T. ) ;
#48221=CARTESIAN_POINT ( 'NONE',  ( 10.00000000000000000, 0.000000000000000000, 0.000000000000000000 ) ) ;
#48240=ORIENTED_EDGE ( 'NONE', *, *, #26800, .F. ) ;
#48242=EDGE_LOOP ( 'NONE', ( #22292, #48105, #46791, #16768 ) ) ;
#48244=ORIENTED_EDGE ( 'NONE', *, *, #32459, .T. ) ;
#48248=LINE ( 'NONE', #14725, #15117 ) ;
#48249=DIRECTION ( 'NONE',  ( 0.000000000000000000, 0.5877852522924742473, -0.8090169943749466741 ) ) ;
#48250=VERTEX_POINT ( 'NONE', #38232 ) ;
#48252=DIRECTION ( 'NONE',  ( -1.000000000000000000, 0.000000000000000000, 0.000000000000000000 ) ) ;
#48253=DIRECTION ( 'NONE',  ( 1.000000000000000000, 0.000000000000000000, 0.000000000000000000 ) ) ;
#48263=CARTESIAN_POINT ( 'NONE',  ( 10.00000000000000000, -54.21277698773715059, 55.38113227695762930 ) ) ;
#48265=DIRECTION ( 'NONE',  ( 0.000000000000000000, 0.000000000000000000, 1.000000000000000000 ) ) ;
#48268=ORIENTED_EDGE ( 'NONE', *, *, #2759, .T. ) ;
#48270=CARTESIAN_POINT ( 'NONE',  ( 10.00000000000000000, -41.19522573413687638, -65.64334221924953283 ) ) ;
#48273=CARTESIAN_POINT ( 'NONE',  ( 10.00000000000000000, -80.55351364060578589, -15.33399622253569028 ) ) ;
#48275=DIRECTION ( 'NONE',  ( -1.000000000000000000, 0.000000000000000000, -0.000000000000000000 ) ) ;
#48276=DIRECTION ( 'NONE',  ( -1.000000000000000000, -0.000000000000000000, 0.000000000000000000 ) ) ;
#48277=ORIENTED_EDGE ( 'NONE', *, *, #10976, .T. ) ;
#48282=CYLINDRICAL_SURFACE ( 'NONE', #11191, 31.99999999999999289 ) ;
#48288=DIRECTION ( 'NONE',  ( 0.000000000000000000, -1.000000000000000000, -1.040834085586084730E-14 ) ) ;
#48289=EDGE_LOOP ( 'NONE', ( #45915, #39229, #46962, #10759 ) ) ;
#48291=AXIS2_PLACEMENT_3D ( 'NONE', #46770, #46276, #24234 ) ;
#48292=CARTESIAN_POINT ( 'NONE',  ( 0.000000000000000000, -11.30684508768284680, -76.66974797899850103 ) ) ;
#48297=ORIENTED_EDGE ( 'NONE', *, *, #44353, .F. ) ;
#48300=EDGE_CURVE ( 'NONE', #43833, #24088, #12417, .T. ) ;
#48303=CARTESIAN_POINT ( 'NONE',  ( 0.000000000000000000, 73.73191006444572793, -14.66109333815486515 ) ) ;
#48304=DIRECTION ( 'NONE',  ( -1.000000000000000000, -0.000000000000000000, 0.000000000000000000 ) ) ;
#48306=CARTESIAN_POINT ( 'NONE',  ( 10.00000000000000000, 0.000000000000000000, 0.000000000000000000 ) ) ;
#48309=ORIENTED_EDGE ( 'NONE', *, *, #7949, .F. ) ;
#48311=CARTESIAN_POINT ( 'NONE',  ( 0.000000000000000000, 59.03961581697465277, -46.53671651293886669 ) ) ;
#48315=EDGE_LOOP ( 'NONE', ( #19204, #16503, #33395, #34203 ) ) ;
#48320=AXIS2_PLACEMENT_3D ( 'NONE', #37113, #29534, #7010 ) ;
#48328=DIRECTION ( 'NONE',  ( 0.000000000000000000, 0.3090169943749412895, 0.9510565162951556406 ) ) ;
#48332=CARTESIAN_POINT ( 'NONE',  ( 10.00000000000000000, 0.000000000000000000, 0.000000000000000000 ) ) ;
#48333=FACE_OUTER_BOUND ( 'NONE', #39637, .T. ) ;
#48335=EDGE_CURVE ( 'NONE', #16500, #4758, #45999, .T. ) ;
#48338=AXIS2_PLACEMENT_3D ( 'NONE', #32883, #43449, #28259 ) ;
#48339=ADVANCED_FACE ( 'NONE', ( #45323 ), #34300, .T. ) ;
#48342=ORIENTED_EDGE ( 'NONE', *, *, #37371, .T. ) ;
#48345=ORIENTED_EDGE ( 'NONE', *, *, #36664, .F. ) ;
#48348=CIRCLE ( 'NONE', #38192, 31.99999999999999289 ) ;
#48355=DIRECTION ( 'NONE',  ( 0.000000000000000000, 0.000000000000000000, 1.000000000000000000 ) ) ;
#48370=AXIS2_PLACEMENT_3D ( 'NONE', #33928, #45680, #27092 ) ;
#48374=CYLINDRICAL_SURFACE ( 'NONE', #2581, 32.00000000000000000 ) ;
#48375=CIRCLE ( 'NONE', #46050, 82.00000000000000000 ) ;
#48378=CARTESIAN_POINT ( 'NONE',  ( 10.00000000000000000, -59.03961581697432592, 46.53671651293927880 ) ) ;
#48383=ORIENTED_EDGE ( 'NONE', *, *, #6757, .F. ) ;
#48385=DIRECTION ( 'NONE',  ( 0.000000000000000000, 0.000000000000000000, 1.000000000000000000 ) ) ;
#48392=ADVANCED_FACE ( 'NONE', ( #9098 ), #5663, .T. ) ;
#48395=CARTESIAN_POINT ( 'NONE',  ( 5.000000000000000000, 77.16300072079660310, 27.74655509720696855 ) ) ;
#48400=CIRCLE ( 'NONE', #21803, 31.99999999999998579 ) ;
#48403=CYLINDRICAL_SURFACE ( 'NONE', #33870, 31.99999999999999289 ) ;
#48407=LINE ( 'NONE', #26145, #5399 ) ;
#48410=CARTESIAN_POINT ( 'NONE',  ( 0.000000000000000000, 75.11764819372149304, -2.946379043146603482 ) ) ;
#48419=DIRECTION ( 'NONE',  ( 0.000000000000000000, -0.1564344650402170744, -0.9876883405951398798 ) ) ;
#48420=ORIENTED_EDGE ( 'NONE', *, *, #28883, .F. ) ;
#48423=CIRCLE ( 'NONE', #32799, 77.49899999999999523 ) ;
#48439=CARTESIAN_POINT ( 'NONE',  ( 0.000000000000000000, 71.87247863392471459, -39.47590169984770370 ) ) ;
#48442=DIRECTION ( 'NONE',  ( 0.000000000000000000, -0.5224985647159559043, 0.8526401643540878483 ) ) ;
#48444=EDGE_CURVE ( 'NONE', #8436, #18013, #47574, .T. ) ;
#48446=DIRECTION ( 'NONE',  ( 0.000000000000000000, 0.000000000000000000, 1.000000000000000000 ) ) ;
#48448=CYLINDRICAL_SURFACE ( 'NONE', #1378, 82.00000000000000000 ) ;
#48450=ORIENTED_EDGE ( 'NONE', *, *, #40117, .T. ) ;
#48452=CIRCLE ( 'NONE', #32852, 31.99999999999999645 ) ;
ENDSEC;
END-ISO-10303-21;
